ISO-10303-21;
HEADER;
/* Generated by software containing ST-Developer
 * from STEP Tools, Inc. (www.steptools.com) 
 */

FILE_DESCRIPTION(
/* description */ (''),
/* implementation_level */ '2;1');

FILE_NAME(
/* name */ '04_Inner_Bearing_Cone_L68149.step',
/* time_stamp */ '2026-10-25T01:26:34-07:00',
/* author */ (''),
/* organization */ (''),
/* preprocessor_version */ 'ST-DEVELOPER v20.2',
/* originating_system */ 'Autodesk Translation Framework v15.15.0.0',
/* authorisation */ '');

FILE_SCHEMA (('AUTOMOTIVE_DESIGN { 1 0 10303 214 3 1 1 }'));
ENDSEC;

DATA;
#10=MECHANICAL_DESIGN_GEOMETRIC_PRESENTATION_REPRESENTATION('',(#325),#71628);
#96=TOROIDAL_SURFACE('',#36411,2.22978791005503,0.3);
#97=TOROIDAL_SURFACE('',#36419,2.56984636336567,0.3);
#98=TOROIDAL_SURFACE('',#36424,2.22978791005503,0.3);
#99=TOROIDAL_SURFACE('',#36432,2.56984636336567,0.3);
#100=TOROIDAL_SURFACE('',#36437,2.22978791005503,0.3);
#101=TOROIDAL_SURFACE('',#36445,2.56984636336567,0.3);
#102=TOROIDAL_SURFACE('',#36450,2.22978791005503,0.3);
#103=TOROIDAL_SURFACE('',#36458,2.56984636336567,0.3);
#104=TOROIDAL_SURFACE('',#36463,2.22978791005503,0.3);
#105=TOROIDAL_SURFACE('',#36471,2.56984636336567,0.3);
#106=TOROIDAL_SURFACE('',#36476,2.22978791005503,0.3);
#107=TOROIDAL_SURFACE('',#36484,2.56984636336567,0.3);
#108=TOROIDAL_SURFACE('',#36489,2.22978791005503,0.3);
#109=TOROIDAL_SURFACE('',#36497,2.56984636336567,0.3);
#110=TOROIDAL_SURFACE('',#36502,2.22978791005503,0.3);
#111=TOROIDAL_SURFACE('',#36510,2.56984636336567,0.3);
#112=TOROIDAL_SURFACE('',#36515,2.22978791005503,0.3);
#113=TOROIDAL_SURFACE('',#36523,2.56984636336567,0.3);
#114=TOROIDAL_SURFACE('',#36528,2.22978791005503,0.3);
#115=TOROIDAL_SURFACE('',#36536,2.56984636336567,0.3);
#116=TOROIDAL_SURFACE('',#36541,2.22978791005503,0.3);
#117=TOROIDAL_SURFACE('',#36549,2.56984636336567,0.3);
#118=TOROIDAL_SURFACE('',#36554,2.22978791005503,0.3);
#119=TOROIDAL_SURFACE('',#36562,2.56984636336567,0.3);
#120=TOROIDAL_SURFACE('',#36567,2.22978791005503,0.3);
#121=TOROIDAL_SURFACE('',#36575,2.56984636336567,0.3);
#122=TOROIDAL_SURFACE('',#36580,2.22978791005503,0.3);
#123=TOROIDAL_SURFACE('',#36588,2.56984636336567,0.3);
#124=TOROIDAL_SURFACE('',#36593,2.22978791005503,0.3);
#125=TOROIDAL_SURFACE('',#36601,2.56984636336567,0.3);
#126=TOROIDAL_SURFACE('',#36606,2.22978791005503,0.3);
#127=TOROIDAL_SURFACE('',#36614,2.56984636336567,0.3);
#128=TOROIDAL_SURFACE('',#36619,2.22978791005503,0.3);
#129=TOROIDAL_SURFACE('',#36627,2.56984636336567,0.3);
#130=TOROIDAL_SURFACE('',#36632,2.22978791005503,0.3);
#131=TOROIDAL_SURFACE('',#36640,2.56984636336567,0.3);
#132=TOROIDAL_SURFACE('',#36645,2.22978791005503,0.3);
#133=TOROIDAL_SURFACE('',#36653,2.56984636336567,0.3);
#134=TOROIDAL_SURFACE('',#36658,2.22978791005503,0.3);
#135=TOROIDAL_SURFACE('',#36666,2.56984636336567,0.3);
#136=TOROIDAL_SURFACE('',#36671,2.22978791005503,0.3);
#137=TOROIDAL_SURFACE('',#36679,2.56984636336567,0.3);
#138=TOROIDAL_SURFACE('',#36684,2.22978791005503,0.3);
#139=TOROIDAL_SURFACE('',#36692,2.56984636336567,0.3);
#299=SHAPE_REPRESENTATION_RELATIONSHIP('SRR','None',#71687,#312);
#312=ADVANCED_BREP_SHAPE_REPRESENTATION('',(#338),#71619);
#325=STYLED_ITEM('',(#71818),#338);
#338=MANIFOLD_SOLID_BREP('Body1',#34212);
#483=B_SPLINE_CURVE_WITH_KNOTS('',3,(#58080,#58081,#58082,#58083,#58084,
#58085,#58086,#58087,#58088,#58089,#58090,#58091,#58092,#58093,#58094,#58095,
#58096,#58097,#58098,#58099,#58100,#58101,#58102,#58103,#58104,#58105,#58106,
#58107),.UNSPECIFIED.,.F.,.F.,(4,2,2,2,2,2,2,2,2,2,2,2,2,4),(0.000552255324501238,
0.00250712865869175,0.00542730315934362,0.0100897003910396,0.0208199668277967,
0.03914332528473,0.0566413877982004,0.0737548216775457,0.0916180344917143,
0.113112730500366,0.124811949413757,0.129415141422697,0.131466822655317,
0.132736838801192),.UNSPECIFIED.);
#484=B_SPLINE_CURVE_WITH_KNOTS('',3,(#58116,#58117,#58118,#58119),
 .UNSPECIFIED.,.F.,.F.,(4,4),(0.973845213090798,1.86224631803132),
 .UNSPECIFIED.);
#485=B_SPLINE_CURVE_WITH_KNOTS('',3,(#58124,#58125,#58126,#58127),
 .UNSPECIFIED.,.F.,.F.,(4,4),(1.01459402224647,1.90299512718699),
 .UNSPECIFIED.);
#486=B_SPLINE_CURVE_WITH_KNOTS('',3,(#58132,#58133,#58134,#58135,#58136,
#58137,#58138,#58139,#58140,#58141,#58142,#58143,#58144,#58145,#58146,#58147,
#58148,#58149,#58150,#58151,#58152,#58153,#58154,#58155,#58156,#58157,#58158,
#58159,#58160),.UNSPECIFIED.,.F.,.F.,(4,3,2,2,2,2,2,2,2,2,2,2,2,4),(0.220457494411324,
0.221514163345612,0.224063974278064,0.227827813747527,0.235231812673064,
0.248804927504688,0.261986328480532,0.275641459334015,0.28913004114437,
0.303381192089668,0.310291199891665,0.313709542902219,0.316059908336669,
0.316319431229452),.UNSPECIFIED.);
#487=B_SPLINE_CURVE_WITH_KNOTS('',3,(#58166,#58167,#58168,#58169,#58170,
#58171,#58172,#58173,#58174,#58175,#58176,#58177,#58178,#58179,#58180,#58181,
#58182,#58183,#58184,#58185,#58186,#58187,#58188,#58189,#58190,#58191,#58192,
#58193,#58194,#58195,#58196,#58197),.UNSPECIFIED.,.F.,.F.,(4,2,2,2,2,2,
2,2,2,2,2,2,2,2,2,4),(0.000552255618180187,0.00250735066624725,0.00544388471025156,
0.010201420453688,0.022077523574172,0.0441976068676189,0.055996906725916,
0.0645228057028066,0.0728085455699138,0.0835882268125382,0.102795441848339,
0.125000410030466,0.136058920133137,0.140727854440821,0.142845621851799,
0.144031712293079),.UNSPECIFIED.);
#488=B_SPLINE_CURVE_WITH_KNOTS('',3,(#58206,#58207,#58208,#58209),
 .UNSPECIFIED.,.F.,.F.,(4,4),(1.01302199639782,1.90133038588088),
 .UNSPECIFIED.);
#489=B_SPLINE_CURVE_WITH_KNOTS('',3,(#58214,#58215,#58216,#58217),
 .UNSPECIFIED.,.F.,.F.,(4,4),(1.01910936201615,1.90741775149922),
 .UNSPECIFIED.);
#490=B_SPLINE_CURVE_WITH_KNOTS('',3,(#58222,#58223,#58224,#58225,#58226,
#58227,#58228,#58229,#58230,#58231,#58232,#58233,#58234,#58235,#58236,#58237,
#58238,#58239,#58240,#58241,#58242,#58243,#58244,#58245,#58246,#58247,#58248,
#58249,#58250,#58251,#58252,#58253,#58254),.UNSPECIFIED.,.F.,.F.,(4,3,2,
2,2,2,2,2,2,2,2,2,2,2,2,4),(0.196959320052513,0.198017145092129,0.200540880261076,
0.20420524906308,0.212045863749151,0.231522357859952,0.239816668297063,
0.245036313836856,0.249558567699146,0.254824767282906,0.263328140173216,
0.280727522166969,0.28716729720564,0.290158226145309,0.292204134755108,
0.292205277806419),.UNSPECIFIED.);
#491=B_SPLINE_CURVE_WITH_KNOTS('',3,(#58260,#58261,#58262,#58263,#58264,
#58265,#58266,#58267,#58268,#58269,#58270,#58271,#58272,#58273,#58274,#58275,
#58276,#58277,#58278,#58279,#58280,#58281,#58282,#58283,#58284,#58285,#58286,
#58287,#58288,#58289,#58290,#58291),.UNSPECIFIED.,.F.,.F.,(4,2,2,2,2,2,
2,2,2,2,2,2,2,2,2,4),(0.000552255618326259,0.00250735068795714,0.00544388481129021,
0.0102014206832928,0.0220775241250821,0.0441976080155335,0.0559969081923875,
0.0645228073995753,0.0728085474906832,0.0835882290248828,0.102795444580419,
0.125000413363,0.136058923763291,0.140727858196649,0.142845625664765,0.144031716095406),
 .UNSPECIFIED.);
#492=B_SPLINE_CURVE_WITH_KNOTS('',3,(#58300,#58301,#58302,#58303),
 .UNSPECIFIED.,.F.,.F.,(4,4),(1.02924883146194,1.91752828913416),
 .UNSPECIFIED.);
#493=B_SPLINE_CURVE_WITH_KNOTS('',3,(#58308,#58309,#58310,#58311),
 .UNSPECIFIED.,.F.,.F.,(4,4),(1.020135190352,1.90841464802423),
 .UNSPECIFIED.);
#494=B_SPLINE_CURVE_WITH_KNOTS('',3,(#58316,#58317,#58318,#58319,#58320,
#58321,#58322,#58323,#58324,#58325,#58326,#58327,#58328,#58329,#58330,#58331,
#58332,#58333,#58334,#58335,#58336,#58337,#58338,#58339,#58340,#58341,#58342,
#58343,#58344,#58345,#58346,#58347,#58348),.UNSPECIFIED.,.F.,.F.,(4,3,2,
2,2,2,2,2,2,2,2,2,2,2,2,4),(0.196959320035475,0.198017145075089,0.200540880244035,
0.204205249046031,0.212045863731981,0.231522357842223,0.239816668279115,
0.245036313818745,0.249558567680855,0.254824767264382,0.263328140154285,
0.28072752214711,0.287167297185208,0.290158226124563,0.292204134734147,
0.292205277785457),.UNSPECIFIED.);
#495=B_SPLINE_CURVE_WITH_KNOTS('',3,(#58354,#58355,#58356,#58357,#58358,
#58359,#58360,#58361,#58362,#58363,#58364,#58365,#58366,#58367,#58368,#58369,
#58370,#58371,#58372,#58373,#58374,#58375,#58376,#58377,#58378,#58379,#58380,
#58381,#58382,#58383,#58384,#58385),.UNSPECIFIED.,.F.,.F.,(4,2,2,2,2,2,
2,2,2,2,2,2,2,2,2,4),(0.000552255618176519,0.00250735066570793,0.00544388470773694,
0.0102014204479581,0.0220775235604603,0.0441976068391316,0.0559969066895389,
0.0645228056607815,0.0728085455224931,0.0835882267580784,0.102795441781326,
0.125000409948151,0.136058920042637,0.140727854346809,0.142845621756309,
0.14403171221705),.UNSPECIFIED.);
#496=B_SPLINE_CURVE_WITH_KNOTS('',3,(#58394,#58395,#58396,#58397),
 .UNSPECIFIED.,.F.,.F.,(4,4),(0.992149273556617,1.8805029517096),
 .UNSPECIFIED.);
#497=B_SPLINE_CURVE_WITH_KNOTS('',3,(#58402,#58403,#58404,#58405),
 .UNSPECIFIED.,.F.,.F.,(4,4),(1.01721488555274,1.90556856370572),
 .UNSPECIFIED.);
#498=B_SPLINE_CURVE_WITH_KNOTS('',3,(#58410,#58411,#58412,#58413,#58414,
#58415,#58416,#58417,#58418,#58419,#58420,#58421,#58422,#58423,#58424,#58425,
#58426,#58427,#58428,#58429,#58430,#58431,#58432,#58433,#58434,#58435,#58436,
#58437,#58438),.UNSPECIFIED.,.F.,.F.,(4,3,2,2,2,2,2,2,2,2,2,2,2,4),(0.244877808035713,
0.245941379437421,0.248507773432569,0.2523525700864,0.260140357197957,0.274281958050968,
0.285777166411162,0.296461087015459,0.307606399535247,0.320385682652649,
0.337686825300976,0.344715117359311,0.34902320135799,0.350883558016063),
 .UNSPECIFIED.);
#499=B_SPLINE_CURVE_WITH_KNOTS('',3,(#58444,#58445,#58446,#58447,#58448,
#58449,#58450,#58451,#58452,#58453,#58454,#58455,#58456,#58457,#58458,#58459,
#58460,#58461,#58462,#58463,#58464,#58465,#58466,#58467,#58468,#58469,#58470,
#58471),.UNSPECIFIED.,.F.,.F.,(4,2,2,2,2,2,2,2,2,2,2,2,2,4),(0.00055225541740831,
0.00250719881231768,0.0054323728801237,0.0101226773987657,0.0211144007255414,
0.0395050112937957,0.0554921421757053,0.0705100097030702,0.0866125226194124,
0.105123282533283,0.115750637514577,0.119917613254093,0.121610784601848,
0.122782730208698),.UNSPECIFIED.);
#500=B_SPLINE_CURVE_WITH_KNOTS('',3,(#58480,#58481,#58482,#58483),
 .UNSPECIFIED.,.F.,.F.,(4,4),(0.960106131022675,1.84854766340329),
 .UNSPECIFIED.);
#501=B_SPLINE_CURVE_WITH_KNOTS('',3,(#58488,#58489,#58490,#58491),
 .UNSPECIFIED.,.F.,.F.,(4,4),(1.0115487697186,1.89999030209922),
 .UNSPECIFIED.);
#502=B_SPLINE_CURVE_WITH_KNOTS('',3,(#58496,#58497,#58498,#58499,#58500,
#58501,#58502,#58503,#58504,#58505,#58506,#58507,#58508,#58509,#58510,#58511,
#58512,#58513,#58514,#58515,#58516,#58517,#58518,#58519,#58520,#58521,#58522),
 .UNSPECIFIED.,.F.,.F.,(4,3,2,2,2,2,2,2,2,2,2,2,4),(0.232932117987348,0.233989323147965,
0.236545962444758,0.24033528190873,0.247744949647774,0.261894911831567,
0.277641329371112,0.294641376545692,0.309755553896968,0.323519464298202,
0.330173674908094,0.334332814154483,0.336361587070415),.UNSPECIFIED.);
#503=B_SPLINE_CURVE_WITH_KNOTS('',3,(#58528,#58529,#58530,#58531,#58532,
#58533,#58534,#58535,#58536,#58537,#58538,#58539,#58540,#58541,#58542,#58543,
#58544,#58545,#58546,#58547,#58548,#58549,#58550,#58551,#58552,#58553,#58554,
#58555),.UNSPECIFIED.,.F.,.F.,(4,2,2,2,2,2,2,2,2,2,2,2,2,4),(0.000552255417408364,
0.00250719881231768,0.00543237288013685,0.0101226773988465,0.0211144007254288,
0.0395050112923411,0.0554921421730382,0.0705100096993886,0.0866125226146962,
0.105123282527376,0.115750637508154,0.119917613246771,0.121610784594084,
0.122782730200613),.UNSPECIFIED.);
#504=B_SPLINE_CURVE_WITH_KNOTS('',3,(#58564,#58565,#58566,#58567),
 .UNSPECIFIED.,.F.,.F.,(4,4),(0.960106131022676,1.84854766340329),
 .UNSPECIFIED.);
#505=B_SPLINE_CURVE_WITH_KNOTS('',3,(#58572,#58573,#58574,#58575),
 .UNSPECIFIED.,.F.,.F.,(4,4),(1.0115487697186,1.89999030209922),
 .UNSPECIFIED.);
#506=B_SPLINE_CURVE_WITH_KNOTS('',3,(#58580,#58581,#58582,#58583,#58584,
#58585,#58586,#58587,#58588,#58589,#58590,#58591,#58592,#58593,#58594,#58595,
#58596,#58597,#58598,#58599,#58600,#58601,#58602,#58603,#58604,#58605,#58606),
 .UNSPECIFIED.,.F.,.F.,(4,3,2,2,2,2,2,2,2,2,2,2,4),(0.232932117990906,0.233989323151543,
0.236545962448293,0.240335281912072,0.247744949650985,0.261894911834848,
0.277641329374929,0.294641376550107,0.309755553901947,0.323519464303881,
0.330173674914252,0.334332814160932,0.33636158707699),.UNSPECIFIED.);
#507=B_SPLINE_CURVE_WITH_KNOTS('',3,(#58612,#58613,#58614,#58615,#58616,
#58617,#58618,#58619,#58620,#58621,#58622,#58623,#58624,#58625,#58626,#58627,
#58628,#58629,#58630,#58631,#58632,#58633,#58634,#58635,#58636,#58637,#58638,
#58639,#58640,#58641,#58642,#58643),.UNSPECIFIED.,.F.,.F.,(4,2,2,2,2,2,
2,2,2,2,2,2,2,2,2,4),(0.000552255618199786,0.00250735066915548,0.00544388472378785,
0.0102014204844693,0.0220775236482432,0.0441976070226107,0.0559969069240703,
0.0645228059321239,0.0728085458295457,0.0835882271116238,0.102795442217763,
0.125000410480877,0.136058920623433,0.140727854947894,0.142845622366623,
0.144031712827498),.UNSPECIFIED.);
#508=B_SPLINE_CURVE_WITH_KNOTS('',3,(#58652,#58653,#58654,#58655),
 .UNSPECIFIED.,.F.,.F.,(4,4),(0.992149273556618,1.8805029517096),
 .UNSPECIFIED.);
#509=B_SPLINE_CURVE_WITH_KNOTS('',3,(#58660,#58661,#58662,#58663),
 .UNSPECIFIED.,.F.,.F.,(4,4),(1.01721488555274,1.90556856370572),
 .UNSPECIFIED.);
#510=B_SPLINE_CURVE_WITH_KNOTS('',3,(#58668,#58669,#58670,#58671,#58672,
#58673,#58674,#58675,#58676,#58677,#58678,#58679,#58680,#58681,#58682,#58683,
#58684,#58685,#58686,#58687,#58688,#58689,#58690,#58691,#58692,#58693,#58694,
#58695,#58696),.UNSPECIFIED.,.F.,.F.,(4,3,2,2,2,2,2,2,2,2,2,2,2,4),(0.244877808040074,
0.24594137944178,0.248507773436917,0.25235257009068,0.260140357202121,0.274281958055093,
0.285777166415387,0.296461087019819,0.307606399539854,0.320385682657535,
0.337686825306311,0.3447151173649,0.349023201363699,0.350883558021839),
 .UNSPECIFIED.);
#511=B_SPLINE_CURVE_WITH_KNOTS('',3,(#58702,#58703,#58704,#58705,#58706,
#58707,#58708,#58709,#58710,#58711,#58712,#58713,#58714,#58715,#58716,#58717,
#58718,#58719,#58720,#58721,#58722,#58723,#58724,#58725,#58726,#58727,#58728,
#58729,#58730,#58731,#58732,#58733),.UNSPECIFIED.,.F.,.F.,(4,2,2,2,2,2,
2,2,2,2,2,2,2,2,2,4),(0.000552255618307427,0.00250735068515379,0.00544388479824744,
0.0102014206536779,0.0220775240540609,0.0441976078674591,0.0559969080032229,
0.0645228071807259,0.0728085472428637,0.0835882287392999,0.102795444227548,
0.125000412932329,0.136058923294133,0.14072785771123,0.142845625171944,
0.144031715617256),.UNSPECIFIED.);
#512=B_SPLINE_CURVE_WITH_KNOTS('',3,(#58742,#58743,#58744,#58745),
 .UNSPECIFIED.,.F.,.F.,(4,4),(1.02924883146194,1.91752828913416),
 .UNSPECIFIED.);
#513=B_SPLINE_CURVE_WITH_KNOTS('',3,(#58750,#58751,#58752,#58753),
 .UNSPECIFIED.,.F.,.F.,(4,4),(1.020135190352,1.90841464802423),
 .UNSPECIFIED.);
#514=B_SPLINE_CURVE_WITH_KNOTS('',3,(#58758,#58759,#58760,#58761,#58762,
#58763,#58764,#58765,#58766,#58767,#58768,#58769,#58770,#58771,#58772,#58773,
#58774,#58775,#58776,#58777,#58778,#58779,#58780,#58781,#58782,#58783,#58784,
#58785,#58786,#58787,#58788,#58789,#58790),.UNSPECIFIED.,.F.,.F.,(4,3,2,
2,2,2,2,2,2,2,2,2,2,2,2,4),(0.196959320035786,0.198017145075391,0.20054088024434,
0.204205249046347,0.21204586373224,0.231522357841158,0.239816668277358,
0.24503631381662,0.249558567678421,0.254824767261635,0.263328140151098,
0.280727522143284,0.287167297181241,0.290158226120517,0.292204134730046,
0.292205277781356),.UNSPECIFIED.);
#515=B_SPLINE_CURVE_WITH_KNOTS('',3,(#58796,#58797,#58798,#58799,#58800,
#58801,#58802,#58803,#58804,#58805,#58806,#58807,#58808,#58809,#58810,#58811,
#58812,#58813,#58814,#58815,#58816,#58817,#58818,#58819,#58820,#58821,#58822,
#58823,#58824,#58825,#58826,#58827),.UNSPECIFIED.,.F.,.F.,(4,2,2,2,2,2,
2,2,2,2,2,2,2,2,2,4),(0.000552255618140622,0.00250735066035639,0.00544388468282173,
0.0102014203913002,0.0220775234245199,0.0441976065560588,0.0559969063279555,
0.064522805242411,0.0728085450487638,0.0835882262122293,0.102795441107005,
0.125000409125109,0.136058919145561,0.140727853418389,0.142845620813663,
0.144031711309052),.UNSPECIFIED.);
#516=B_SPLINE_CURVE_WITH_KNOTS('',3,(#58836,#58837,#58838,#58839),
 .UNSPECIFIED.,.F.,.F.,(4,4),(1.01302199639782,1.90133038588089),
 .UNSPECIFIED.);
#517=B_SPLINE_CURVE_WITH_KNOTS('',3,(#58844,#58845,#58846,#58847),
 .UNSPECIFIED.,.F.,.F.,(4,4),(1.01910936201615,1.90741775149922),
 .UNSPECIFIED.);
#518=B_SPLINE_CURVE_WITH_KNOTS('',3,(#58852,#58853,#58854,#58855,#58856,
#58857,#58858,#58859,#58860,#58861,#58862,#58863,#58864,#58865,#58866,#58867,
#58868,#58869,#58870,#58871,#58872,#58873,#58874,#58875,#58876,#58877,#58878,
#58879,#58880,#58881,#58882,#58883,#58884),.UNSPECIFIED.,.F.,.F.,(4,3,2,
2,2,2,2,2,2,2,2,2,2,2,2,4),(0.196959320037348,0.198017145076955,0.200540880245902,
0.204205249047899,0.212045863733824,0.231522357843424,0.239816668280005,
0.245036313819491,0.249558567681539,0.254824767264985,0.263328140154792,
0.280727522147479,0.287167297185466,0.290158226124763,0.292204134734313,
0.292205277785624),.UNSPECIFIED.);
#519=B_SPLINE_CURVE_WITH_KNOTS('',3,(#58890,#58891,#58892,#58893,#58894,
#58895,#58896,#58897,#58898,#58899,#58900,#58901,#58902,#58903,#58904,#58905,
#58906,#58907,#58908,#58909,#58910,#58911,#58912,#58913,#58914,#58915,#58916,
#58917),.UNSPECIFIED.,.F.,.F.,(4,2,2,2,2,2,2,2,2,2,2,2,2,4),(0.000552255324449124,
0.0025071286509707,0.00542730312346706,0.0100897003100863,0.0208199666431741,
0.0391433249235541,0.0566413872684798,0.0737548209829379,0.0916180336249932,
0.113112729425786,0.124811948226245,0.129415140189881,0.131466821402301,
0.132736837572989),.UNSPECIFIED.);
#520=B_SPLINE_CURVE_WITH_KNOTS('',3,(#58926,#58927,#58928,#58929),
 .UNSPECIFIED.,.F.,.F.,(4,4),(0.973845213090799,1.86224631803132),
 .UNSPECIFIED.);
#521=B_SPLINE_CURVE_WITH_KNOTS('',3,(#58934,#58935,#58936,#58937),
 .UNSPECIFIED.,.F.,.F.,(4,4),(1.01459402224647,1.90299512718699),
 .UNSPECIFIED.);
#522=B_SPLINE_CURVE_WITH_KNOTS('',3,(#58942,#58943,#58944,#58945,#58946,
#58947,#58948,#58949,#58950,#58951,#58952,#58953,#58954,#58955,#58956,#58957,
#58958,#58959,#58960,#58961,#58962,#58963,#58964,#58965,#58966,#58967,#58968,
#58969,#58970),.UNSPECIFIED.,.F.,.F.,(4,3,2,2,2,2,2,2,2,2,2,2,2,4),(0.220457494407796,
0.221514163342054,0.224063974274498,0.227827813743946,0.235231812669523,
0.248804927500911,0.26198632847626,0.275641459329111,0.289130041138783,
0.303381192083739,0.310291199885813,0.313709542896337,0.316059908330814,
0.316319431223601),.UNSPECIFIED.);
#523=B_SPLINE_CURVE_WITH_KNOTS('',3,(#58976,#58977,#58978,#58979,#58980,
#58981,#58982,#58983,#58984,#58985,#58986,#58987,#58988,#58989,#58990,#58991),
 .UNSPECIFIED.,.F.,.F.,(4,2,2,2,2,2,2,4),(0.000552255452524527,0.0025072256329463,
0.00543435587026899,0.010135846530597,0.0212263042677829,0.0396611687049569,
0.0549611368371748,0.0626032386529709),.UNSPECIFIED.);
#524=B_SPLINE_CURVE_WITH_KNOTS('',3,(#58999,#59000,#59001,#59002,#59003,
#59004,#59005,#59006,#59007,#59008,#59009,#59010,#59011,#59012,#59013,#59014),
 .UNSPECIFIED.,.F.,.F.,(4,2,2,2,2,2,2,4),(0.0626032386529709,0.0690038332396629,
0.0841023648099793,0.102253718460132,0.114574293882771,0.118850101323579,
0.120613951052394,0.121845703091679),.UNSPECIFIED.);
#525=B_SPLINE_CURVE_WITH_KNOTS('',3,(#59017,#59018,#59019,#59020),
 .UNSPECIFIED.,.F.,.F.,(4,4),(0.952234974413515,1.84070284457626),
 .UNSPECIFIED.);
#526=B_SPLINE_CURVE_WITH_KNOTS('',3,(#59025,#59026,#59027,#59028),
 .UNSPECIFIED.,.F.,.F.,(4,4),(1.00739097317572,1.89585884333848),
 .UNSPECIFIED.);
#527=B_SPLINE_CURVE_WITH_KNOTS('',3,(#59034,#59035,#59036,#59037,#59038,
#59039,#59040,#59041,#59042,#59043,#59044,#59045,#59046,#59047,#59048,#59049),
 .UNSPECIFIED.,.F.,.F.,(4,2,2,2,2,2,2,4),(0.265850124074439,0.273928386135499,
0.284993617049668,0.300677807852058,0.308332988403192,0.3136252683209,0.316793712699132,
0.318373416046925),.UNSPECIFIED.);
#528=B_SPLINE_CURVE_WITH_KNOTS('',3,(#59050,#59051,#59052,#59053,#59054,
#59055,#59056,#59057,#59058,#59059,#59060,#59061,#59062,#59063,#59064,#59065,
#59066,#59067,#59068),.UNSPECIFIED.,.F.,.F.,(4,3,2,2,2,2,2,2,4),(0.214188423781497,
0.215245209126414,0.217829605846206,0.221760415278908,0.229921784182885,
0.245839020956828,0.256431324628773,0.265077654336287,0.265850124074439),
 .UNSPECIFIED.);
#529=B_SPLINE_CURVE_WITH_KNOTS('',3,(#59074,#59075,#59076,#59077,#59078,
#59079,#59080,#59081,#59082,#59083,#59084,#59085,#59086,#59087,#59088,#59089,
#59090,#59091,#59092,#59093,#59094,#59095,#59096,#59097,#59098,#59099,#59100,
#59101),.UNSPECIFIED.,.F.,.F.,(4,2,2,2,2,2,2,2,2,2,2,2,2,4),(0.000552255324103493,
0.00250712859975242,0.00542730288565579,0.0100896997742742,0.0208199654208688,
0.039143322528832,0.0566413837541626,0.0737548163735086,0.0916180278724114,
0.113112722297835,0.124811940352812,0.129415132021259,0.131466813102152,
0.132736829274288),.UNSPECIFIED.);
#530=B_SPLINE_CURVE_WITH_KNOTS('',3,(#59110,#59111,#59112,#59113),
 .UNSPECIFIED.,.F.,.F.,(4,4),(0.973845213090798,1.86224631803132),
 .UNSPECIFIED.);
#531=B_SPLINE_CURVE_WITH_KNOTS('',3,(#59118,#59119,#59120,#59121),
 .UNSPECIFIED.,.F.,.F.,(4,4),(1.01459402224647,1.90299512718699),
 .UNSPECIFIED.);
#532=B_SPLINE_CURVE_WITH_KNOTS('',3,(#59126,#59127,#59128,#59129,#59130,
#59131,#59132,#59133,#59134,#59135,#59136,#59137,#59138,#59139,#59140,#59141,
#59142,#59143,#59144,#59145,#59146,#59147,#59148,#59149,#59150,#59151,#59152,
#59153,#59154),.UNSPECIFIED.,.F.,.F.,(4,3,2,2,2,2,2,2,2,2,2,2,2,4),(0.220457494412775,
0.221514163347042,0.224063974279508,0.227827813749052,0.235231812674751,
0.248804927506449,0.261986328482189,0.275641459335547,0.289130041145789,
0.303381192091107,0.310291199893207,0.313709542903786,0.316059908338292,
0.316319431231083),.UNSPECIFIED.);
#533=B_SPLINE_CURVE_WITH_KNOTS('',3,(#59160,#59161,#59162,#59163,#59164,
#59165,#59166,#59167,#59168,#59169,#59170,#59171,#59172,#59173,#59174,#59175,
#59176,#59177,#59178,#59179,#59180,#59181,#59182,#59183,#59184,#59185,#59186,
#59187,#59188,#59189,#59190,#59191),.UNSPECIFIED.,.F.,.F.,(4,2,2,2,2,2,
2,2,2,2,2,2,2,2,2,4),(0.000552255618150325,0.00250735066180447,0.00544388468956596,
0.010201420406642,0.0220775234613036,0.0441976066326517,0.055996906425799,
0.0645228053555453,0.0728085451768181,0.0835882263598216,0.102795441289329,
0.125000409347919,0.13605891938857,0.140727853669976,0.142845621069164,
0.144031711509465),.UNSPECIFIED.);
#534=B_SPLINE_CURVE_WITH_KNOTS('',3,(#59200,#59201,#59202,#59203),
 .UNSPECIFIED.,.F.,.F.,(4,4),(1.01302199639782,1.90133038588089),
 .UNSPECIFIED.);
#535=B_SPLINE_CURVE_WITH_KNOTS('',3,(#59208,#59209,#59210,#59211),
 .UNSPECIFIED.,.F.,.F.,(4,4),(1.01910936201615,1.90741775149922),
 .UNSPECIFIED.);
#536=B_SPLINE_CURVE_WITH_KNOTS('',3,(#59216,#59217,#59218,#59219,#59220,
#59221,#59222,#59223,#59224,#59225,#59226,#59227,#59228,#59229,#59230,#59231,
#59232,#59233,#59234,#59235,#59236,#59237,#59238,#59239,#59240,#59241,#59242,
#59243,#59244,#59245,#59246,#59247,#59248),.UNSPECIFIED.,.F.,.F.,(4,3,2,
2,2,2,2,2,2,2,2,2,2,2,2,4),(0.196959320041271,0.19801714508091,0.200540880249857,
0.204205249051859,0.212045863737848,0.231522357847912,0.239816668284666,
0.245036313824251,0.249558567686326,0.254824767269862,0.263328140159838,
0.280727522153003,0.287167297191319,0.290158226130778,0.29220413474042,
0.292205277791729),.UNSPECIFIED.);
#537=B_SPLINE_CURVE_WITH_KNOTS('',3,(#59254,#59255,#59256,#59257,#59258,
#59259,#59260,#59261,#59262,#59263,#59264,#59265,#59266,#59267,#59268,#59269,
#59270,#59271,#59272,#59273,#59274,#59275,#59276,#59277,#59278,#59279,#59280,
#59281,#59282,#59283,#59284,#59285),.UNSPECIFIED.,.F.,.F.,(4,2,2,2,2,2,
2,2,2,2,2,2,2,2,2,4),(0.000552255618256276,0.00250735067755829,0.00544388476289,
0.0102014205732942,0.0220775238611849,0.0441976074657267,0.0559969074900062,
0.0645228065868935,0.0728085465706407,0.0835882279650627,0.102795443271529,
0.125000411766022,0.136058922023308,0.140727856396235,0.142845623836849,
0.14403171428955),.UNSPECIFIED.);
#538=B_SPLINE_CURVE_WITH_KNOTS('',3,(#59294,#59295,#59296,#59297),
 .UNSPECIFIED.,.F.,.F.,(4,4),(1.02924883146194,1.91752828913416),
 .UNSPECIFIED.);
#539=B_SPLINE_CURVE_WITH_KNOTS('',3,(#59302,#59303,#59304,#59305),
 .UNSPECIFIED.,.F.,.F.,(4,4),(1.020135190352,1.90841464802423),
 .UNSPECIFIED.);
#540=B_SPLINE_CURVE_WITH_KNOTS('',3,(#59310,#59311,#59312,#59313,#59314,
#59315,#59316,#59317,#59318,#59319,#59320,#59321,#59322,#59323,#59324,#59325,
#59326,#59327,#59328,#59329,#59330,#59331,#59332,#59333,#59334,#59335,#59336,
#59337,#59338,#59339,#59340,#59341,#59342),.UNSPECIFIED.,.F.,.F.,(4,3,2,
2,2,2,2,2,2,2,2,2,2,2,2,4),(0.196959320024652,0.198017145064251,0.200540880233189,
0.204205249035151,0.212045863720946,0.231522357830115,0.239816668266482,
0.245036313805818,0.249558567667623,0.254824767250817,0.263328140140195,
0.280727522132095,0.287167297169923,0.290158226109145,0.292204134718638,
0.292205277769948),.UNSPECIFIED.);
#541=B_SPLINE_CURVE_WITH_KNOTS('',3,(#59348,#59349,#59350,#59351,#59352,
#59353,#59354,#59355,#59356,#59357,#59358,#59359,#59360,#59361,#59362,#59363,
#59364,#59365,#59366,#59367,#59368,#59369,#59370,#59371,#59372,#59373,#59374,
#59375,#59376,#59377,#59378,#59379),.UNSPECIFIED.,.F.,.F.,(4,2,2,2,2,2,
2,2,2,2,2,2,2,2,2,4),(0.000552255618195755,0.00250735066855508,0.00544388472099276,
0.0102014204781084,0.0220775236328774,0.0441976069902035,0.055996906882568,
0.0645228058841012,0.0728085457752267,0.0835882270490723,0.10279544214055,
0.125000410385944,0.136058920518909,0.140727854839246,0.142845622256129,
0.144031712714974),.UNSPECIFIED.);
#542=B_SPLINE_CURVE_WITH_KNOTS('',3,(#59388,#59389,#59390,#59391),
 .UNSPECIFIED.,.F.,.F.,(4,4),(0.992149273556617,1.8805029517096),
 .UNSPECIFIED.);
#543=B_SPLINE_CURVE_WITH_KNOTS('',3,(#59396,#59397,#59398,#59399),
 .UNSPECIFIED.,.F.,.F.,(4,4),(1.01721488555274,1.90556856370572),
 .UNSPECIFIED.);
#544=B_SPLINE_CURVE_WITH_KNOTS('',3,(#59404,#59405,#59406,#59407,#59408,
#59409,#59410,#59411,#59412,#59413,#59414,#59415,#59416,#59417,#59418,#59419,
#59420,#59421,#59422,#59423,#59424,#59425,#59426,#59427,#59428,#59429,#59430,
#59431,#59432),.UNSPECIFIED.,.F.,.F.,(4,3,2,2,2,2,2,2,2,2,2,2,2,4),(0.244877808035147,
0.245941379436854,0.248507773431997,0.252352570085808,0.260140357197332,
0.274281958050489,0.285777166411083,0.296461087015731,0.307606399535822,
0.32038568265349,0.337686825302001,0.344715117360385,0.349023201359046,
0.350883558017123),.UNSPECIFIED.);
#545=B_SPLINE_CURVE_WITH_KNOTS('',3,(#59438,#59439,#59440,#59441,#59442,
#59443,#59444,#59445,#59446,#59447,#59448,#59449,#59450,#59451,#59452,#59453,
#59454,#59455,#59456,#59457,#59458,#59459,#59460,#59461,#59462,#59463,#59464,
#59465),.UNSPECIFIED.,.F.,.F.,(4,2,2,2,2,2,2,2,2,2,2,2,2,4),(0.000552255417408142,
0.00250719881228533,0.00543237287997538,0.0101226773984433,0.021114400724837,
0.0395050112925363,0.0554921421739572,0.0705100097009322,0.0866125226168388,
0.10512328253025,0.115750637511601,0.119917613252859,0.121610784601703,
0.122782730209295),.UNSPECIFIED.);
#546=B_SPLINE_CURVE_WITH_KNOTS('',3,(#59474,#59475,#59476,#59477),
 .UNSPECIFIED.,.F.,.F.,(4,4),(0.960106131022676,1.84854766340329),
 .UNSPECIFIED.);
#547=B_SPLINE_CURVE_WITH_KNOTS('',3,(#59482,#59483,#59484,#59485),
 .UNSPECIFIED.,.F.,.F.,(4,4),(1.0115487697186,1.89999030209922),
 .UNSPECIFIED.);
#548=B_SPLINE_CURVE_WITH_KNOTS('',3,(#59490,#59491,#59492,#59493,#59494,
#59495,#59496,#59497,#59498,#59499,#59500,#59501,#59502,#59503,#59504,#59505,
#59506,#59507,#59508,#59509,#59510,#59511,#59512,#59513,#59514,#59515,#59516),
 .UNSPECIFIED.,.F.,.F.,(4,3,2,2,2,2,2,2,2,2,2,2,4),(0.232932117998903,0.233989323159604,
0.236545962456403,0.240335281920403,0.247744949659532,0.261894911843477,
0.277641329383194,0.294641376558072,0.309755553909664,0.323519464311306,
0.330173674921484,0.334332814168025,0.336361587084032),.UNSPECIFIED.);
#549=B_SPLINE_CURVE_WITH_KNOTS('',3,(#59522,#59523,#59524,#59525,#59526,
#59527,#59528,#59529,#59530,#59531,#59532,#59533,#59534,#59535,#59536,#59537,
#59538,#59539,#59540,#59541,#59542,#59543,#59544,#59545,#59546,#59547,#59548,
#59549),.UNSPECIFIED.,.F.,.F.,(4,2,2,2,2,2,2,2,2,2,2,2,2,4),(0.000552255417408064,
0.00250719881228644,0.00543237287999154,0.0101226773985182,0.0211144007248477,
0.0395050112920569,0.0554921421730817,0.0705100096996193,0.086612522615075,
0.105123282527957,0.115750637508788,0.119917613246066,0.121610784592526,
0.122782730198486),.UNSPECIFIED.);
#550=B_SPLINE_CURVE_WITH_KNOTS('',3,(#59558,#59559,#59560,#59561),
 .UNSPECIFIED.,.F.,.F.,(4,4),(0.960106131022676,1.8485476634033),
 .UNSPECIFIED.);
#551=B_SPLINE_CURVE_WITH_KNOTS('',3,(#59566,#59567,#59568,#59569),
 .UNSPECIFIED.,.F.,.F.,(4,4),(1.0115487697186,1.89999030209922),
 .UNSPECIFIED.);
#552=B_SPLINE_CURVE_WITH_KNOTS('',3,(#59574,#59575,#59576,#59577,#59578,
#59579,#59580,#59581,#59582,#59583,#59584,#59585,#59586,#59587,#59588,#59589,
#59590,#59591,#59592,#59593,#59594,#59595,#59596,#59597,#59598,#59599,#59600),
 .UNSPECIFIED.,.F.,.F.,(4,3,2,2,2,2,2,2,2,2,2,2,4),(0.232932117987128,0.233989323147793,
0.236545962444563,0.240335281908429,0.24774494964748,0.261894911831244,
0.277641329370738,0.294641376545414,0.30975555389686,0.323519464298527,
0.33017367490881,0.3343328141555,0.336361587071577),.UNSPECIFIED.);
#553=B_SPLINE_CURVE_WITH_KNOTS('',3,(#59606,#59607,#59608,#59609,#59610,
#59611,#59612,#59613,#59614,#59615,#59616,#59617,#59618,#59619,#59620,#59621,
#59622,#59623,#59624,#59625,#59626,#59627,#59628,#59629,#59630,#59631,#59632,
#59633,#59634,#59635,#59636,#59637),.UNSPECIFIED.,.F.,.F.,(4,2,2,2,2,2,
2,2,2,2,2,2,2,2,2,4),(0.000552255618197645,0.00250735066884162,0.00544388472231144,
0.0102014204810308,0.0220775236397517,0.044197607004219,0.0559969069004104,
0.0645228059047183,0.0728085457984712,0.0835882270757895,0.102795442173472,
0.125000410426586,0.136058920564129,0.140727854886482,0.142845622304253,
0.144031712762546),.UNSPECIFIED.);
#554=B_SPLINE_CURVE_WITH_KNOTS('',3,(#59646,#59647,#59648,#59649),
 .UNSPECIFIED.,.F.,.F.,(4,4),(0.992149273556617,1.8805029517096),
 .UNSPECIFIED.);
#555=B_SPLINE_CURVE_WITH_KNOTS('',3,(#59654,#59655,#59656,#59657),
 .UNSPECIFIED.,.F.,.F.,(4,4),(1.01721488555274,1.90556856370572),
 .UNSPECIFIED.);
#556=B_SPLINE_CURVE_WITH_KNOTS('',3,(#59662,#59663,#59664,#59665,#59666,
#59667,#59668,#59669,#59670,#59671,#59672,#59673,#59674,#59675,#59676,#59677,
#59678,#59679,#59680,#59681,#59682,#59683,#59684,#59685,#59686,#59687,#59688,
#59689,#59690),.UNSPECIFIED.,.F.,.F.,(4,3,2,2,2,2,2,2,2,2,2,2,2,4),(0.244877808034099,
0.245941379435807,0.248507773430932,0.252352570084648,0.260140357196049,
0.274281958048573,0.28577716640828,0.296461087012187,0.30760639953159,0.320385682648555,
0.337686825296551,0.34471511735484,0.349023201353445,0.350883558011521),
 .UNSPECIFIED.);
#557=B_SPLINE_CURVE_WITH_KNOTS('',3,(#59696,#59697,#59698,#59699,#59700,
#59701,#59702,#59703,#59704,#59705,#59706,#59707,#59708,#59709,#59710,#59711,
#59712,#59713,#59714,#59715,#59716,#59717,#59718,#59719,#59720,#59721,#59722,
#59723,#59724,#59725,#59726,#59727),.UNSPECIFIED.,.F.,.F.,(4,2,2,2,2,2,
2,2,2,2,2,2,2,2,2,4),(0.000552255618249655,0.00250735067656752,0.00544388475827691,
0.0102014205628046,0.0220775238360495,0.0441976074134883,0.055996907423309,
0.0645228065097832,0.0728085464834914,0.0835882278647535,0.102795443147687,
0.125000411614945,0.136058921858814,0.140727856226151,0.142845623664258,
0.144031714104742),.UNSPECIFIED.);
#558=B_SPLINE_CURVE_WITH_KNOTS('',3,(#59736,#59737,#59738,#59739),
 .UNSPECIFIED.,.F.,.F.,(4,4),(1.02924883146194,1.91752828913416),
 .UNSPECIFIED.);
#559=B_SPLINE_CURVE_WITH_KNOTS('',3,(#59744,#59745,#59746,#59747),
 .UNSPECIFIED.,.F.,.F.,(4,4),(1.020135190352,1.90841464802423),
 .UNSPECIFIED.);
#560=B_SPLINE_CURVE_WITH_KNOTS('',3,(#59752,#59753,#59754,#59755,#59756,
#59757,#59758,#59759,#59760,#59761,#59762,#59763,#59764,#59765,#59766,#59767,
#59768,#59769,#59770,#59771,#59772,#59773,#59774,#59775,#59776,#59777,#59778,
#59779,#59780,#59781,#59782,#59783,#59784),.UNSPECIFIED.,.F.,.F.,(4,3,2,
2,2,2,2,2,2,2,2,2,2,2,2,4),(0.196959320042169,0.198017145081817,0.200540880250775,
0.204205249052827,0.212045863738905,0.231522357849409,0.239816668286406,
0.245036313826137,0.249558567688347,0.254824767272002,0.263328140162152,
0.280727522155542,0.287167297193858,0.290158226133316,0.29220413474297,
0.292205277794279),.UNSPECIFIED.);
#561=B_SPLINE_CURVE_WITH_KNOTS('',3,(#59790,#59791,#59792,#59793,#59794,
#59795,#59796,#59797,#59798,#59799,#59800,#59801,#59802,#59803,#59804,#59805,
#59806,#59807,#59808,#59809,#59810,#59811,#59812,#59813,#59814,#59815,#59816,
#59817,#59818,#59819,#59820,#59821),.UNSPECIFIED.,.F.,.F.,(4,2,2,2,2,2,
2,2,2,2,2,2,2,2,2,4),(0.000552255618140626,0.00250735066035772,0.0054438846828297,
0.0102014203913245,0.022077523424572,0.0441976065561941,0.055996906328127,
0.0645228052426097,0.0728085450491545,0.0835882262128905,0.102795441108078,
0.12500040912679,0.136058919148013,0.14072785342133,0.142845620816795,0.144031711312269),
 .UNSPECIFIED.);
#562=B_SPLINE_CURVE_WITH_KNOTS('',3,(#59830,#59831,#59832,#59833),
 .UNSPECIFIED.,.F.,.F.,(4,4),(1.01302199639782,1.90133038588089),
 .UNSPECIFIED.);
#563=B_SPLINE_CURVE_WITH_KNOTS('',3,(#59838,#59839,#59840,#59841),
 .UNSPECIFIED.,.F.,.F.,(4,4),(1.01910936201615,1.90741775149922),
 .UNSPECIFIED.);
#564=B_SPLINE_CURVE_WITH_KNOTS('',3,(#59846,#59847,#59848,#59849,#59850,
#59851,#59852,#59853,#59854,#59855,#59856,#59857,#59858,#59859,#59860,#59861,
#59862,#59863,#59864,#59865,#59866,#59867,#59868,#59869,#59870,#59871,#59872,
#59873,#59874,#59875,#59876,#59877,#59878),.UNSPECIFIED.,.F.,.F.,(4,3,2,
2,2,2,2,2,2,2,2,2,2,2,2,4),(0.19695932004261,0.198017145082242,0.200540880251192,
0.204205249053208,0.212045863739241,0.23152235784927,0.239816668286048,
0.24503631382569,0.24955856768786,0.254824767271468,0.263328140161551,0.280727522154842,
0.287167297192917,0.290158226132224,0.292204134741798,0.292205277793109),
 .UNSPECIFIED.);
#565=B_SPLINE_CURVE_WITH_KNOTS('',3,(#59884,#59885,#59886,#59887,#59888,
#59889,#59890,#59891,#59892,#59893,#59894,#59895,#59896,#59897,#59898,#59899,
#59900,#59901,#59902,#59903,#59904,#59905,#59906,#59907,#59908,#59909,#59910,
#59911),.UNSPECIFIED.,.F.,.F.,(4,2,2,2,2,2,2,2,2,2,2,2,2,4),(0.000552255324019496,
0.00250712858729281,0.00542730282780847,0.0100896996439777,0.0208199651240228,
0.0391433219483803,0.056641382902855,0.0737548152573535,0.0916180264797638,
0.113112720573213,0.124811938447872,0.129415130046053,0.13146681109567,
0.132736827221508),.UNSPECIFIED.);
#566=B_SPLINE_CURVE_WITH_KNOTS('',3,(#59920,#59921,#59922,#59923),
 .UNSPECIFIED.,.F.,.F.,(4,4),(0.973845213090798,1.86224631803132),
 .UNSPECIFIED.);
#567=B_SPLINE_CURVE_WITH_KNOTS('',3,(#59928,#59929,#59930,#59931),
 .UNSPECIFIED.,.F.,.F.,(4,4),(1.01459402224647,1.90299512718699),
 .UNSPECIFIED.);
#568=B_SPLINE_CURVE_WITH_KNOTS('',3,(#59936,#59937,#59938,#59939,#59940,
#59941,#59942,#59943,#59944,#59945,#59946,#59947,#59948,#59949,#59950,#59951,
#59952,#59953,#59954,#59955,#59956,#59957,#59958,#59959,#59960,#59961,#59962,
#59963,#59964),.UNSPECIFIED.,.F.,.F.,(4,3,2,2,2,2,2,2,2,2,2,2,2,4),(0.220457494407383,
0.221514163341664,0.224063974274128,0.227827813743661,0.235231812669406,
0.248804927500478,0.261986328474954,0.275641459327076,0.289130041136135,
0.303381192080165,0.310291199881849,0.313709542892314,0.316059908326691,
0.316319431219465),.UNSPECIFIED.);
#569=B_SPLINE_CURVE_WITH_KNOTS('',3,(#59970,#59971,#59972,#59973,#59974,
#59975,#59976,#59977,#59978,#59979,#59980,#59981,#59982,#59983,#59984,#59985,
#59986,#59987,#59988,#59989,#59990,#59991,#59992,#59993,#59994,#59995,#59996,
#59997),.UNSPECIFIED.,.F.,.F.,(4,2,2,2,2,2,2,2,2,2,2,2,2,4),(0.000552255452470749,
0.0025072256249705,0.00543435583319841,0.0101358464467806,0.0212263040739443,
0.0396611683296533,0.0549611363112922,0.069003832575456,0.0841023639971007,
0.102253717468459,0.114574292768908,0.118850100165663,0.120613949875907,
0.121845701929046),.UNSPECIFIED.);
#570=B_SPLINE_CURVE_WITH_KNOTS('',3,(#60006,#60007,#60008,#60009),
 .UNSPECIFIED.,.F.,.F.,(4,4),(0.952234974413515,1.84070284457626),
 .UNSPECIFIED.);
#571=B_SPLINE_CURVE_WITH_KNOTS('',3,(#60014,#60015,#60016,#60017),
 .UNSPECIFIED.,.F.,.F.,(4,4),(1.00739097317572,1.89585884333848),
 .UNSPECIFIED.);
#572=B_SPLINE_CURVE_WITH_KNOTS('',3,(#60022,#60023,#60024,#60025,#60026,
#60027,#60028,#60029,#60030,#60031,#60032,#60033,#60034,#60035,#60036,#60037,
#60038,#60039,#60040,#60041,#60042,#60043,#60044,#60045,#60046,#60047,#60048,
#60049,#60050,#60051,#60052),.UNSPECIFIED.,.F.,.F.,(4,3,2,2,2,2,2,2,2,2,
2,2,2,2,4),(0.214188423795365,0.215245209140312,0.217829605860112,0.22176041529285,
0.229921784196946,0.245839020971122,0.256431324643212,0.265077654350895,
0.273928386150392,0.28499361706498,0.300677807868051,0.308332988419563,
0.31362526833756,0.316793712715947,0.31837341606385),.UNSPECIFIED.);
#1240=FACE_BOUND('',#6760,.T.);
#1241=FACE_BOUND('',#6765,.T.);
#1242=FACE_BOUND('',#6878,.T.);
#1243=FACE_BOUND('',#6879,.T.);
#1244=FACE_BOUND('',#6880,.T.);
#1245=FACE_BOUND('',#6881,.T.);
#1246=FACE_BOUND('',#6882,.T.);
#1247=FACE_BOUND('',#6883,.T.);
#1248=FACE_BOUND('',#6884,.T.);
#1249=FACE_BOUND('',#6885,.T.);
#1250=FACE_BOUND('',#6886,.T.);
#1251=FACE_BOUND('',#6887,.T.);
#1252=FACE_BOUND('',#6888,.T.);
#1253=FACE_BOUND('',#6889,.T.);
#1254=FACE_BOUND('',#6890,.T.);
#1255=FACE_BOUND('',#6891,.T.);
#1256=FACE_BOUND('',#6892,.T.);
#1257=FACE_BOUND('',#6893,.T.);
#1258=FACE_BOUND('',#6894,.T.);
#1259=FACE_BOUND('',#6895,.T.);
#1260=FACE_BOUND('',#6896,.T.);
#1261=FACE_BOUND('',#6897,.T.);
#1262=FACE_BOUND('',#6898,.T.);
#1263=FACE_BOUND('',#6901,.T.);
#1264=FACE_BOUND('',#6906,.T.);
#2597=PLANE('',#36399);
#2598=PLANE('',#36409);
#2599=PLANE('',#36422);
#2600=PLANE('',#36423);
#2601=PLANE('',#36435);
#2602=PLANE('',#36436);
#2603=PLANE('',#36448);
#2604=PLANE('',#36449);
#2605=PLANE('',#36461);
#2606=PLANE('',#36462);
#2607=PLANE('',#36474);
#2608=PLANE('',#36475);
#2609=PLANE('',#36487);
#2610=PLANE('',#36488);
#2611=PLANE('',#36500);
#2612=PLANE('',#36501);
#2613=PLANE('',#36513);
#2614=PLANE('',#36514);
#2615=PLANE('',#36526);
#2616=PLANE('',#36527);
#2617=PLANE('',#36539);
#2618=PLANE('',#36540);
#2619=PLANE('',#36552);
#2620=PLANE('',#36553);
#2621=PLANE('',#36565);
#2622=PLANE('',#36566);
#2623=PLANE('',#36578);
#2624=PLANE('',#36579);
#2625=PLANE('',#36591);
#2626=PLANE('',#36592);
#2627=PLANE('',#36604);
#2628=PLANE('',#36605);
#2629=PLANE('',#36617);
#2630=PLANE('',#36618);
#2631=PLANE('',#36630);
#2632=PLANE('',#36631);
#2633=PLANE('',#36643);
#2634=PLANE('',#36644);
#2635=PLANE('',#36656);
#2636=PLANE('',#36657);
#2637=PLANE('',#36669);
#2638=PLANE('',#36670);
#2639=PLANE('',#36682);
#2640=PLANE('',#36683);
#2641=PLANE('',#36695);
#2642=PLANE('',#36696);
#2643=PLANE('',#36702);
#2644=PLANE('',#36710);
#3061=CYLINDRICAL_SURFACE('',#36401,25.8846416389917);
#3062=CYLINDRICAL_SURFACE('',#36407,22.7743990607509);
#3063=CYLINDRICAL_SURFACE('',#36706,17.494);
#4553=FACE_OUTER_BOUND('',#6758,.T.);
#4554=FACE_OUTER_BOUND('',#6759,.T.);
#4555=FACE_OUTER_BOUND('',#6761,.T.);
#4556=FACE_OUTER_BOUND('',#6762,.T.);
#4557=FACE_OUTER_BOUND('',#6763,.T.);
#4558=FACE_OUTER_BOUND('',#6764,.T.);
#4559=FACE_OUTER_BOUND('',#6766,.T.);
#4560=FACE_OUTER_BOUND('',#6767,.T.);
#4561=FACE_OUTER_BOUND('',#6768,.T.);
#4562=FACE_OUTER_BOUND('',#6769,.T.);
#4563=FACE_OUTER_BOUND('',#6770,.T.);
#4564=FACE_OUTER_BOUND('',#6771,.T.);
#4565=FACE_OUTER_BOUND('',#6772,.T.);
#4566=FACE_OUTER_BOUND('',#6773,.T.);
#4567=FACE_OUTER_BOUND('',#6774,.T.);
#4568=FACE_OUTER_BOUND('',#6775,.T.);
#4569=FACE_OUTER_BOUND('',#6776,.T.);
#4570=FACE_OUTER_BOUND('',#6777,.T.);
#4571=FACE_OUTER_BOUND('',#6778,.T.);
#4572=FACE_OUTER_BOUND('',#6779,.T.);
#4573=FACE_OUTER_BOUND('',#6780,.T.);
#4574=FACE_OUTER_BOUND('',#6781,.T.);
#4575=FACE_OUTER_BOUND('',#6782,.T.);
#4576=FACE_OUTER_BOUND('',#6783,.T.);
#4577=FACE_OUTER_BOUND('',#6784,.T.);
#4578=FACE_OUTER_BOUND('',#6785,.T.);
#4579=FACE_OUTER_BOUND('',#6786,.T.);
#4580=FACE_OUTER_BOUND('',#6787,.T.);
#4581=FACE_OUTER_BOUND('',#6788,.T.);
#4582=FACE_OUTER_BOUND('',#6789,.T.);
#4583=FACE_OUTER_BOUND('',#6790,.T.);
#4584=FACE_OUTER_BOUND('',#6791,.T.);
#4585=FACE_OUTER_BOUND('',#6792,.T.);
#4586=FACE_OUTER_BOUND('',#6793,.T.);
#4587=FACE_OUTER_BOUND('',#6794,.T.);
#4588=FACE_OUTER_BOUND('',#6795,.T.);
#4589=FACE_OUTER_BOUND('',#6796,.T.);
#4590=FACE_OUTER_BOUND('',#6797,.T.);
#4591=FACE_OUTER_BOUND('',#6798,.T.);
#4592=FACE_OUTER_BOUND('',#6799,.T.);
#4593=FACE_OUTER_BOUND('',#6800,.T.);
#4594=FACE_OUTER_BOUND('',#6801,.T.);
#4595=FACE_OUTER_BOUND('',#6802,.T.);
#4596=FACE_OUTER_BOUND('',#6803,.T.);
#4597=FACE_OUTER_BOUND('',#6804,.T.);
#4598=FACE_OUTER_BOUND('',#6805,.T.);
#4599=FACE_OUTER_BOUND('',#6806,.T.);
#4600=FACE_OUTER_BOUND('',#6807,.T.);
#4601=FACE_OUTER_BOUND('',#6808,.T.);
#4602=FACE_OUTER_BOUND('',#6809,.T.);
#4603=FACE_OUTER_BOUND('',#6810,.T.);
#4604=FACE_OUTER_BOUND('',#6811,.T.);
#4605=FACE_OUTER_BOUND('',#6812,.T.);
#4606=FACE_OUTER_BOUND('',#6813,.T.);
#4607=FACE_OUTER_BOUND('',#6814,.T.);
#4608=FACE_OUTER_BOUND('',#6815,.T.);
#4609=FACE_OUTER_BOUND('',#6816,.T.);
#4610=FACE_OUTER_BOUND('',#6817,.T.);
#4611=FACE_OUTER_BOUND('',#6818,.T.);
#4612=FACE_OUTER_BOUND('',#6819,.T.);
#4613=FACE_OUTER_BOUND('',#6820,.T.);
#4614=FACE_OUTER_BOUND('',#6821,.T.);
#4615=FACE_OUTER_BOUND('',#6822,.T.);
#4616=FACE_OUTER_BOUND('',#6823,.T.);
#4617=FACE_OUTER_BOUND('',#6824,.T.);
#4618=FACE_OUTER_BOUND('',#6825,.T.);
#4619=FACE_OUTER_BOUND('',#6826,.T.);
#4620=FACE_OUTER_BOUND('',#6827,.T.);
#4621=FACE_OUTER_BOUND('',#6828,.T.);
#4622=FACE_OUTER_BOUND('',#6829,.T.);
#4623=FACE_OUTER_BOUND('',#6830,.T.);
#4624=FACE_OUTER_BOUND('',#6831,.T.);
#4625=FACE_OUTER_BOUND('',#6832,.T.);
#4626=FACE_OUTER_BOUND('',#6833,.T.);
#4627=FACE_OUTER_BOUND('',#6834,.T.);
#4628=FACE_OUTER_BOUND('',#6835,.T.);
#4629=FACE_OUTER_BOUND('',#6836,.T.);
#4630=FACE_OUTER_BOUND('',#6837,.T.);
#4631=FACE_OUTER_BOUND('',#6838,.T.);
#4632=FACE_OUTER_BOUND('',#6839,.T.);
#4633=FACE_OUTER_BOUND('',#6840,.T.);
#4634=FACE_OUTER_BOUND('',#6841,.T.);
#4635=FACE_OUTER_BOUND('',#6842,.T.);
#4636=FACE_OUTER_BOUND('',#6843,.T.);
#4637=FACE_OUTER_BOUND('',#6844,.T.);
#4638=FACE_OUTER_BOUND('',#6845,.T.);
#4639=FACE_OUTER_BOUND('',#6846,.T.);
#4640=FACE_OUTER_BOUND('',#6847,.T.);
#4641=FACE_OUTER_BOUND('',#6848,.T.);
#4642=FACE_OUTER_BOUND('',#6849,.T.);
#4643=FACE_OUTER_BOUND('',#6850,.T.);
#4644=FACE_OUTER_BOUND('',#6851,.T.);
#4645=FACE_OUTER_BOUND('',#6852,.T.);
#4646=FACE_OUTER_BOUND('',#6853,.T.);
#4647=FACE_OUTER_BOUND('',#6854,.T.);
#4648=FACE_OUTER_BOUND('',#6855,.T.);
#4649=FACE_OUTER_BOUND('',#6856,.T.);
#4650=FACE_OUTER_BOUND('',#6857,.T.);
#4651=FACE_OUTER_BOUND('',#6858,.T.);
#4652=FACE_OUTER_BOUND('',#6859,.T.);
#4653=FACE_OUTER_BOUND('',#6860,.T.);
#4654=FACE_OUTER_BOUND('',#6861,.T.);
#4655=FACE_OUTER_BOUND('',#6862,.T.);
#4656=FACE_OUTER_BOUND('',#6863,.T.);
#4657=FACE_OUTER_BOUND('',#6864,.T.);
#4658=FACE_OUTER_BOUND('',#6865,.T.);
#4659=FACE_OUTER_BOUND('',#6866,.T.);
#4660=FACE_OUTER_BOUND('',#6867,.T.);
#4661=FACE_OUTER_BOUND('',#6868,.T.);
#4662=FACE_OUTER_BOUND('',#6869,.T.);
#4663=FACE_OUTER_BOUND('',#6870,.T.);
#4664=FACE_OUTER_BOUND('',#6871,.T.);
#4665=FACE_OUTER_BOUND('',#6872,.T.);
#4666=FACE_OUTER_BOUND('',#6873,.T.);
#4667=FACE_OUTER_BOUND('',#6874,.T.);
#4668=FACE_OUTER_BOUND('',#6875,.T.);
#4669=FACE_OUTER_BOUND('',#6876,.T.);
#4670=FACE_OUTER_BOUND('',#6877,.T.);
#4671=FACE_OUTER_BOUND('',#6899,.T.);
#4672=FACE_OUTER_BOUND('',#6900,.T.);
#4673=FACE_OUTER_BOUND('',#6902,.T.);
#4674=FACE_OUTER_BOUND('',#6903,.T.);
#4675=FACE_OUTER_BOUND('',#6904,.T.);
#4676=FACE_OUTER_BOUND('',#6905,.T.);
#6758=EDGE_LOOP('',(#28600,#28601,#28602,#28603,#28604));
#6759=EDGE_LOOP('',(#28605));
#6760=EDGE_LOOP('',(#28606));
#6761=EDGE_LOOP('',(#28607,#28608,#28609,#28610,#28611));
#6762=EDGE_LOOP('',(#28612,#28613,#28614,#28615,#28616));
#6763=EDGE_LOOP('',(#28617,#28618,#28619,#28620,#28621));
#6764=EDGE_LOOP('',(#28622));
#6765=EDGE_LOOP('',(#28623));
#6766=EDGE_LOOP('',(#28624,#28625,#28626,#28627,#28628,#28629));
#6767=EDGE_LOOP('',(#28630,#28631,#28632,#28633,#28634,#28635));
#6768=EDGE_LOOP('',(#28636,#28637,#28638,#28639,#28640,#28641));
#6769=EDGE_LOOP('',(#28642));
#6770=EDGE_LOOP('',(#28643));
#6771=EDGE_LOOP('',(#28644,#28645,#28646,#28647,#28648,#28649));
#6772=EDGE_LOOP('',(#28650,#28651,#28652,#28653,#28654,#28655));
#6773=EDGE_LOOP('',(#28656,#28657,#28658,#28659,#28660,#28661));
#6774=EDGE_LOOP('',(#28662));
#6775=EDGE_LOOP('',(#28663));
#6776=EDGE_LOOP('',(#28664,#28665,#28666,#28667,#28668,#28669));
#6777=EDGE_LOOP('',(#28670,#28671,#28672,#28673,#28674,#28675));
#6778=EDGE_LOOP('',(#28676,#28677,#28678,#28679,#28680,#28681));
#6779=EDGE_LOOP('',(#28682));
#6780=EDGE_LOOP('',(#28683));
#6781=EDGE_LOOP('',(#28684,#28685,#28686,#28687,#28688,#28689));
#6782=EDGE_LOOP('',(#28690,#28691,#28692,#28693,#28694,#28695));
#6783=EDGE_LOOP('',(#28696,#28697,#28698,#28699,#28700,#28701));
#6784=EDGE_LOOP('',(#28702));
#6785=EDGE_LOOP('',(#28703));
#6786=EDGE_LOOP('',(#28704,#28705,#28706,#28707,#28708,#28709));
#6787=EDGE_LOOP('',(#28710,#28711,#28712,#28713,#28714,#28715));
#6788=EDGE_LOOP('',(#28716,#28717,#28718,#28719,#28720,#28721));
#6789=EDGE_LOOP('',(#28722));
#6790=EDGE_LOOP('',(#28723));
#6791=EDGE_LOOP('',(#28724,#28725,#28726,#28727,#28728,#28729));
#6792=EDGE_LOOP('',(#28730,#28731,#28732,#28733,#28734,#28735));
#6793=EDGE_LOOP('',(#28736,#28737,#28738,#28739,#28740,#28741));
#6794=EDGE_LOOP('',(#28742));
#6795=EDGE_LOOP('',(#28743));
#6796=EDGE_LOOP('',(#28744,#28745,#28746,#28747,#28748,#28749));
#6797=EDGE_LOOP('',(#28750,#28751,#28752,#28753,#28754,#28755));
#6798=EDGE_LOOP('',(#28756,#28757,#28758,#28759,#28760,#28761));
#6799=EDGE_LOOP('',(#28762));
#6800=EDGE_LOOP('',(#28763));
#6801=EDGE_LOOP('',(#28764,#28765,#28766,#28767,#28768,#28769));
#6802=EDGE_LOOP('',(#28770,#28771,#28772,#28773,#28774,#28775));
#6803=EDGE_LOOP('',(#28776,#28777,#28778,#28779,#28780,#28781));
#6804=EDGE_LOOP('',(#28782));
#6805=EDGE_LOOP('',(#28783));
#6806=EDGE_LOOP('',(#28784,#28785,#28786,#28787,#28788,#28789));
#6807=EDGE_LOOP('',(#28790,#28791,#28792,#28793,#28794,#28795));
#6808=EDGE_LOOP('',(#28796,#28797,#28798,#28799,#28800,#28801));
#6809=EDGE_LOOP('',(#28802));
#6810=EDGE_LOOP('',(#28803));
#6811=EDGE_LOOP('',(#28804,#28805,#28806,#28807,#28808,#28809));
#6812=EDGE_LOOP('',(#28810,#28811,#28812,#28813,#28814,#28815));
#6813=EDGE_LOOP('',(#28816,#28817,#28818,#28819,#28820,#28821));
#6814=EDGE_LOOP('',(#28822));
#6815=EDGE_LOOP('',(#28823));
#6816=EDGE_LOOP('',(#28824,#28825,#28826,#28827,#28828,#28829,#28830));
#6817=EDGE_LOOP('',(#28831,#28832,#28833,#28834,#28835,#28836));
#6818=EDGE_LOOP('',(#28837,#28838,#28839,#28840,#28841,#28842,#28843));
#6819=EDGE_LOOP('',(#28844));
#6820=EDGE_LOOP('',(#28845));
#6821=EDGE_LOOP('',(#28846,#28847,#28848,#28849,#28850,#28851));
#6822=EDGE_LOOP('',(#28852,#28853,#28854,#28855,#28856,#28857));
#6823=EDGE_LOOP('',(#28858,#28859,#28860,#28861,#28862,#28863));
#6824=EDGE_LOOP('',(#28864));
#6825=EDGE_LOOP('',(#28865));
#6826=EDGE_LOOP('',(#28866,#28867,#28868,#28869,#28870,#28871));
#6827=EDGE_LOOP('',(#28872,#28873,#28874,#28875,#28876,#28877));
#6828=EDGE_LOOP('',(#28878,#28879,#28880,#28881,#28882,#28883));
#6829=EDGE_LOOP('',(#28884));
#6830=EDGE_LOOP('',(#28885));
#6831=EDGE_LOOP('',(#28886,#28887,#28888,#28889,#28890,#28891));
#6832=EDGE_LOOP('',(#28892,#28893,#28894,#28895,#28896,#28897));
#6833=EDGE_LOOP('',(#28898,#28899,#28900,#28901,#28902,#28903));
#6834=EDGE_LOOP('',(#28904));
#6835=EDGE_LOOP('',(#28905));
#6836=EDGE_LOOP('',(#28906,#28907,#28908,#28909,#28910,#28911));
#6837=EDGE_LOOP('',(#28912,#28913,#28914,#28915,#28916,#28917));
#6838=EDGE_LOOP('',(#28918,#28919,#28920,#28921,#28922,#28923));
#6839=EDGE_LOOP('',(#28924));
#6840=EDGE_LOOP('',(#28925));
#6841=EDGE_LOOP('',(#28926,#28927,#28928,#28929,#28930,#28931));
#6842=EDGE_LOOP('',(#28932,#28933,#28934,#28935,#28936,#28937));
#6843=EDGE_LOOP('',(#28938,#28939,#28940,#28941,#28942,#28943));
#6844=EDGE_LOOP('',(#28944));
#6845=EDGE_LOOP('',(#28945));
#6846=EDGE_LOOP('',(#28946,#28947,#28948,#28949,#28950,#28951));
#6847=EDGE_LOOP('',(#28952,#28953,#28954,#28955,#28956,#28957));
#6848=EDGE_LOOP('',(#28958,#28959,#28960,#28961,#28962,#28963));
#6849=EDGE_LOOP('',(#28964));
#6850=EDGE_LOOP('',(#28965));
#6851=EDGE_LOOP('',(#28966,#28967,#28968,#28969,#28970,#28971));
#6852=EDGE_LOOP('',(#28972,#28973,#28974,#28975,#28976,#28977));
#6853=EDGE_LOOP('',(#28978,#28979,#28980,#28981,#28982,#28983));
#6854=EDGE_LOOP('',(#28984));
#6855=EDGE_LOOP('',(#28985));
#6856=EDGE_LOOP('',(#28986,#28987,#28988,#28989,#28990,#28991));
#6857=EDGE_LOOP('',(#28992,#28993,#28994,#28995,#28996,#28997));
#6858=EDGE_LOOP('',(#28998,#28999,#29000,#29001,#29002,#29003));
#6859=EDGE_LOOP('',(#29004));
#6860=EDGE_LOOP('',(#29005));
#6861=EDGE_LOOP('',(#29006,#29007,#29008,#29009,#29010,#29011));
#6862=EDGE_LOOP('',(#29012,#29013,#29014,#29015,#29016,#29017));
#6863=EDGE_LOOP('',(#29018,#29019,#29020,#29021,#29022,#29023));
#6864=EDGE_LOOP('',(#29024));
#6865=EDGE_LOOP('',(#29025));
#6866=EDGE_LOOP('',(#29026,#29027,#29028,#29029,#29030,#29031));
#6867=EDGE_LOOP('',(#29032,#29033,#29034,#29035,#29036,#29037));
#6868=EDGE_LOOP('',(#29038,#29039,#29040,#29041,#29042,#29043));
#6869=EDGE_LOOP('',(#29044));
#6870=EDGE_LOOP('',(#29045));
#6871=EDGE_LOOP('',(#29046,#29047,#29048,#29049,#29050,#29051));
#6872=EDGE_LOOP('',(#29052,#29053,#29054,#29055,#29056,#29057));
#6873=EDGE_LOOP('',(#29058,#29059,#29060,#29061,#29062,#29063));
#6874=EDGE_LOOP('',(#29064));
#6875=EDGE_LOOP('',(#29065));
#6876=EDGE_LOOP('',(#29066,#29067,#29068,#29069));
#6877=EDGE_LOOP('',(#29070,#29071,#29072,#29073,#29074,#29075,#29076,#29077,
#29078,#29079,#29080,#29081));
#6878=EDGE_LOOP('',(#29082,#29083,#29084,#29085));
#6879=EDGE_LOOP('',(#29086,#29087,#29088,#29089));
#6880=EDGE_LOOP('',(#29090,#29091,#29092,#29093));
#6881=EDGE_LOOP('',(#29094,#29095,#29096,#29097));
#6882=EDGE_LOOP('',(#29098,#29099,#29100,#29101));
#6883=EDGE_LOOP('',(#29102,#29103,#29104,#29105));
#6884=EDGE_LOOP('',(#29106,#29107,#29108,#29109));
#6885=EDGE_LOOP('',(#29110,#29111,#29112,#29113));
#6886=EDGE_LOOP('',(#29114,#29115,#29116,#29117));
#6887=EDGE_LOOP('',(#29118,#29119,#29120,#29121));
#6888=EDGE_LOOP('',(#29122,#29123,#29124,#29125));
#6889=EDGE_LOOP('',(#29126,#29127,#29128,#29129));
#6890=EDGE_LOOP('',(#29130,#29131,#29132,#29133));
#6891=EDGE_LOOP('',(#29134,#29135,#29136,#29137));
#6892=EDGE_LOOP('',(#29138,#29139,#29140,#29141));
#6893=EDGE_LOOP('',(#29142,#29143,#29144,#29145));
#6894=EDGE_LOOP('',(#29146,#29147,#29148,#29149));
#6895=EDGE_LOOP('',(#29150,#29151,#29152,#29153));
#6896=EDGE_LOOP('',(#29154,#29155,#29156,#29157));
#6897=EDGE_LOOP('',(#29158,#29159,#29160,#29161));
#6898=EDGE_LOOP('',(#29162,#29163,#29164,#29165));
#6899=EDGE_LOOP('',(#29166,#29167,#29168,#29169));
#6900=EDGE_LOOP('',(#29170));
#6901=EDGE_LOOP('',(#29171));
#6902=EDGE_LOOP('',(#29172,#29173,#29174,#29175));
#6903=EDGE_LOOP('',(#29176,#29177,#29178,#29179));
#6904=EDGE_LOOP('',(#29180,#29181,#29182,#29183));
#6905=EDGE_LOOP('',(#29184));
#6906=EDGE_LOOP('',(#29185));
#9935=LINE('',#58053,#12985);
#9936=LINE('',#58061,#12986);
#9937=LINE('',#58066,#12987);
#9938=LINE('',#58072,#12988);
#9939=LINE('',#60057,#12989);
#9940=LINE('',#60060,#12990);
#9941=LINE('',#60061,#12991);
#9942=LINE('',#60065,#12992);
#9943=LINE('',#60071,#12993);
#9944=LINE('',#60075,#12994);
#9945=LINE('',#60079,#12995);
#12985=VECTOR('',#44128,25.6346416389917);
#12986=VECTOR('',#44139,25.8846416389917);
#12987=VECTOR('',#44144,22.5243990607509);
#12988=VECTOR('',#44151,22.7743990607509);
#12989=VECTOR('',#44732,22.5743990607509);
#12990=VECTOR('',#44737,22.011553150687);
#12991=VECTOR('',#44738,22.011553150687);
#12992=VECTOR('',#44743,25.6346416389917);
#12993=VECTOR('',#44750,17.894);
#12994=VECTOR('',#44755,17.494);
#12995=VECTOR('',#44760,17.794);
#13968=CIRCLE('',#36396,25.8846416389917);
#13969=CIRCLE('',#36397,25.8846416389917);
#13970=CIRCLE('',#36398,25.3846416389917);
#13971=CIRCLE('',#36400,22.4888907487754);
#13972=CIRCLE('',#36402,25.8846416389917);
#13973=CIRCLE('',#36404,22.2743990607509);
#13974=CIRCLE('',#36405,22.7743990607509);
#13975=CIRCLE('',#36406,22.7743990607509);
#13976=CIRCLE('',#36408,22.7743990607509);
#13977=CIRCLE('',#36410,21.5342155525986);
#13978=CIRCLE('',#36412,2.52960515816076);
#13979=CIRCLE('',#36413,0.3);
#13980=CIRCLE('',#36414,2.22978791005503);
#13981=CIRCLE('',#36415,2.52960515816076);
#13982=CIRCLE('',#36417,2.8696636114714);
#13983=CIRCLE('',#36418,2.8696636114714);
#13984=CIRCLE('',#36420,2.56984636336567);
#13985=CIRCLE('',#36421,0.3);
#13986=CIRCLE('',#36425,2.52960515816076);
#13987=CIRCLE('',#36426,0.3);
#13988=CIRCLE('',#36427,2.22978791005503);
#13989=CIRCLE('',#36428,2.52960515816076);
#13990=CIRCLE('',#36430,2.8696636114714);
#13991=CIRCLE('',#36431,2.8696636114714);
#13992=CIRCLE('',#36433,2.56984636336567);
#13993=CIRCLE('',#36434,0.3);
#13994=CIRCLE('',#36438,2.52960515816076);
#13995=CIRCLE('',#36439,0.3);
#13996=CIRCLE('',#36440,2.22978791005503);
#13997=CIRCLE('',#36441,2.52960515816076);
#13998=CIRCLE('',#36443,2.8696636114714);
#13999=CIRCLE('',#36444,2.8696636114714);
#14000=CIRCLE('',#36446,2.56984636336567);
#14001=CIRCLE('',#36447,0.3);
#14002=CIRCLE('',#36451,2.52960515816076);
#14003=CIRCLE('',#36452,0.3);
#14004=CIRCLE('',#36453,2.22978791005503);
#14005=CIRCLE('',#36454,2.52960515816076);
#14006=CIRCLE('',#36456,2.8696636114714);
#14007=CIRCLE('',#36457,2.8696636114714);
#14008=CIRCLE('',#36459,2.56984636336567);
#14009=CIRCLE('',#36460,0.3);
#14010=CIRCLE('',#36464,2.52960515816076);
#14011=CIRCLE('',#36465,0.3);
#14012=CIRCLE('',#36466,2.22978791005503);
#14013=CIRCLE('',#36467,2.52960515816076);
#14014=CIRCLE('',#36469,2.8696636114714);
#14015=CIRCLE('',#36470,2.8696636114714);
#14016=CIRCLE('',#36472,2.56984636336567);
#14017=CIRCLE('',#36473,0.3);
#14018=CIRCLE('',#36477,2.52960515816076);
#14019=CIRCLE('',#36478,0.3);
#14020=CIRCLE('',#36479,2.22978791005503);
#14021=CIRCLE('',#36480,2.52960515816076);
#14022=CIRCLE('',#36482,2.8696636114714);
#14023=CIRCLE('',#36483,2.8696636114714);
#14024=CIRCLE('',#36485,2.56984636336567);
#14025=CIRCLE('',#36486,0.3);
#14026=CIRCLE('',#36490,2.52960515816076);
#14027=CIRCLE('',#36491,0.3);
#14028=CIRCLE('',#36492,2.22978791005503);
#14029=CIRCLE('',#36493,2.52960515816076);
#14030=CIRCLE('',#36495,2.8696636114714);
#14031=CIRCLE('',#36496,2.8696636114714);
#14032=CIRCLE('',#36498,2.56984636336567);
#14033=CIRCLE('',#36499,0.3);
#14034=CIRCLE('',#36503,2.52960515816076);
#14035=CIRCLE('',#36504,0.3);
#14036=CIRCLE('',#36505,2.22978791005503);
#14037=CIRCLE('',#36506,2.52960515816076);
#14038=CIRCLE('',#36508,2.8696636114714);
#14039=CIRCLE('',#36509,2.8696636114714);
#14040=CIRCLE('',#36511,2.56984636336567);
#14041=CIRCLE('',#36512,0.3);
#14042=CIRCLE('',#36516,2.52960515816076);
#14043=CIRCLE('',#36517,0.3);
#14044=CIRCLE('',#36518,2.22978791005503);
#14045=CIRCLE('',#36519,2.52960515816076);
#14046=CIRCLE('',#36521,2.8696636114714);
#14047=CIRCLE('',#36522,2.8696636114714);
#14048=CIRCLE('',#36524,2.56984636336567);
#14049=CIRCLE('',#36525,0.3);
#14050=CIRCLE('',#36529,2.52960515816076);
#14051=CIRCLE('',#36530,0.3);
#14052=CIRCLE('',#36531,2.22978791005503);
#14053=CIRCLE('',#36532,2.52960515816076);
#14054=CIRCLE('',#36534,2.8696636114714);
#14055=CIRCLE('',#36535,2.8696636114714);
#14056=CIRCLE('',#36537,2.56984636336567);
#14057=CIRCLE('',#36538,0.3);
#14058=CIRCLE('',#36542,2.52960515816076);
#14059=CIRCLE('',#36543,0.3);
#14060=CIRCLE('',#36544,2.22978791005503);
#14061=CIRCLE('',#36545,2.52960515816076);
#14062=CIRCLE('',#36547,2.8696636114714);
#14063=CIRCLE('',#36548,2.8696636114714);
#14064=CIRCLE('',#36550,2.56984636336567);
#14065=CIRCLE('',#36551,0.3);
#14066=CIRCLE('',#36555,2.52960515816076);
#14067=CIRCLE('',#36556,0.3);
#14068=CIRCLE('',#36557,2.22978791005503);
#14069=CIRCLE('',#36558,2.52960515816076);
#14070=CIRCLE('',#36560,2.8696636114714);
#14071=CIRCLE('',#36561,2.8696636114714);
#14072=CIRCLE('',#36563,2.56984636336567);
#14073=CIRCLE('',#36564,0.3);
#14074=CIRCLE('',#36568,2.52960515816076);
#14075=CIRCLE('',#36569,0.3);
#14076=CIRCLE('',#36570,2.22978791005503);
#14077=CIRCLE('',#36571,2.52960515816076);
#14078=CIRCLE('',#36573,2.8696636114714);
#14079=CIRCLE('',#36574,2.8696636114714);
#14080=CIRCLE('',#36576,2.56984636336567);
#14081=CIRCLE('',#36577,0.3);
#14082=CIRCLE('',#36581,2.52960515816076);
#14083=CIRCLE('',#36582,0.3);
#14084=CIRCLE('',#36583,2.22978791005503);
#14085=CIRCLE('',#36584,2.52960515816076);
#14086=CIRCLE('',#36586,2.8696636114714);
#14087=CIRCLE('',#36587,2.8696636114714);
#14088=CIRCLE('',#36589,2.56984636336567);
#14089=CIRCLE('',#36590,0.3);
#14090=CIRCLE('',#36594,2.52960515816076);
#14091=CIRCLE('',#36595,0.3);
#14092=CIRCLE('',#36596,2.22978791005503);
#14093=CIRCLE('',#36597,2.52960515816076);
#14094=CIRCLE('',#36599,2.8696636114714);
#14095=CIRCLE('',#36600,2.8696636114714);
#14096=CIRCLE('',#36602,2.56984636336567);
#14097=CIRCLE('',#36603,0.3);
#14098=CIRCLE('',#36607,2.52960515816076);
#14099=CIRCLE('',#36608,0.3);
#14100=CIRCLE('',#36609,2.22978791005503);
#14101=CIRCLE('',#36610,2.52960515816076);
#14102=CIRCLE('',#36612,2.8696636114714);
#14103=CIRCLE('',#36613,2.8696636114714);
#14104=CIRCLE('',#36615,2.56984636336567);
#14105=CIRCLE('',#36616,0.3);
#14106=CIRCLE('',#36620,2.52960515816076);
#14107=CIRCLE('',#36621,0.3);
#14108=CIRCLE('',#36622,2.22978791005503);
#14109=CIRCLE('',#36623,2.52960515816076);
#14110=CIRCLE('',#36625,2.8696636114714);
#14111=CIRCLE('',#36626,2.8696636114714);
#14112=CIRCLE('',#36628,2.56984636336567);
#14113=CIRCLE('',#36629,0.3);
#14114=CIRCLE('',#36633,2.52960515816076);
#14115=CIRCLE('',#36634,0.3);
#14116=CIRCLE('',#36635,2.22978791005503);
#14117=CIRCLE('',#36636,2.52960515816076);
#14118=CIRCLE('',#36638,2.8696636114714);
#14119=CIRCLE('',#36639,2.8696636114714);
#14120=CIRCLE('',#36641,2.56984636336567);
#14121=CIRCLE('',#36642,0.3);
#14122=CIRCLE('',#36646,2.52960515816076);
#14123=CIRCLE('',#36647,0.3);
#14124=CIRCLE('',#36648,2.22978791005503);
#14125=CIRCLE('',#36649,2.52960515816076);
#14126=CIRCLE('',#36651,2.8696636114714);
#14127=CIRCLE('',#36652,2.8696636114714);
#14128=CIRCLE('',#36654,2.56984636336567);
#14129=CIRCLE('',#36655,0.3);
#14130=CIRCLE('',#36659,2.52960515816076);
#14131=CIRCLE('',#36660,0.3);
#14132=CIRCLE('',#36661,2.22978791005503);
#14133=CIRCLE('',#36662,2.52960515816076);
#14134=CIRCLE('',#36664,2.8696636114714);
#14135=CIRCLE('',#36665,2.8696636114714);
#14136=CIRCLE('',#36667,2.56984636336567);
#14137=CIRCLE('',#36668,0.3);
#14138=CIRCLE('',#36672,2.52960515816076);
#14139=CIRCLE('',#36673,0.3);
#14140=CIRCLE('',#36674,2.22978791005503);
#14141=CIRCLE('',#36675,2.52960515816076);
#14142=CIRCLE('',#36677,2.8696636114714);
#14143=CIRCLE('',#36678,2.8696636114714);
#14144=CIRCLE('',#36680,2.56984636336567);
#14145=CIRCLE('',#36681,0.3);
#14146=CIRCLE('',#36685,2.52960515816076);
#14147=CIRCLE('',#36686,0.3);
#14148=CIRCLE('',#36687,2.22978791005503);
#14149=CIRCLE('',#36688,2.52960515816076);
#14150=CIRCLE('',#36690,2.8696636114714);
#14151=CIRCLE('',#36691,2.8696636114714);
#14152=CIRCLE('',#36693,2.56984636336567);
#14153=CIRCLE('',#36694,0.3);
#14154=CIRCLE('',#36698,22.3743990607509);
#14155=CIRCLE('',#36701,25.3846416389917);
#14156=CIRCLE('',#36703,18.294);
#14157=CIRCLE('',#36705,17.494);
#14158=CIRCLE('',#36707,17.494);
#14159=CIRCLE('',#36709,18.094);
#16371=VERTEX_POINT('',#58048);
#16372=VERTEX_POINT('',#58049);
#16373=VERTEX_POINT('',#58052);
#16374=VERTEX_POINT('',#58056);
#16375=VERTEX_POINT('',#58059);
#16376=VERTEX_POINT('',#58063);
#16377=VERTEX_POINT('',#58065);
#16378=VERTEX_POINT('',#58067);
#16379=VERTEX_POINT('',#58071);
#16380=VERTEX_POINT('',#58075);
#16381=VERTEX_POINT('',#58078);
#16382=VERTEX_POINT('',#58079);
#16383=VERTEX_POINT('',#58108);
#16384=VERTEX_POINT('',#58110);
#16385=VERTEX_POINT('',#58115);
#16386=VERTEX_POINT('',#58120);
#16387=VERTEX_POINT('',#58122);
#16388=VERTEX_POINT('',#58129);
#16389=VERTEX_POINT('',#58164);
#16390=VERTEX_POINT('',#58165);
#16391=VERTEX_POINT('',#58198);
#16392=VERTEX_POINT('',#58200);
#16393=VERTEX_POINT('',#58205);
#16394=VERTEX_POINT('',#58210);
#16395=VERTEX_POINT('',#58212);
#16396=VERTEX_POINT('',#58219);
#16397=VERTEX_POINT('',#58258);
#16398=VERTEX_POINT('',#58259);
#16399=VERTEX_POINT('',#58292);
#16400=VERTEX_POINT('',#58294);
#16401=VERTEX_POINT('',#58299);
#16402=VERTEX_POINT('',#58304);
#16403=VERTEX_POINT('',#58306);
#16404=VERTEX_POINT('',#58313);
#16405=VERTEX_POINT('',#58352);
#16406=VERTEX_POINT('',#58353);
#16407=VERTEX_POINT('',#58386);
#16408=VERTEX_POINT('',#58388);
#16409=VERTEX_POINT('',#58393);
#16410=VERTEX_POINT('',#58398);
#16411=VERTEX_POINT('',#58400);
#16412=VERTEX_POINT('',#58407);
#16413=VERTEX_POINT('',#58442);
#16414=VERTEX_POINT('',#58443);
#16415=VERTEX_POINT('',#58472);
#16416=VERTEX_POINT('',#58474);
#16417=VERTEX_POINT('',#58479);
#16418=VERTEX_POINT('',#58484);
#16419=VERTEX_POINT('',#58486);
#16420=VERTEX_POINT('',#58493);
#16421=VERTEX_POINT('',#58526);
#16422=VERTEX_POINT('',#58527);
#16423=VERTEX_POINT('',#58556);
#16424=VERTEX_POINT('',#58558);
#16425=VERTEX_POINT('',#58563);
#16426=VERTEX_POINT('',#58568);
#16427=VERTEX_POINT('',#58570);
#16428=VERTEX_POINT('',#58577);
#16429=VERTEX_POINT('',#58610);
#16430=VERTEX_POINT('',#58611);
#16431=VERTEX_POINT('',#58644);
#16432=VERTEX_POINT('',#58646);
#16433=VERTEX_POINT('',#58651);
#16434=VERTEX_POINT('',#58656);
#16435=VERTEX_POINT('',#58658);
#16436=VERTEX_POINT('',#58665);
#16437=VERTEX_POINT('',#58700);
#16438=VERTEX_POINT('',#58701);
#16439=VERTEX_POINT('',#58734);
#16440=VERTEX_POINT('',#58736);
#16441=VERTEX_POINT('',#58741);
#16442=VERTEX_POINT('',#58746);
#16443=VERTEX_POINT('',#58748);
#16444=VERTEX_POINT('',#58755);
#16445=VERTEX_POINT('',#58794);
#16446=VERTEX_POINT('',#58795);
#16447=VERTEX_POINT('',#58828);
#16448=VERTEX_POINT('',#58830);
#16449=VERTEX_POINT('',#58835);
#16450=VERTEX_POINT('',#58840);
#16451=VERTEX_POINT('',#58842);
#16452=VERTEX_POINT('',#58849);
#16453=VERTEX_POINT('',#58888);
#16454=VERTEX_POINT('',#58889);
#16455=VERTEX_POINT('',#58918);
#16456=VERTEX_POINT('',#58920);
#16457=VERTEX_POINT('',#58925);
#16458=VERTEX_POINT('',#58930);
#16459=VERTEX_POINT('',#58932);
#16460=VERTEX_POINT('',#58939);
#16461=VERTEX_POINT('',#58974);
#16462=VERTEX_POINT('',#58975);
#16463=VERTEX_POINT('',#58992);
#16464=VERTEX_POINT('',#58994);
#16465=VERTEX_POINT('',#58997);
#16466=VERTEX_POINT('',#59016);
#16467=VERTEX_POINT('',#59021);
#16468=VERTEX_POINT('',#59023);
#16469=VERTEX_POINT('',#59030);
#16470=VERTEX_POINT('',#59033);
#16471=VERTEX_POINT('',#59072);
#16472=VERTEX_POINT('',#59073);
#16473=VERTEX_POINT('',#59102);
#16474=VERTEX_POINT('',#59104);
#16475=VERTEX_POINT('',#59109);
#16476=VERTEX_POINT('',#59114);
#16477=VERTEX_POINT('',#59116);
#16478=VERTEX_POINT('',#59123);
#16479=VERTEX_POINT('',#59158);
#16480=VERTEX_POINT('',#59159);
#16481=VERTEX_POINT('',#59192);
#16482=VERTEX_POINT('',#59194);
#16483=VERTEX_POINT('',#59199);
#16484=VERTEX_POINT('',#59204);
#16485=VERTEX_POINT('',#59206);
#16486=VERTEX_POINT('',#59213);
#16487=VERTEX_POINT('',#59252);
#16488=VERTEX_POINT('',#59253);
#16489=VERTEX_POINT('',#59286);
#16490=VERTEX_POINT('',#59288);
#16491=VERTEX_POINT('',#59293);
#16492=VERTEX_POINT('',#59298);
#16493=VERTEX_POINT('',#59300);
#16494=VERTEX_POINT('',#59307);
#16495=VERTEX_POINT('',#59346);
#16496=VERTEX_POINT('',#59347);
#16497=VERTEX_POINT('',#59380);
#16498=VERTEX_POINT('',#59382);
#16499=VERTEX_POINT('',#59387);
#16500=VERTEX_POINT('',#59392);
#16501=VERTEX_POINT('',#59394);
#16502=VERTEX_POINT('',#59401);
#16503=VERTEX_POINT('',#59436);
#16504=VERTEX_POINT('',#59437);
#16505=VERTEX_POINT('',#59466);
#16506=VERTEX_POINT('',#59468);
#16507=VERTEX_POINT('',#59473);
#16508=VERTEX_POINT('',#59478);
#16509=VERTEX_POINT('',#59480);
#16510=VERTEX_POINT('',#59487);
#16511=VERTEX_POINT('',#59520);
#16512=VERTEX_POINT('',#59521);
#16513=VERTEX_POINT('',#59550);
#16514=VERTEX_POINT('',#59552);
#16515=VERTEX_POINT('',#59557);
#16516=VERTEX_POINT('',#59562);
#16517=VERTEX_POINT('',#59564);
#16518=VERTEX_POINT('',#59571);
#16519=VERTEX_POINT('',#59604);
#16520=VERTEX_POINT('',#59605);
#16521=VERTEX_POINT('',#59638);
#16522=VERTEX_POINT('',#59640);
#16523=VERTEX_POINT('',#59645);
#16524=VERTEX_POINT('',#59650);
#16525=VERTEX_POINT('',#59652);
#16526=VERTEX_POINT('',#59659);
#16527=VERTEX_POINT('',#59694);
#16528=VERTEX_POINT('',#59695);
#16529=VERTEX_POINT('',#59728);
#16530=VERTEX_POINT('',#59730);
#16531=VERTEX_POINT('',#59735);
#16532=VERTEX_POINT('',#59740);
#16533=VERTEX_POINT('',#59742);
#16534=VERTEX_POINT('',#59749);
#16535=VERTEX_POINT('',#59788);
#16536=VERTEX_POINT('',#59789);
#16537=VERTEX_POINT('',#59822);
#16538=VERTEX_POINT('',#59824);
#16539=VERTEX_POINT('',#59829);
#16540=VERTEX_POINT('',#59834);
#16541=VERTEX_POINT('',#59836);
#16542=VERTEX_POINT('',#59843);
#16543=VERTEX_POINT('',#59882);
#16544=VERTEX_POINT('',#59883);
#16545=VERTEX_POINT('',#59912);
#16546=VERTEX_POINT('',#59914);
#16547=VERTEX_POINT('',#59919);
#16548=VERTEX_POINT('',#59924);
#16549=VERTEX_POINT('',#59926);
#16550=VERTEX_POINT('',#59933);
#16551=VERTEX_POINT('',#59968);
#16552=VERTEX_POINT('',#59969);
#16553=VERTEX_POINT('',#59998);
#16554=VERTEX_POINT('',#60000);
#16555=VERTEX_POINT('',#60005);
#16556=VERTEX_POINT('',#60010);
#16557=VERTEX_POINT('',#60012);
#16558=VERTEX_POINT('',#60019);
#16559=VERTEX_POINT('',#60056);
#16560=VERTEX_POINT('',#60063);
#16561=VERTEX_POINT('',#60067);
#16562=VERTEX_POINT('',#60070);
#16563=VERTEX_POINT('',#60074);
#16564=VERTEX_POINT('',#60078);
#20614=EDGE_CURVE('',#16371,#16372,#13968,.T.);
#20615=EDGE_CURVE('',#16372,#16371,#13969,.T.);
#20616=EDGE_CURVE('',#16371,#16373,#9935,.T.);
#20617=EDGE_CURVE('',#16373,#16373,#13970,.T.);
#20618=EDGE_CURVE('',#16374,#16374,#13971,.T.);
#20619=EDGE_CURVE('',#16375,#16375,#13972,.T.);
#20620=EDGE_CURVE('',#16375,#16372,#9936,.T.);
#20621=EDGE_CURVE('',#16376,#16376,#13973,.T.);
#20622=EDGE_CURVE('',#16376,#16377,#9937,.T.);
#20623=EDGE_CURVE('',#16377,#16378,#13974,.T.);
#20624=EDGE_CURVE('',#16378,#16377,#13975,.T.);
#20625=EDGE_CURVE('',#16378,#16379,#9938,.T.);
#20626=EDGE_CURVE('',#16379,#16379,#13976,.T.);
#20627=EDGE_CURVE('',#16380,#16380,#13977,.T.);
#20628=EDGE_CURVE('',#16381,#16382,#483,.T.);
#20629=EDGE_CURVE('',#16381,#16383,#13978,.T.);
#20630=EDGE_CURVE('',#16383,#16384,#13979,.T.);
#20631=EDGE_CURVE('',#16384,#16384,#13980,.T.);
#20632=EDGE_CURVE('',#16383,#16382,#13981,.T.);
#20633=EDGE_CURVE('',#16385,#16381,#484,.T.);
#20634=EDGE_CURVE('',#16386,#16385,#13982,.T.);
#20635=EDGE_CURVE('',#16387,#16386,#13983,.T.);
#20636=EDGE_CURVE('',#16382,#16387,#485,.T.);
#20637=EDGE_CURVE('',#16388,#16388,#13984,.T.);
#20638=EDGE_CURVE('',#16388,#16386,#13985,.T.);
#20639=EDGE_CURVE('',#16387,#16385,#486,.T.);
#20640=EDGE_CURVE('',#16389,#16390,#487,.T.);
#20641=EDGE_CURVE('',#16389,#16391,#13986,.T.);
#20642=EDGE_CURVE('',#16391,#16392,#13987,.T.);
#20643=EDGE_CURVE('',#16392,#16392,#13988,.T.);
#20644=EDGE_CURVE('',#16391,#16390,#13989,.T.);
#20645=EDGE_CURVE('',#16393,#16389,#488,.T.);
#20646=EDGE_CURVE('',#16394,#16393,#13990,.T.);
#20647=EDGE_CURVE('',#16395,#16394,#13991,.T.);
#20648=EDGE_CURVE('',#16390,#16395,#489,.T.);
#20649=EDGE_CURVE('',#16396,#16396,#13992,.T.);
#20650=EDGE_CURVE('',#16396,#16394,#13993,.T.);
#20651=EDGE_CURVE('',#16395,#16393,#490,.T.);
#20652=EDGE_CURVE('',#16397,#16398,#491,.T.);
#20653=EDGE_CURVE('',#16397,#16399,#13994,.T.);
#20654=EDGE_CURVE('',#16399,#16400,#13995,.T.);
#20655=EDGE_CURVE('',#16400,#16400,#13996,.T.);
#20656=EDGE_CURVE('',#16399,#16398,#13997,.T.);
#20657=EDGE_CURVE('',#16401,#16397,#492,.T.);
#20658=EDGE_CURVE('',#16402,#16401,#13998,.T.);
#20659=EDGE_CURVE('',#16403,#16402,#13999,.T.);
#20660=EDGE_CURVE('',#16398,#16403,#493,.T.);
#20661=EDGE_CURVE('',#16404,#16404,#14000,.T.);
#20662=EDGE_CURVE('',#16404,#16402,#14001,.T.);
#20663=EDGE_CURVE('',#16403,#16401,#494,.T.);
#20664=EDGE_CURVE('',#16405,#16406,#495,.T.);
#20665=EDGE_CURVE('',#16405,#16407,#14002,.T.);
#20666=EDGE_CURVE('',#16407,#16408,#14003,.T.);
#20667=EDGE_CURVE('',#16408,#16408,#14004,.T.);
#20668=EDGE_CURVE('',#16407,#16406,#14005,.T.);
#20669=EDGE_CURVE('',#16409,#16405,#496,.T.);
#20670=EDGE_CURVE('',#16410,#16409,#14006,.T.);
#20671=EDGE_CURVE('',#16411,#16410,#14007,.T.);
#20672=EDGE_CURVE('',#16406,#16411,#497,.T.);
#20673=EDGE_CURVE('',#16412,#16412,#14008,.T.);
#20674=EDGE_CURVE('',#16412,#16410,#14009,.T.);
#20675=EDGE_CURVE('',#16411,#16409,#498,.T.);
#20676=EDGE_CURVE('',#16413,#16414,#499,.T.);
#20677=EDGE_CURVE('',#16413,#16415,#14010,.T.);
#20678=EDGE_CURVE('',#16415,#16416,#14011,.T.);
#20679=EDGE_CURVE('',#16416,#16416,#14012,.T.);
#20680=EDGE_CURVE('',#16415,#16414,#14013,.T.);
#20681=EDGE_CURVE('',#16417,#16413,#500,.T.);
#20682=EDGE_CURVE('',#16418,#16417,#14014,.T.);
#20683=EDGE_CURVE('',#16419,#16418,#14015,.T.);
#20684=EDGE_CURVE('',#16414,#16419,#501,.T.);
#20685=EDGE_CURVE('',#16420,#16420,#14016,.T.);
#20686=EDGE_CURVE('',#16420,#16418,#14017,.T.);
#20687=EDGE_CURVE('',#16419,#16417,#502,.T.);
#20688=EDGE_CURVE('',#16421,#16422,#503,.T.);
#20689=EDGE_CURVE('',#16421,#16423,#14018,.T.);
#20690=EDGE_CURVE('',#16423,#16424,#14019,.T.);
#20691=EDGE_CURVE('',#16424,#16424,#14020,.T.);
#20692=EDGE_CURVE('',#16423,#16422,#14021,.T.);
#20693=EDGE_CURVE('',#16425,#16421,#504,.T.);
#20694=EDGE_CURVE('',#16426,#16425,#14022,.T.);
#20695=EDGE_CURVE('',#16427,#16426,#14023,.T.);
#20696=EDGE_CURVE('',#16422,#16427,#505,.T.);
#20697=EDGE_CURVE('',#16428,#16428,#14024,.T.);
#20698=EDGE_CURVE('',#16428,#16426,#14025,.T.);
#20699=EDGE_CURVE('',#16427,#16425,#506,.T.);
#20700=EDGE_CURVE('',#16429,#16430,#507,.T.);
#20701=EDGE_CURVE('',#16429,#16431,#14026,.T.);
#20702=EDGE_CURVE('',#16431,#16432,#14027,.T.);
#20703=EDGE_CURVE('',#16432,#16432,#14028,.T.);
#20704=EDGE_CURVE('',#16431,#16430,#14029,.T.);
#20705=EDGE_CURVE('',#16433,#16429,#508,.T.);
#20706=EDGE_CURVE('',#16434,#16433,#14030,.T.);
#20707=EDGE_CURVE('',#16435,#16434,#14031,.T.);
#20708=EDGE_CURVE('',#16430,#16435,#509,.T.);
#20709=EDGE_CURVE('',#16436,#16436,#14032,.T.);
#20710=EDGE_CURVE('',#16436,#16434,#14033,.T.);
#20711=EDGE_CURVE('',#16435,#16433,#510,.T.);
#20712=EDGE_CURVE('',#16437,#16438,#511,.T.);
#20713=EDGE_CURVE('',#16437,#16439,#14034,.T.);
#20714=EDGE_CURVE('',#16439,#16440,#14035,.T.);
#20715=EDGE_CURVE('',#16440,#16440,#14036,.T.);
#20716=EDGE_CURVE('',#16439,#16438,#14037,.T.);
#20717=EDGE_CURVE('',#16441,#16437,#512,.T.);
#20718=EDGE_CURVE('',#16442,#16441,#14038,.T.);
#20719=EDGE_CURVE('',#16443,#16442,#14039,.T.);
#20720=EDGE_CURVE('',#16438,#16443,#513,.T.);
#20721=EDGE_CURVE('',#16444,#16444,#14040,.T.);
#20722=EDGE_CURVE('',#16444,#16442,#14041,.T.);
#20723=EDGE_CURVE('',#16443,#16441,#514,.T.);
#20724=EDGE_CURVE('',#16445,#16446,#515,.T.);
#20725=EDGE_CURVE('',#16445,#16447,#14042,.T.);
#20726=EDGE_CURVE('',#16447,#16448,#14043,.T.);
#20727=EDGE_CURVE('',#16448,#16448,#14044,.T.);
#20728=EDGE_CURVE('',#16447,#16446,#14045,.T.);
#20729=EDGE_CURVE('',#16449,#16445,#516,.T.);
#20730=EDGE_CURVE('',#16450,#16449,#14046,.T.);
#20731=EDGE_CURVE('',#16451,#16450,#14047,.T.);
#20732=EDGE_CURVE('',#16446,#16451,#517,.T.);
#20733=EDGE_CURVE('',#16452,#16452,#14048,.T.);
#20734=EDGE_CURVE('',#16452,#16450,#14049,.T.);
#20735=EDGE_CURVE('',#16451,#16449,#518,.T.);
#20736=EDGE_CURVE('',#16453,#16454,#519,.T.);
#20737=EDGE_CURVE('',#16453,#16455,#14050,.T.);
#20738=EDGE_CURVE('',#16455,#16456,#14051,.T.);
#20739=EDGE_CURVE('',#16456,#16456,#14052,.T.);
#20740=EDGE_CURVE('',#16455,#16454,#14053,.T.);
#20741=EDGE_CURVE('',#16457,#16453,#520,.T.);
#20742=EDGE_CURVE('',#16458,#16457,#14054,.T.);
#20743=EDGE_CURVE('',#16459,#16458,#14055,.T.);
#20744=EDGE_CURVE('',#16454,#16459,#521,.T.);
#20745=EDGE_CURVE('',#16460,#16460,#14056,.T.);
#20746=EDGE_CURVE('',#16460,#16458,#14057,.T.);
#20747=EDGE_CURVE('',#16459,#16457,#522,.T.);
#20748=EDGE_CURVE('',#16461,#16462,#523,.T.);
#20749=EDGE_CURVE('',#16461,#16463,#14058,.T.);
#20750=EDGE_CURVE('',#16463,#16464,#14059,.T.);
#20751=EDGE_CURVE('',#16464,#16464,#14060,.T.);
#20752=EDGE_CURVE('',#16463,#16465,#14061,.T.);
#20753=EDGE_CURVE('',#16462,#16465,#524,.T.);
#20754=EDGE_CURVE('',#16466,#16461,#525,.T.);
#20755=EDGE_CURVE('',#16467,#16466,#14062,.T.);
#20756=EDGE_CURVE('',#16468,#16467,#14063,.T.);
#20757=EDGE_CURVE('',#16465,#16468,#526,.T.);
#20758=EDGE_CURVE('',#16469,#16469,#14064,.T.);
#20759=EDGE_CURVE('',#16469,#16467,#14065,.T.);
#20760=EDGE_CURVE('',#16470,#16466,#527,.T.);
#20761=EDGE_CURVE('',#16468,#16470,#528,.T.);
#20762=EDGE_CURVE('',#16471,#16472,#529,.T.);
#20763=EDGE_CURVE('',#16471,#16473,#14066,.T.);
#20764=EDGE_CURVE('',#16473,#16474,#14067,.T.);
#20765=EDGE_CURVE('',#16474,#16474,#14068,.T.);
#20766=EDGE_CURVE('',#16473,#16472,#14069,.T.);
#20767=EDGE_CURVE('',#16475,#16471,#530,.T.);
#20768=EDGE_CURVE('',#16476,#16475,#14070,.T.);
#20769=EDGE_CURVE('',#16477,#16476,#14071,.T.);
#20770=EDGE_CURVE('',#16472,#16477,#531,.T.);
#20771=EDGE_CURVE('',#16478,#16478,#14072,.T.);
#20772=EDGE_CURVE('',#16478,#16476,#14073,.T.);
#20773=EDGE_CURVE('',#16477,#16475,#532,.T.);
#20774=EDGE_CURVE('',#16479,#16480,#533,.T.);
#20775=EDGE_CURVE('',#16479,#16481,#14074,.T.);
#20776=EDGE_CURVE('',#16481,#16482,#14075,.T.);
#20777=EDGE_CURVE('',#16482,#16482,#14076,.T.);
#20778=EDGE_CURVE('',#16481,#16480,#14077,.T.);
#20779=EDGE_CURVE('',#16483,#16479,#534,.T.);
#20780=EDGE_CURVE('',#16484,#16483,#14078,.T.);
#20781=EDGE_CURVE('',#16485,#16484,#14079,.T.);
#20782=EDGE_CURVE('',#16480,#16485,#535,.T.);
#20783=EDGE_CURVE('',#16486,#16486,#14080,.T.);
#20784=EDGE_CURVE('',#16486,#16484,#14081,.T.);
#20785=EDGE_CURVE('',#16485,#16483,#536,.T.);
#20786=EDGE_CURVE('',#16487,#16488,#537,.T.);
#20787=EDGE_CURVE('',#16487,#16489,#14082,.T.);
#20788=EDGE_CURVE('',#16489,#16490,#14083,.T.);
#20789=EDGE_CURVE('',#16490,#16490,#14084,.T.);
#20790=EDGE_CURVE('',#16489,#16488,#14085,.T.);
#20791=EDGE_CURVE('',#16491,#16487,#538,.T.);
#20792=EDGE_CURVE('',#16492,#16491,#14086,.T.);
#20793=EDGE_CURVE('',#16493,#16492,#14087,.T.);
#20794=EDGE_CURVE('',#16488,#16493,#539,.T.);
#20795=EDGE_CURVE('',#16494,#16494,#14088,.T.);
#20796=EDGE_CURVE('',#16494,#16492,#14089,.T.);
#20797=EDGE_CURVE('',#16493,#16491,#540,.T.);
#20798=EDGE_CURVE('',#16495,#16496,#541,.T.);
#20799=EDGE_CURVE('',#16495,#16497,#14090,.T.);
#20800=EDGE_CURVE('',#16497,#16498,#14091,.T.);
#20801=EDGE_CURVE('',#16498,#16498,#14092,.T.);
#20802=EDGE_CURVE('',#16497,#16496,#14093,.T.);
#20803=EDGE_CURVE('',#16499,#16495,#542,.T.);
#20804=EDGE_CURVE('',#16500,#16499,#14094,.T.);
#20805=EDGE_CURVE('',#16501,#16500,#14095,.T.);
#20806=EDGE_CURVE('',#16496,#16501,#543,.T.);
#20807=EDGE_CURVE('',#16502,#16502,#14096,.T.);
#20808=EDGE_CURVE('',#16502,#16500,#14097,.T.);
#20809=EDGE_CURVE('',#16501,#16499,#544,.T.);
#20810=EDGE_CURVE('',#16503,#16504,#545,.T.);
#20811=EDGE_CURVE('',#16503,#16505,#14098,.T.);
#20812=EDGE_CURVE('',#16505,#16506,#14099,.T.);
#20813=EDGE_CURVE('',#16506,#16506,#14100,.T.);
#20814=EDGE_CURVE('',#16505,#16504,#14101,.T.);
#20815=EDGE_CURVE('',#16507,#16503,#546,.T.);
#20816=EDGE_CURVE('',#16508,#16507,#14102,.T.);
#20817=EDGE_CURVE('',#16509,#16508,#14103,.T.);
#20818=EDGE_CURVE('',#16504,#16509,#547,.T.);
#20819=EDGE_CURVE('',#16510,#16510,#14104,.T.);
#20820=EDGE_CURVE('',#16510,#16508,#14105,.T.);
#20821=EDGE_CURVE('',#16509,#16507,#548,.T.);
#20822=EDGE_CURVE('',#16511,#16512,#549,.T.);
#20823=EDGE_CURVE('',#16511,#16513,#14106,.T.);
#20824=EDGE_CURVE('',#16513,#16514,#14107,.T.);
#20825=EDGE_CURVE('',#16514,#16514,#14108,.T.);
#20826=EDGE_CURVE('',#16513,#16512,#14109,.T.);
#20827=EDGE_CURVE('',#16515,#16511,#550,.T.);
#20828=EDGE_CURVE('',#16516,#16515,#14110,.T.);
#20829=EDGE_CURVE('',#16517,#16516,#14111,.T.);
#20830=EDGE_CURVE('',#16512,#16517,#551,.T.);
#20831=EDGE_CURVE('',#16518,#16518,#14112,.T.);
#20832=EDGE_CURVE('',#16518,#16516,#14113,.T.);
#20833=EDGE_CURVE('',#16517,#16515,#552,.T.);
#20834=EDGE_CURVE('',#16519,#16520,#553,.T.);
#20835=EDGE_CURVE('',#16519,#16521,#14114,.T.);
#20836=EDGE_CURVE('',#16521,#16522,#14115,.T.);
#20837=EDGE_CURVE('',#16522,#16522,#14116,.T.);
#20838=EDGE_CURVE('',#16521,#16520,#14117,.T.);
#20839=EDGE_CURVE('',#16523,#16519,#554,.T.);
#20840=EDGE_CURVE('',#16524,#16523,#14118,.T.);
#20841=EDGE_CURVE('',#16525,#16524,#14119,.T.);
#20842=EDGE_CURVE('',#16520,#16525,#555,.T.);
#20843=EDGE_CURVE('',#16526,#16526,#14120,.T.);
#20844=EDGE_CURVE('',#16526,#16524,#14121,.T.);
#20845=EDGE_CURVE('',#16525,#16523,#556,.T.);
#20846=EDGE_CURVE('',#16527,#16528,#557,.T.);
#20847=EDGE_CURVE('',#16527,#16529,#14122,.T.);
#20848=EDGE_CURVE('',#16529,#16530,#14123,.T.);
#20849=EDGE_CURVE('',#16530,#16530,#14124,.T.);
#20850=EDGE_CURVE('',#16529,#16528,#14125,.T.);
#20851=EDGE_CURVE('',#16531,#16527,#558,.T.);
#20852=EDGE_CURVE('',#16532,#16531,#14126,.T.);
#20853=EDGE_CURVE('',#16533,#16532,#14127,.T.);
#20854=EDGE_CURVE('',#16528,#16533,#559,.T.);
#20855=EDGE_CURVE('',#16534,#16534,#14128,.T.);
#20856=EDGE_CURVE('',#16534,#16532,#14129,.T.);
#20857=EDGE_CURVE('',#16533,#16531,#560,.T.);
#20858=EDGE_CURVE('',#16535,#16536,#561,.T.);
#20859=EDGE_CURVE('',#16535,#16537,#14130,.T.);
#20860=EDGE_CURVE('',#16537,#16538,#14131,.T.);
#20861=EDGE_CURVE('',#16538,#16538,#14132,.T.);
#20862=EDGE_CURVE('',#16537,#16536,#14133,.T.);
#20863=EDGE_CURVE('',#16539,#16535,#562,.T.);
#20864=EDGE_CURVE('',#16540,#16539,#14134,.T.);
#20865=EDGE_CURVE('',#16541,#16540,#14135,.T.);
#20866=EDGE_CURVE('',#16536,#16541,#563,.T.);
#20867=EDGE_CURVE('',#16542,#16542,#14136,.T.);
#20868=EDGE_CURVE('',#16542,#16540,#14137,.T.);
#20869=EDGE_CURVE('',#16541,#16539,#564,.T.);
#20870=EDGE_CURVE('',#16543,#16544,#565,.T.);
#20871=EDGE_CURVE('',#16543,#16545,#14138,.T.);
#20872=EDGE_CURVE('',#16545,#16546,#14139,.T.);
#20873=EDGE_CURVE('',#16546,#16546,#14140,.T.);
#20874=EDGE_CURVE('',#16545,#16544,#14141,.T.);
#20875=EDGE_CURVE('',#16547,#16543,#566,.T.);
#20876=EDGE_CURVE('',#16548,#16547,#14142,.T.);
#20877=EDGE_CURVE('',#16549,#16548,#14143,.T.);
#20878=EDGE_CURVE('',#16544,#16549,#567,.T.);
#20879=EDGE_CURVE('',#16550,#16550,#14144,.T.);
#20880=EDGE_CURVE('',#16550,#16548,#14145,.T.);
#20881=EDGE_CURVE('',#16549,#16547,#568,.T.);
#20882=EDGE_CURVE('',#16551,#16552,#569,.T.);
#20883=EDGE_CURVE('',#16551,#16553,#14146,.T.);
#20884=EDGE_CURVE('',#16553,#16554,#14147,.T.);
#20885=EDGE_CURVE('',#16554,#16554,#14148,.T.);
#20886=EDGE_CURVE('',#16553,#16552,#14149,.T.);
#20887=EDGE_CURVE('',#16555,#16551,#570,.T.);
#20888=EDGE_CURVE('',#16556,#16555,#14150,.T.);
#20889=EDGE_CURVE('',#16557,#16556,#14151,.T.);
#20890=EDGE_CURVE('',#16552,#16557,#571,.T.);
#20891=EDGE_CURVE('',#16558,#16558,#14152,.T.);
#20892=EDGE_CURVE('',#16558,#16556,#14153,.T.);
#20893=EDGE_CURVE('',#16557,#16555,#572,.T.);
#20894=EDGE_CURVE('',#16379,#16559,#9939,.T.);
#20895=EDGE_CURVE('',#16559,#16559,#14154,.T.);
#20896=EDGE_CURVE('',#16374,#16470,#9940,.T.);
#20897=EDGE_CURVE('',#16462,#16380,#9941,.T.);
#20898=EDGE_CURVE('',#16560,#16560,#14155,.T.);
#20899=EDGE_CURVE('',#16560,#16375,#9942,.T.);
#20900=EDGE_CURVE('',#16561,#16561,#14156,.T.);
#20901=EDGE_CURVE('',#16561,#16562,#9943,.T.);
#20902=EDGE_CURVE('',#16562,#16562,#14157,.T.);
#20903=EDGE_CURVE('',#16562,#16563,#9944,.T.);
#20904=EDGE_CURVE('',#16563,#16563,#14158,.T.);
#20905=EDGE_CURVE('',#16563,#16564,#9945,.T.);
#20906=EDGE_CURVE('',#16564,#16564,#14159,.T.);
#28600=ORIENTED_EDGE('',*,*,#20614,.T.);
#28601=ORIENTED_EDGE('',*,*,#20615,.T.);
#28602=ORIENTED_EDGE('',*,*,#20616,.T.);
#28603=ORIENTED_EDGE('',*,*,#20617,.T.);
#28604=ORIENTED_EDGE('',*,*,#20616,.F.);
#28605=ORIENTED_EDGE('',*,*,#20617,.F.);
#28606=ORIENTED_EDGE('',*,*,#20618,.T.);
#28607=ORIENTED_EDGE('',*,*,#20619,.F.);
#28608=ORIENTED_EDGE('',*,*,#20620,.T.);
#28609=ORIENTED_EDGE('',*,*,#20614,.F.);
#28610=ORIENTED_EDGE('',*,*,#20615,.F.);
#28611=ORIENTED_EDGE('',*,*,#20620,.F.);
#28612=ORIENTED_EDGE('',*,*,#20621,.T.);
#28613=ORIENTED_EDGE('',*,*,#20622,.T.);
#28614=ORIENTED_EDGE('',*,*,#20623,.T.);
#28615=ORIENTED_EDGE('',*,*,#20624,.T.);
#28616=ORIENTED_EDGE('',*,*,#20622,.F.);
#28617=ORIENTED_EDGE('',*,*,#20623,.F.);
#28618=ORIENTED_EDGE('',*,*,#20624,.F.);
#28619=ORIENTED_EDGE('',*,*,#20625,.T.);
#28620=ORIENTED_EDGE('',*,*,#20626,.T.);
#28621=ORIENTED_EDGE('',*,*,#20625,.F.);
#28622=ORIENTED_EDGE('',*,*,#20621,.F.);
#28623=ORIENTED_EDGE('',*,*,#20627,.F.);
#28624=ORIENTED_EDGE('',*,*,#20628,.F.);
#28625=ORIENTED_EDGE('',*,*,#20629,.T.);
#28626=ORIENTED_EDGE('',*,*,#20630,.T.);
#28627=ORIENTED_EDGE('',*,*,#20631,.T.);
#28628=ORIENTED_EDGE('',*,*,#20630,.F.);
#28629=ORIENTED_EDGE('',*,*,#20632,.T.);
#28630=ORIENTED_EDGE('',*,*,#20633,.F.);
#28631=ORIENTED_EDGE('',*,*,#20634,.F.);
#28632=ORIENTED_EDGE('',*,*,#20635,.F.);
#28633=ORIENTED_EDGE('',*,*,#20636,.F.);
#28634=ORIENTED_EDGE('',*,*,#20632,.F.);
#28635=ORIENTED_EDGE('',*,*,#20629,.F.);
#28636=ORIENTED_EDGE('',*,*,#20637,.T.);
#28637=ORIENTED_EDGE('',*,*,#20638,.T.);
#28638=ORIENTED_EDGE('',*,*,#20634,.T.);
#28639=ORIENTED_EDGE('',*,*,#20639,.F.);
#28640=ORIENTED_EDGE('',*,*,#20635,.T.);
#28641=ORIENTED_EDGE('',*,*,#20638,.F.);
#28642=ORIENTED_EDGE('',*,*,#20637,.F.);
#28643=ORIENTED_EDGE('',*,*,#20631,.F.);
#28644=ORIENTED_EDGE('',*,*,#20640,.F.);
#28645=ORIENTED_EDGE('',*,*,#20641,.T.);
#28646=ORIENTED_EDGE('',*,*,#20642,.T.);
#28647=ORIENTED_EDGE('',*,*,#20643,.T.);
#28648=ORIENTED_EDGE('',*,*,#20642,.F.);
#28649=ORIENTED_EDGE('',*,*,#20644,.T.);
#28650=ORIENTED_EDGE('',*,*,#20645,.F.);
#28651=ORIENTED_EDGE('',*,*,#20646,.F.);
#28652=ORIENTED_EDGE('',*,*,#20647,.F.);
#28653=ORIENTED_EDGE('',*,*,#20648,.F.);
#28654=ORIENTED_EDGE('',*,*,#20644,.F.);
#28655=ORIENTED_EDGE('',*,*,#20641,.F.);
#28656=ORIENTED_EDGE('',*,*,#20649,.T.);
#28657=ORIENTED_EDGE('',*,*,#20650,.T.);
#28658=ORIENTED_EDGE('',*,*,#20646,.T.);
#28659=ORIENTED_EDGE('',*,*,#20651,.F.);
#28660=ORIENTED_EDGE('',*,*,#20647,.T.);
#28661=ORIENTED_EDGE('',*,*,#20650,.F.);
#28662=ORIENTED_EDGE('',*,*,#20649,.F.);
#28663=ORIENTED_EDGE('',*,*,#20643,.F.);
#28664=ORIENTED_EDGE('',*,*,#20652,.F.);
#28665=ORIENTED_EDGE('',*,*,#20653,.T.);
#28666=ORIENTED_EDGE('',*,*,#20654,.T.);
#28667=ORIENTED_EDGE('',*,*,#20655,.T.);
#28668=ORIENTED_EDGE('',*,*,#20654,.F.);
#28669=ORIENTED_EDGE('',*,*,#20656,.T.);
#28670=ORIENTED_EDGE('',*,*,#20657,.F.);
#28671=ORIENTED_EDGE('',*,*,#20658,.F.);
#28672=ORIENTED_EDGE('',*,*,#20659,.F.);
#28673=ORIENTED_EDGE('',*,*,#20660,.F.);
#28674=ORIENTED_EDGE('',*,*,#20656,.F.);
#28675=ORIENTED_EDGE('',*,*,#20653,.F.);
#28676=ORIENTED_EDGE('',*,*,#20661,.T.);
#28677=ORIENTED_EDGE('',*,*,#20662,.T.);
#28678=ORIENTED_EDGE('',*,*,#20658,.T.);
#28679=ORIENTED_EDGE('',*,*,#20663,.F.);
#28680=ORIENTED_EDGE('',*,*,#20659,.T.);
#28681=ORIENTED_EDGE('',*,*,#20662,.F.);
#28682=ORIENTED_EDGE('',*,*,#20661,.F.);
#28683=ORIENTED_EDGE('',*,*,#20655,.F.);
#28684=ORIENTED_EDGE('',*,*,#20664,.F.);
#28685=ORIENTED_EDGE('',*,*,#20665,.T.);
#28686=ORIENTED_EDGE('',*,*,#20666,.T.);
#28687=ORIENTED_EDGE('',*,*,#20667,.T.);
#28688=ORIENTED_EDGE('',*,*,#20666,.F.);
#28689=ORIENTED_EDGE('',*,*,#20668,.T.);
#28690=ORIENTED_EDGE('',*,*,#20669,.F.);
#28691=ORIENTED_EDGE('',*,*,#20670,.F.);
#28692=ORIENTED_EDGE('',*,*,#20671,.F.);
#28693=ORIENTED_EDGE('',*,*,#20672,.F.);
#28694=ORIENTED_EDGE('',*,*,#20668,.F.);
#28695=ORIENTED_EDGE('',*,*,#20665,.F.);
#28696=ORIENTED_EDGE('',*,*,#20673,.T.);
#28697=ORIENTED_EDGE('',*,*,#20674,.T.);
#28698=ORIENTED_EDGE('',*,*,#20670,.T.);
#28699=ORIENTED_EDGE('',*,*,#20675,.F.);
#28700=ORIENTED_EDGE('',*,*,#20671,.T.);
#28701=ORIENTED_EDGE('',*,*,#20674,.F.);
#28702=ORIENTED_EDGE('',*,*,#20673,.F.);
#28703=ORIENTED_EDGE('',*,*,#20667,.F.);
#28704=ORIENTED_EDGE('',*,*,#20676,.F.);
#28705=ORIENTED_EDGE('',*,*,#20677,.T.);
#28706=ORIENTED_EDGE('',*,*,#20678,.T.);
#28707=ORIENTED_EDGE('',*,*,#20679,.T.);
#28708=ORIENTED_EDGE('',*,*,#20678,.F.);
#28709=ORIENTED_EDGE('',*,*,#20680,.T.);
#28710=ORIENTED_EDGE('',*,*,#20681,.F.);
#28711=ORIENTED_EDGE('',*,*,#20682,.F.);
#28712=ORIENTED_EDGE('',*,*,#20683,.F.);
#28713=ORIENTED_EDGE('',*,*,#20684,.F.);
#28714=ORIENTED_EDGE('',*,*,#20680,.F.);
#28715=ORIENTED_EDGE('',*,*,#20677,.F.);
#28716=ORIENTED_EDGE('',*,*,#20685,.T.);
#28717=ORIENTED_EDGE('',*,*,#20686,.T.);
#28718=ORIENTED_EDGE('',*,*,#20682,.T.);
#28719=ORIENTED_EDGE('',*,*,#20687,.F.);
#28720=ORIENTED_EDGE('',*,*,#20683,.T.);
#28721=ORIENTED_EDGE('',*,*,#20686,.F.);
#28722=ORIENTED_EDGE('',*,*,#20685,.F.);
#28723=ORIENTED_EDGE('',*,*,#20679,.F.);
#28724=ORIENTED_EDGE('',*,*,#20688,.F.);
#28725=ORIENTED_EDGE('',*,*,#20689,.T.);
#28726=ORIENTED_EDGE('',*,*,#20690,.T.);
#28727=ORIENTED_EDGE('',*,*,#20691,.T.);
#28728=ORIENTED_EDGE('',*,*,#20690,.F.);
#28729=ORIENTED_EDGE('',*,*,#20692,.T.);
#28730=ORIENTED_EDGE('',*,*,#20693,.F.);
#28731=ORIENTED_EDGE('',*,*,#20694,.F.);
#28732=ORIENTED_EDGE('',*,*,#20695,.F.);
#28733=ORIENTED_EDGE('',*,*,#20696,.F.);
#28734=ORIENTED_EDGE('',*,*,#20692,.F.);
#28735=ORIENTED_EDGE('',*,*,#20689,.F.);
#28736=ORIENTED_EDGE('',*,*,#20697,.T.);
#28737=ORIENTED_EDGE('',*,*,#20698,.T.);
#28738=ORIENTED_EDGE('',*,*,#20694,.T.);
#28739=ORIENTED_EDGE('',*,*,#20699,.F.);
#28740=ORIENTED_EDGE('',*,*,#20695,.T.);
#28741=ORIENTED_EDGE('',*,*,#20698,.F.);
#28742=ORIENTED_EDGE('',*,*,#20697,.F.);
#28743=ORIENTED_EDGE('',*,*,#20691,.F.);
#28744=ORIENTED_EDGE('',*,*,#20700,.F.);
#28745=ORIENTED_EDGE('',*,*,#20701,.T.);
#28746=ORIENTED_EDGE('',*,*,#20702,.T.);
#28747=ORIENTED_EDGE('',*,*,#20703,.T.);
#28748=ORIENTED_EDGE('',*,*,#20702,.F.);
#28749=ORIENTED_EDGE('',*,*,#20704,.T.);
#28750=ORIENTED_EDGE('',*,*,#20705,.F.);
#28751=ORIENTED_EDGE('',*,*,#20706,.F.);
#28752=ORIENTED_EDGE('',*,*,#20707,.F.);
#28753=ORIENTED_EDGE('',*,*,#20708,.F.);
#28754=ORIENTED_EDGE('',*,*,#20704,.F.);
#28755=ORIENTED_EDGE('',*,*,#20701,.F.);
#28756=ORIENTED_EDGE('',*,*,#20709,.T.);
#28757=ORIENTED_EDGE('',*,*,#20710,.T.);
#28758=ORIENTED_EDGE('',*,*,#20706,.T.);
#28759=ORIENTED_EDGE('',*,*,#20711,.F.);
#28760=ORIENTED_EDGE('',*,*,#20707,.T.);
#28761=ORIENTED_EDGE('',*,*,#20710,.F.);
#28762=ORIENTED_EDGE('',*,*,#20709,.F.);
#28763=ORIENTED_EDGE('',*,*,#20703,.F.);
#28764=ORIENTED_EDGE('',*,*,#20712,.F.);
#28765=ORIENTED_EDGE('',*,*,#20713,.T.);
#28766=ORIENTED_EDGE('',*,*,#20714,.T.);
#28767=ORIENTED_EDGE('',*,*,#20715,.T.);
#28768=ORIENTED_EDGE('',*,*,#20714,.F.);
#28769=ORIENTED_EDGE('',*,*,#20716,.T.);
#28770=ORIENTED_EDGE('',*,*,#20717,.F.);
#28771=ORIENTED_EDGE('',*,*,#20718,.F.);
#28772=ORIENTED_EDGE('',*,*,#20719,.F.);
#28773=ORIENTED_EDGE('',*,*,#20720,.F.);
#28774=ORIENTED_EDGE('',*,*,#20716,.F.);
#28775=ORIENTED_EDGE('',*,*,#20713,.F.);
#28776=ORIENTED_EDGE('',*,*,#20721,.T.);
#28777=ORIENTED_EDGE('',*,*,#20722,.T.);
#28778=ORIENTED_EDGE('',*,*,#20718,.T.);
#28779=ORIENTED_EDGE('',*,*,#20723,.F.);
#28780=ORIENTED_EDGE('',*,*,#20719,.T.);
#28781=ORIENTED_EDGE('',*,*,#20722,.F.);
#28782=ORIENTED_EDGE('',*,*,#20721,.F.);
#28783=ORIENTED_EDGE('',*,*,#20715,.F.);
#28784=ORIENTED_EDGE('',*,*,#20724,.F.);
#28785=ORIENTED_EDGE('',*,*,#20725,.T.);
#28786=ORIENTED_EDGE('',*,*,#20726,.T.);
#28787=ORIENTED_EDGE('',*,*,#20727,.T.);
#28788=ORIENTED_EDGE('',*,*,#20726,.F.);
#28789=ORIENTED_EDGE('',*,*,#20728,.T.);
#28790=ORIENTED_EDGE('',*,*,#20729,.F.);
#28791=ORIENTED_EDGE('',*,*,#20730,.F.);
#28792=ORIENTED_EDGE('',*,*,#20731,.F.);
#28793=ORIENTED_EDGE('',*,*,#20732,.F.);
#28794=ORIENTED_EDGE('',*,*,#20728,.F.);
#28795=ORIENTED_EDGE('',*,*,#20725,.F.);
#28796=ORIENTED_EDGE('',*,*,#20733,.T.);
#28797=ORIENTED_EDGE('',*,*,#20734,.T.);
#28798=ORIENTED_EDGE('',*,*,#20730,.T.);
#28799=ORIENTED_EDGE('',*,*,#20735,.F.);
#28800=ORIENTED_EDGE('',*,*,#20731,.T.);
#28801=ORIENTED_EDGE('',*,*,#20734,.F.);
#28802=ORIENTED_EDGE('',*,*,#20733,.F.);
#28803=ORIENTED_EDGE('',*,*,#20727,.F.);
#28804=ORIENTED_EDGE('',*,*,#20736,.F.);
#28805=ORIENTED_EDGE('',*,*,#20737,.T.);
#28806=ORIENTED_EDGE('',*,*,#20738,.T.);
#28807=ORIENTED_EDGE('',*,*,#20739,.T.);
#28808=ORIENTED_EDGE('',*,*,#20738,.F.);
#28809=ORIENTED_EDGE('',*,*,#20740,.T.);
#28810=ORIENTED_EDGE('',*,*,#20741,.F.);
#28811=ORIENTED_EDGE('',*,*,#20742,.F.);
#28812=ORIENTED_EDGE('',*,*,#20743,.F.);
#28813=ORIENTED_EDGE('',*,*,#20744,.F.);
#28814=ORIENTED_EDGE('',*,*,#20740,.F.);
#28815=ORIENTED_EDGE('',*,*,#20737,.F.);
#28816=ORIENTED_EDGE('',*,*,#20745,.T.);
#28817=ORIENTED_EDGE('',*,*,#20746,.T.);
#28818=ORIENTED_EDGE('',*,*,#20742,.T.);
#28819=ORIENTED_EDGE('',*,*,#20747,.F.);
#28820=ORIENTED_EDGE('',*,*,#20743,.T.);
#28821=ORIENTED_EDGE('',*,*,#20746,.F.);
#28822=ORIENTED_EDGE('',*,*,#20745,.F.);
#28823=ORIENTED_EDGE('',*,*,#20739,.F.);
#28824=ORIENTED_EDGE('',*,*,#20748,.F.);
#28825=ORIENTED_EDGE('',*,*,#20749,.T.);
#28826=ORIENTED_EDGE('',*,*,#20750,.T.);
#28827=ORIENTED_EDGE('',*,*,#20751,.T.);
#28828=ORIENTED_EDGE('',*,*,#20750,.F.);
#28829=ORIENTED_EDGE('',*,*,#20752,.T.);
#28830=ORIENTED_EDGE('',*,*,#20753,.F.);
#28831=ORIENTED_EDGE('',*,*,#20754,.F.);
#28832=ORIENTED_EDGE('',*,*,#20755,.F.);
#28833=ORIENTED_EDGE('',*,*,#20756,.F.);
#28834=ORIENTED_EDGE('',*,*,#20757,.F.);
#28835=ORIENTED_EDGE('',*,*,#20752,.F.);
#28836=ORIENTED_EDGE('',*,*,#20749,.F.);
#28837=ORIENTED_EDGE('',*,*,#20758,.T.);
#28838=ORIENTED_EDGE('',*,*,#20759,.T.);
#28839=ORIENTED_EDGE('',*,*,#20755,.T.);
#28840=ORIENTED_EDGE('',*,*,#20760,.F.);
#28841=ORIENTED_EDGE('',*,*,#20761,.F.);
#28842=ORIENTED_EDGE('',*,*,#20756,.T.);
#28843=ORIENTED_EDGE('',*,*,#20759,.F.);
#28844=ORIENTED_EDGE('',*,*,#20758,.F.);
#28845=ORIENTED_EDGE('',*,*,#20751,.F.);
#28846=ORIENTED_EDGE('',*,*,#20762,.F.);
#28847=ORIENTED_EDGE('',*,*,#20763,.T.);
#28848=ORIENTED_EDGE('',*,*,#20764,.T.);
#28849=ORIENTED_EDGE('',*,*,#20765,.T.);
#28850=ORIENTED_EDGE('',*,*,#20764,.F.);
#28851=ORIENTED_EDGE('',*,*,#20766,.T.);
#28852=ORIENTED_EDGE('',*,*,#20767,.F.);
#28853=ORIENTED_EDGE('',*,*,#20768,.F.);
#28854=ORIENTED_EDGE('',*,*,#20769,.F.);
#28855=ORIENTED_EDGE('',*,*,#20770,.F.);
#28856=ORIENTED_EDGE('',*,*,#20766,.F.);
#28857=ORIENTED_EDGE('',*,*,#20763,.F.);
#28858=ORIENTED_EDGE('',*,*,#20771,.T.);
#28859=ORIENTED_EDGE('',*,*,#20772,.T.);
#28860=ORIENTED_EDGE('',*,*,#20768,.T.);
#28861=ORIENTED_EDGE('',*,*,#20773,.F.);
#28862=ORIENTED_EDGE('',*,*,#20769,.T.);
#28863=ORIENTED_EDGE('',*,*,#20772,.F.);
#28864=ORIENTED_EDGE('',*,*,#20771,.F.);
#28865=ORIENTED_EDGE('',*,*,#20765,.F.);
#28866=ORIENTED_EDGE('',*,*,#20774,.F.);
#28867=ORIENTED_EDGE('',*,*,#20775,.T.);
#28868=ORIENTED_EDGE('',*,*,#20776,.T.);
#28869=ORIENTED_EDGE('',*,*,#20777,.T.);
#28870=ORIENTED_EDGE('',*,*,#20776,.F.);
#28871=ORIENTED_EDGE('',*,*,#20778,.T.);
#28872=ORIENTED_EDGE('',*,*,#20779,.F.);
#28873=ORIENTED_EDGE('',*,*,#20780,.F.);
#28874=ORIENTED_EDGE('',*,*,#20781,.F.);
#28875=ORIENTED_EDGE('',*,*,#20782,.F.);
#28876=ORIENTED_EDGE('',*,*,#20778,.F.);
#28877=ORIENTED_EDGE('',*,*,#20775,.F.);
#28878=ORIENTED_EDGE('',*,*,#20783,.T.);
#28879=ORIENTED_EDGE('',*,*,#20784,.T.);
#28880=ORIENTED_EDGE('',*,*,#20780,.T.);
#28881=ORIENTED_EDGE('',*,*,#20785,.F.);
#28882=ORIENTED_EDGE('',*,*,#20781,.T.);
#28883=ORIENTED_EDGE('',*,*,#20784,.F.);
#28884=ORIENTED_EDGE('',*,*,#20783,.F.);
#28885=ORIENTED_EDGE('',*,*,#20777,.F.);
#28886=ORIENTED_EDGE('',*,*,#20786,.F.);
#28887=ORIENTED_EDGE('',*,*,#20787,.T.);
#28888=ORIENTED_EDGE('',*,*,#20788,.T.);
#28889=ORIENTED_EDGE('',*,*,#20789,.T.);
#28890=ORIENTED_EDGE('',*,*,#20788,.F.);
#28891=ORIENTED_EDGE('',*,*,#20790,.T.);
#28892=ORIENTED_EDGE('',*,*,#20791,.F.);
#28893=ORIENTED_EDGE('',*,*,#20792,.F.);
#28894=ORIENTED_EDGE('',*,*,#20793,.F.);
#28895=ORIENTED_EDGE('',*,*,#20794,.F.);
#28896=ORIENTED_EDGE('',*,*,#20790,.F.);
#28897=ORIENTED_EDGE('',*,*,#20787,.F.);
#28898=ORIENTED_EDGE('',*,*,#20795,.T.);
#28899=ORIENTED_EDGE('',*,*,#20796,.T.);
#28900=ORIENTED_EDGE('',*,*,#20792,.T.);
#28901=ORIENTED_EDGE('',*,*,#20797,.F.);
#28902=ORIENTED_EDGE('',*,*,#20793,.T.);
#28903=ORIENTED_EDGE('',*,*,#20796,.F.);
#28904=ORIENTED_EDGE('',*,*,#20795,.F.);
#28905=ORIENTED_EDGE('',*,*,#20789,.F.);
#28906=ORIENTED_EDGE('',*,*,#20798,.F.);
#28907=ORIENTED_EDGE('',*,*,#20799,.T.);
#28908=ORIENTED_EDGE('',*,*,#20800,.T.);
#28909=ORIENTED_EDGE('',*,*,#20801,.T.);
#28910=ORIENTED_EDGE('',*,*,#20800,.F.);
#28911=ORIENTED_EDGE('',*,*,#20802,.T.);
#28912=ORIENTED_EDGE('',*,*,#20803,.F.);
#28913=ORIENTED_EDGE('',*,*,#20804,.F.);
#28914=ORIENTED_EDGE('',*,*,#20805,.F.);
#28915=ORIENTED_EDGE('',*,*,#20806,.F.);
#28916=ORIENTED_EDGE('',*,*,#20802,.F.);
#28917=ORIENTED_EDGE('',*,*,#20799,.F.);
#28918=ORIENTED_EDGE('',*,*,#20807,.T.);
#28919=ORIENTED_EDGE('',*,*,#20808,.T.);
#28920=ORIENTED_EDGE('',*,*,#20804,.T.);
#28921=ORIENTED_EDGE('',*,*,#20809,.F.);
#28922=ORIENTED_EDGE('',*,*,#20805,.T.);
#28923=ORIENTED_EDGE('',*,*,#20808,.F.);
#28924=ORIENTED_EDGE('',*,*,#20807,.F.);
#28925=ORIENTED_EDGE('',*,*,#20801,.F.);
#28926=ORIENTED_EDGE('',*,*,#20810,.F.);
#28927=ORIENTED_EDGE('',*,*,#20811,.T.);
#28928=ORIENTED_EDGE('',*,*,#20812,.T.);
#28929=ORIENTED_EDGE('',*,*,#20813,.T.);
#28930=ORIENTED_EDGE('',*,*,#20812,.F.);
#28931=ORIENTED_EDGE('',*,*,#20814,.T.);
#28932=ORIENTED_EDGE('',*,*,#20815,.F.);
#28933=ORIENTED_EDGE('',*,*,#20816,.F.);
#28934=ORIENTED_EDGE('',*,*,#20817,.F.);
#28935=ORIENTED_EDGE('',*,*,#20818,.F.);
#28936=ORIENTED_EDGE('',*,*,#20814,.F.);
#28937=ORIENTED_EDGE('',*,*,#20811,.F.);
#28938=ORIENTED_EDGE('',*,*,#20819,.T.);
#28939=ORIENTED_EDGE('',*,*,#20820,.T.);
#28940=ORIENTED_EDGE('',*,*,#20816,.T.);
#28941=ORIENTED_EDGE('',*,*,#20821,.F.);
#28942=ORIENTED_EDGE('',*,*,#20817,.T.);
#28943=ORIENTED_EDGE('',*,*,#20820,.F.);
#28944=ORIENTED_EDGE('',*,*,#20819,.F.);
#28945=ORIENTED_EDGE('',*,*,#20813,.F.);
#28946=ORIENTED_EDGE('',*,*,#20822,.F.);
#28947=ORIENTED_EDGE('',*,*,#20823,.T.);
#28948=ORIENTED_EDGE('',*,*,#20824,.T.);
#28949=ORIENTED_EDGE('',*,*,#20825,.T.);
#28950=ORIENTED_EDGE('',*,*,#20824,.F.);
#28951=ORIENTED_EDGE('',*,*,#20826,.T.);
#28952=ORIENTED_EDGE('',*,*,#20827,.F.);
#28953=ORIENTED_EDGE('',*,*,#20828,.F.);
#28954=ORIENTED_EDGE('',*,*,#20829,.F.);
#28955=ORIENTED_EDGE('',*,*,#20830,.F.);
#28956=ORIENTED_EDGE('',*,*,#20826,.F.);
#28957=ORIENTED_EDGE('',*,*,#20823,.F.);
#28958=ORIENTED_EDGE('',*,*,#20831,.T.);
#28959=ORIENTED_EDGE('',*,*,#20832,.T.);
#28960=ORIENTED_EDGE('',*,*,#20828,.T.);
#28961=ORIENTED_EDGE('',*,*,#20833,.F.);
#28962=ORIENTED_EDGE('',*,*,#20829,.T.);
#28963=ORIENTED_EDGE('',*,*,#20832,.F.);
#28964=ORIENTED_EDGE('',*,*,#20831,.F.);
#28965=ORIENTED_EDGE('',*,*,#20825,.F.);
#28966=ORIENTED_EDGE('',*,*,#20834,.F.);
#28967=ORIENTED_EDGE('',*,*,#20835,.T.);
#28968=ORIENTED_EDGE('',*,*,#20836,.T.);
#28969=ORIENTED_EDGE('',*,*,#20837,.T.);
#28970=ORIENTED_EDGE('',*,*,#20836,.F.);
#28971=ORIENTED_EDGE('',*,*,#20838,.T.);
#28972=ORIENTED_EDGE('',*,*,#20839,.F.);
#28973=ORIENTED_EDGE('',*,*,#20840,.F.);
#28974=ORIENTED_EDGE('',*,*,#20841,.F.);
#28975=ORIENTED_EDGE('',*,*,#20842,.F.);
#28976=ORIENTED_EDGE('',*,*,#20838,.F.);
#28977=ORIENTED_EDGE('',*,*,#20835,.F.);
#28978=ORIENTED_EDGE('',*,*,#20843,.T.);
#28979=ORIENTED_EDGE('',*,*,#20844,.T.);
#28980=ORIENTED_EDGE('',*,*,#20840,.T.);
#28981=ORIENTED_EDGE('',*,*,#20845,.F.);
#28982=ORIENTED_EDGE('',*,*,#20841,.T.);
#28983=ORIENTED_EDGE('',*,*,#20844,.F.);
#28984=ORIENTED_EDGE('',*,*,#20843,.F.);
#28985=ORIENTED_EDGE('',*,*,#20837,.F.);
#28986=ORIENTED_EDGE('',*,*,#20846,.F.);
#28987=ORIENTED_EDGE('',*,*,#20847,.T.);
#28988=ORIENTED_EDGE('',*,*,#20848,.T.);
#28989=ORIENTED_EDGE('',*,*,#20849,.T.);
#28990=ORIENTED_EDGE('',*,*,#20848,.F.);
#28991=ORIENTED_EDGE('',*,*,#20850,.T.);
#28992=ORIENTED_EDGE('',*,*,#20851,.F.);
#28993=ORIENTED_EDGE('',*,*,#20852,.F.);
#28994=ORIENTED_EDGE('',*,*,#20853,.F.);
#28995=ORIENTED_EDGE('',*,*,#20854,.F.);
#28996=ORIENTED_EDGE('',*,*,#20850,.F.);
#28997=ORIENTED_EDGE('',*,*,#20847,.F.);
#28998=ORIENTED_EDGE('',*,*,#20855,.T.);
#28999=ORIENTED_EDGE('',*,*,#20856,.T.);
#29000=ORIENTED_EDGE('',*,*,#20852,.T.);
#29001=ORIENTED_EDGE('',*,*,#20857,.F.);
#29002=ORIENTED_EDGE('',*,*,#20853,.T.);
#29003=ORIENTED_EDGE('',*,*,#20856,.F.);
#29004=ORIENTED_EDGE('',*,*,#20855,.F.);
#29005=ORIENTED_EDGE('',*,*,#20849,.F.);
#29006=ORIENTED_EDGE('',*,*,#20858,.F.);
#29007=ORIENTED_EDGE('',*,*,#20859,.T.);
#29008=ORIENTED_EDGE('',*,*,#20860,.T.);
#29009=ORIENTED_EDGE('',*,*,#20861,.T.);
#29010=ORIENTED_EDGE('',*,*,#20860,.F.);
#29011=ORIENTED_EDGE('',*,*,#20862,.T.);
#29012=ORIENTED_EDGE('',*,*,#20863,.F.);
#29013=ORIENTED_EDGE('',*,*,#20864,.F.);
#29014=ORIENTED_EDGE('',*,*,#20865,.F.);
#29015=ORIENTED_EDGE('',*,*,#20866,.F.);
#29016=ORIENTED_EDGE('',*,*,#20862,.F.);
#29017=ORIENTED_EDGE('',*,*,#20859,.F.);
#29018=ORIENTED_EDGE('',*,*,#20867,.T.);
#29019=ORIENTED_EDGE('',*,*,#20868,.T.);
#29020=ORIENTED_EDGE('',*,*,#20864,.T.);
#29021=ORIENTED_EDGE('',*,*,#20869,.F.);
#29022=ORIENTED_EDGE('',*,*,#20865,.T.);
#29023=ORIENTED_EDGE('',*,*,#20868,.F.);
#29024=ORIENTED_EDGE('',*,*,#20867,.F.);
#29025=ORIENTED_EDGE('',*,*,#20861,.F.);
#29026=ORIENTED_EDGE('',*,*,#20870,.F.);
#29027=ORIENTED_EDGE('',*,*,#20871,.T.);
#29028=ORIENTED_EDGE('',*,*,#20872,.T.);
#29029=ORIENTED_EDGE('',*,*,#20873,.T.);
#29030=ORIENTED_EDGE('',*,*,#20872,.F.);
#29031=ORIENTED_EDGE('',*,*,#20874,.T.);
#29032=ORIENTED_EDGE('',*,*,#20875,.F.);
#29033=ORIENTED_EDGE('',*,*,#20876,.F.);
#29034=ORIENTED_EDGE('',*,*,#20877,.F.);
#29035=ORIENTED_EDGE('',*,*,#20878,.F.);
#29036=ORIENTED_EDGE('',*,*,#20874,.F.);
#29037=ORIENTED_EDGE('',*,*,#20871,.F.);
#29038=ORIENTED_EDGE('',*,*,#20879,.T.);
#29039=ORIENTED_EDGE('',*,*,#20880,.T.);
#29040=ORIENTED_EDGE('',*,*,#20876,.T.);
#29041=ORIENTED_EDGE('',*,*,#20881,.F.);
#29042=ORIENTED_EDGE('',*,*,#20877,.T.);
#29043=ORIENTED_EDGE('',*,*,#20880,.F.);
#29044=ORIENTED_EDGE('',*,*,#20879,.F.);
#29045=ORIENTED_EDGE('',*,*,#20873,.F.);
#29046=ORIENTED_EDGE('',*,*,#20882,.F.);
#29047=ORIENTED_EDGE('',*,*,#20883,.T.);
#29048=ORIENTED_EDGE('',*,*,#20884,.T.);
#29049=ORIENTED_EDGE('',*,*,#20885,.T.);
#29050=ORIENTED_EDGE('',*,*,#20884,.F.);
#29051=ORIENTED_EDGE('',*,*,#20886,.T.);
#29052=ORIENTED_EDGE('',*,*,#20887,.F.);
#29053=ORIENTED_EDGE('',*,*,#20888,.F.);
#29054=ORIENTED_EDGE('',*,*,#20889,.F.);
#29055=ORIENTED_EDGE('',*,*,#20890,.F.);
#29056=ORIENTED_EDGE('',*,*,#20886,.F.);
#29057=ORIENTED_EDGE('',*,*,#20883,.F.);
#29058=ORIENTED_EDGE('',*,*,#20891,.T.);
#29059=ORIENTED_EDGE('',*,*,#20892,.T.);
#29060=ORIENTED_EDGE('',*,*,#20888,.T.);
#29061=ORIENTED_EDGE('',*,*,#20893,.F.);
#29062=ORIENTED_EDGE('',*,*,#20889,.T.);
#29063=ORIENTED_EDGE('',*,*,#20892,.F.);
#29064=ORIENTED_EDGE('',*,*,#20891,.F.);
#29065=ORIENTED_EDGE('',*,*,#20885,.F.);
#29066=ORIENTED_EDGE('',*,*,#20626,.F.);
#29067=ORIENTED_EDGE('',*,*,#20894,.T.);
#29068=ORIENTED_EDGE('',*,*,#20895,.T.);
#29069=ORIENTED_EDGE('',*,*,#20894,.F.);
#29070=ORIENTED_EDGE('',*,*,#20618,.F.);
#29071=ORIENTED_EDGE('',*,*,#20896,.T.);
#29072=ORIENTED_EDGE('',*,*,#20760,.T.);
#29073=ORIENTED_EDGE('',*,*,#20754,.T.);
#29074=ORIENTED_EDGE('',*,*,#20748,.T.);
#29075=ORIENTED_EDGE('',*,*,#20897,.T.);
#29076=ORIENTED_EDGE('',*,*,#20627,.T.);
#29077=ORIENTED_EDGE('',*,*,#20897,.F.);
#29078=ORIENTED_EDGE('',*,*,#20753,.T.);
#29079=ORIENTED_EDGE('',*,*,#20757,.T.);
#29080=ORIENTED_EDGE('',*,*,#20761,.T.);
#29081=ORIENTED_EDGE('',*,*,#20896,.F.);
#29082=ORIENTED_EDGE('',*,*,#20639,.T.);
#29083=ORIENTED_EDGE('',*,*,#20633,.T.);
#29084=ORIENTED_EDGE('',*,*,#20628,.T.);
#29085=ORIENTED_EDGE('',*,*,#20636,.T.);
#29086=ORIENTED_EDGE('',*,*,#20651,.T.);
#29087=ORIENTED_EDGE('',*,*,#20645,.T.);
#29088=ORIENTED_EDGE('',*,*,#20640,.T.);
#29089=ORIENTED_EDGE('',*,*,#20648,.T.);
#29090=ORIENTED_EDGE('',*,*,#20663,.T.);
#29091=ORIENTED_EDGE('',*,*,#20657,.T.);
#29092=ORIENTED_EDGE('',*,*,#20652,.T.);
#29093=ORIENTED_EDGE('',*,*,#20660,.T.);
#29094=ORIENTED_EDGE('',*,*,#20675,.T.);
#29095=ORIENTED_EDGE('',*,*,#20669,.T.);
#29096=ORIENTED_EDGE('',*,*,#20664,.T.);
#29097=ORIENTED_EDGE('',*,*,#20672,.T.);
#29098=ORIENTED_EDGE('',*,*,#20687,.T.);
#29099=ORIENTED_EDGE('',*,*,#20681,.T.);
#29100=ORIENTED_EDGE('',*,*,#20676,.T.);
#29101=ORIENTED_EDGE('',*,*,#20684,.T.);
#29102=ORIENTED_EDGE('',*,*,#20699,.T.);
#29103=ORIENTED_EDGE('',*,*,#20693,.T.);
#29104=ORIENTED_EDGE('',*,*,#20688,.T.);
#29105=ORIENTED_EDGE('',*,*,#20696,.T.);
#29106=ORIENTED_EDGE('',*,*,#20711,.T.);
#29107=ORIENTED_EDGE('',*,*,#20705,.T.);
#29108=ORIENTED_EDGE('',*,*,#20700,.T.);
#29109=ORIENTED_EDGE('',*,*,#20708,.T.);
#29110=ORIENTED_EDGE('',*,*,#20723,.T.);
#29111=ORIENTED_EDGE('',*,*,#20717,.T.);
#29112=ORIENTED_EDGE('',*,*,#20712,.T.);
#29113=ORIENTED_EDGE('',*,*,#20720,.T.);
#29114=ORIENTED_EDGE('',*,*,#20735,.T.);
#29115=ORIENTED_EDGE('',*,*,#20729,.T.);
#29116=ORIENTED_EDGE('',*,*,#20724,.T.);
#29117=ORIENTED_EDGE('',*,*,#20732,.T.);
#29118=ORIENTED_EDGE('',*,*,#20747,.T.);
#29119=ORIENTED_EDGE('',*,*,#20741,.T.);
#29120=ORIENTED_EDGE('',*,*,#20736,.T.);
#29121=ORIENTED_EDGE('',*,*,#20744,.T.);
#29122=ORIENTED_EDGE('',*,*,#20773,.T.);
#29123=ORIENTED_EDGE('',*,*,#20767,.T.);
#29124=ORIENTED_EDGE('',*,*,#20762,.T.);
#29125=ORIENTED_EDGE('',*,*,#20770,.T.);
#29126=ORIENTED_EDGE('',*,*,#20785,.T.);
#29127=ORIENTED_EDGE('',*,*,#20779,.T.);
#29128=ORIENTED_EDGE('',*,*,#20774,.T.);
#29129=ORIENTED_EDGE('',*,*,#20782,.T.);
#29130=ORIENTED_EDGE('',*,*,#20797,.T.);
#29131=ORIENTED_EDGE('',*,*,#20791,.T.);
#29132=ORIENTED_EDGE('',*,*,#20786,.T.);
#29133=ORIENTED_EDGE('',*,*,#20794,.T.);
#29134=ORIENTED_EDGE('',*,*,#20809,.T.);
#29135=ORIENTED_EDGE('',*,*,#20803,.T.);
#29136=ORIENTED_EDGE('',*,*,#20798,.T.);
#29137=ORIENTED_EDGE('',*,*,#20806,.T.);
#29138=ORIENTED_EDGE('',*,*,#20821,.T.);
#29139=ORIENTED_EDGE('',*,*,#20815,.T.);
#29140=ORIENTED_EDGE('',*,*,#20810,.T.);
#29141=ORIENTED_EDGE('',*,*,#20818,.T.);
#29142=ORIENTED_EDGE('',*,*,#20833,.T.);
#29143=ORIENTED_EDGE('',*,*,#20827,.T.);
#29144=ORIENTED_EDGE('',*,*,#20822,.T.);
#29145=ORIENTED_EDGE('',*,*,#20830,.T.);
#29146=ORIENTED_EDGE('',*,*,#20845,.T.);
#29147=ORIENTED_EDGE('',*,*,#20839,.T.);
#29148=ORIENTED_EDGE('',*,*,#20834,.T.);
#29149=ORIENTED_EDGE('',*,*,#20842,.T.);
#29150=ORIENTED_EDGE('',*,*,#20857,.T.);
#29151=ORIENTED_EDGE('',*,*,#20851,.T.);
#29152=ORIENTED_EDGE('',*,*,#20846,.T.);
#29153=ORIENTED_EDGE('',*,*,#20854,.T.);
#29154=ORIENTED_EDGE('',*,*,#20869,.T.);
#29155=ORIENTED_EDGE('',*,*,#20863,.T.);
#29156=ORIENTED_EDGE('',*,*,#20858,.T.);
#29157=ORIENTED_EDGE('',*,*,#20866,.T.);
#29158=ORIENTED_EDGE('',*,*,#20881,.T.);
#29159=ORIENTED_EDGE('',*,*,#20875,.T.);
#29160=ORIENTED_EDGE('',*,*,#20870,.T.);
#29161=ORIENTED_EDGE('',*,*,#20878,.T.);
#29162=ORIENTED_EDGE('',*,*,#20893,.T.);
#29163=ORIENTED_EDGE('',*,*,#20887,.T.);
#29164=ORIENTED_EDGE('',*,*,#20882,.T.);
#29165=ORIENTED_EDGE('',*,*,#20890,.T.);
#29166=ORIENTED_EDGE('',*,*,#20898,.F.);
#29167=ORIENTED_EDGE('',*,*,#20899,.T.);
#29168=ORIENTED_EDGE('',*,*,#20619,.T.);
#29169=ORIENTED_EDGE('',*,*,#20899,.F.);
#29170=ORIENTED_EDGE('',*,*,#20898,.T.);
#29171=ORIENTED_EDGE('',*,*,#20900,.F.);
#29172=ORIENTED_EDGE('',*,*,#20900,.T.);
#29173=ORIENTED_EDGE('',*,*,#20901,.T.);
#29174=ORIENTED_EDGE('',*,*,#20902,.F.);
#29175=ORIENTED_EDGE('',*,*,#20901,.F.);
#29176=ORIENTED_EDGE('',*,*,#20902,.T.);
#29177=ORIENTED_EDGE('',*,*,#20903,.T.);
#29178=ORIENTED_EDGE('',*,*,#20904,.F.);
#29179=ORIENTED_EDGE('',*,*,#20903,.F.);
#29180=ORIENTED_EDGE('',*,*,#20904,.T.);
#29181=ORIENTED_EDGE('',*,*,#20905,.T.);
#29182=ORIENTED_EDGE('',*,*,#20906,.F.);
#29183=ORIENTED_EDGE('',*,*,#20905,.F.);
#29184=ORIENTED_EDGE('',*,*,#20895,.F.);
#29185=ORIENTED_EDGE('',*,*,#20906,.T.);
#31998=CONICAL_SURFACE('',#36395,25.6346416389917,0.785398163397446);
#31999=CONICAL_SURFACE('',#36403,22.5243990607509,0.785398163397447);
#32000=CONICAL_SURFACE('',#36416,2.7,0.0349065850398862);
#32001=CONICAL_SURFACE('',#36429,2.7,0.0349065850398862);
#32002=CONICAL_SURFACE('',#36442,2.7,0.0349065850398862);
#32003=CONICAL_SURFACE('',#36455,2.7,0.0349065850398862);
#32004=CONICAL_SURFACE('',#36468,2.7,0.0349065850398862);
#32005=CONICAL_SURFACE('',#36481,2.7,0.0349065850398862);
#32006=CONICAL_SURFACE('',#36494,2.7,0.0349065850398862);
#32007=CONICAL_SURFACE('',#36507,2.7,0.0349065850398862);
#32008=CONICAL_SURFACE('',#36520,2.7,0.0349065850398862);
#32009=CONICAL_SURFACE('',#36533,2.7,0.0349065850398862);
#32010=CONICAL_SURFACE('',#36546,2.7,0.0349065850398862);
#32011=CONICAL_SURFACE('',#36559,2.7,0.0349065850398862);
#32012=CONICAL_SURFACE('',#36572,2.7,0.0349065850398862);
#32013=CONICAL_SURFACE('',#36585,2.7,0.0349065850398862);
#32014=CONICAL_SURFACE('',#36598,2.7,0.0349065850398862);
#32015=CONICAL_SURFACE('',#36611,2.7,0.0349065850398862);
#32016=CONICAL_SURFACE('',#36624,2.7,0.0349065850398862);
#32017=CONICAL_SURFACE('',#36637,2.7,0.0349065850398862);
#32018=CONICAL_SURFACE('',#36650,2.7,0.0349065850398862);
#32019=CONICAL_SURFACE('',#36663,2.7,0.0349065850398862);
#32020=CONICAL_SURFACE('',#36676,2.7,0.0349065850398862);
#32021=CONICAL_SURFACE('',#36689,2.7,0.0349065850398862);
#32022=CONICAL_SURFACE('',#36697,22.5743990607509,0.785398163397443);
#32023=CONICAL_SURFACE('',#36699,22.011553150687,0.0872664625997167);
#32024=CONICAL_SURFACE('',#36700,25.6346416389917,0.785398163397448);
#32025=CONICAL_SURFACE('',#36704,17.894,0.785398163397448);
#32026=CONICAL_SURFACE('',#36708,17.794,0.785398163397449);
#33527=ADVANCED_FACE('',(#4553),#31998,.T.);
#33528=ADVANCED_FACE('',(#4554,#1240),#2597,.T.);
#33529=ADVANCED_FACE('',(#4555),#3061,.T.);
#33530=ADVANCED_FACE('',(#4556),#31999,.T.);
#33531=ADVANCED_FACE('',(#4557),#3062,.T.);
#33532=ADVANCED_FACE('',(#4558,#1241),#2598,.T.);
#33533=ADVANCED_FACE('',(#4559),#96,.T.);
#33534=ADVANCED_FACE('',(#4560),#32000,.T.);
#33535=ADVANCED_FACE('',(#4561),#97,.T.);
#33536=ADVANCED_FACE('',(#4562),#2599,.T.);
#33537=ADVANCED_FACE('',(#4563),#2600,.T.);
#33538=ADVANCED_FACE('',(#4564),#98,.T.);
#33539=ADVANCED_FACE('',(#4565),#32001,.T.);
#33540=ADVANCED_FACE('',(#4566),#99,.T.);
#33541=ADVANCED_FACE('',(#4567),#2601,.T.);
#33542=ADVANCED_FACE('',(#4568),#2602,.T.);
#33543=ADVANCED_FACE('',(#4569),#100,.T.);
#33544=ADVANCED_FACE('',(#4570),#32002,.T.);
#33545=ADVANCED_FACE('',(#4571),#101,.T.);
#33546=ADVANCED_FACE('',(#4572),#2603,.T.);
#33547=ADVANCED_FACE('',(#4573),#2604,.T.);
#33548=ADVANCED_FACE('',(#4574),#102,.T.);
#33549=ADVANCED_FACE('',(#4575),#32003,.T.);
#33550=ADVANCED_FACE('',(#4576),#103,.T.);
#33551=ADVANCED_FACE('',(#4577),#2605,.T.);
#33552=ADVANCED_FACE('',(#4578),#2606,.T.);
#33553=ADVANCED_FACE('',(#4579),#104,.T.);
#33554=ADVANCED_FACE('',(#4580),#32004,.T.);
#33555=ADVANCED_FACE('',(#4581),#105,.T.);
#33556=ADVANCED_FACE('',(#4582),#2607,.T.);
#33557=ADVANCED_FACE('',(#4583),#2608,.T.);
#33558=ADVANCED_FACE('',(#4584),#106,.T.);
#33559=ADVANCED_FACE('',(#4585),#32005,.T.);
#33560=ADVANCED_FACE('',(#4586),#107,.T.);
#33561=ADVANCED_FACE('',(#4587),#2609,.T.);
#33562=ADVANCED_FACE('',(#4588),#2610,.T.);
#33563=ADVANCED_FACE('',(#4589),#108,.T.);
#33564=ADVANCED_FACE('',(#4590),#32006,.T.);
#33565=ADVANCED_FACE('',(#4591),#109,.T.);
#33566=ADVANCED_FACE('',(#4592),#2611,.T.);
#33567=ADVANCED_FACE('',(#4593),#2612,.T.);
#33568=ADVANCED_FACE('',(#4594),#110,.T.);
#33569=ADVANCED_FACE('',(#4595),#32007,.T.);
#33570=ADVANCED_FACE('',(#4596),#111,.T.);
#33571=ADVANCED_FACE('',(#4597),#2613,.T.);
#33572=ADVANCED_FACE('',(#4598),#2614,.T.);
#33573=ADVANCED_FACE('',(#4599),#112,.T.);
#33574=ADVANCED_FACE('',(#4600),#32008,.T.);
#33575=ADVANCED_FACE('',(#4601),#113,.T.);
#33576=ADVANCED_FACE('',(#4602),#2615,.T.);
#33577=ADVANCED_FACE('',(#4603),#2616,.T.);
#33578=ADVANCED_FACE('',(#4604),#114,.T.);
#33579=ADVANCED_FACE('',(#4605),#32009,.T.);
#33580=ADVANCED_FACE('',(#4606),#115,.T.);
#33581=ADVANCED_FACE('',(#4607),#2617,.T.);
#33582=ADVANCED_FACE('',(#4608),#2618,.T.);
#33583=ADVANCED_FACE('',(#4609),#116,.T.);
#33584=ADVANCED_FACE('',(#4610),#32010,.T.);
#33585=ADVANCED_FACE('',(#4611),#117,.T.);
#33586=ADVANCED_FACE('',(#4612),#2619,.T.);
#33587=ADVANCED_FACE('',(#4613),#2620,.T.);
#33588=ADVANCED_FACE('',(#4614),#118,.T.);
#33589=ADVANCED_FACE('',(#4615),#32011,.T.);
#33590=ADVANCED_FACE('',(#4616),#119,.T.);
#33591=ADVANCED_FACE('',(#4617),#2621,.T.);
#33592=ADVANCED_FACE('',(#4618),#2622,.T.);
#33593=ADVANCED_FACE('',(#4619),#120,.T.);
#33594=ADVANCED_FACE('',(#4620),#32012,.T.);
#33595=ADVANCED_FACE('',(#4621),#121,.T.);
#33596=ADVANCED_FACE('',(#4622),#2623,.T.);
#33597=ADVANCED_FACE('',(#4623),#2624,.T.);
#33598=ADVANCED_FACE('',(#4624),#122,.T.);
#33599=ADVANCED_FACE('',(#4625),#32013,.T.);
#33600=ADVANCED_FACE('',(#4626),#123,.T.);
#33601=ADVANCED_FACE('',(#4627),#2625,.T.);
#33602=ADVANCED_FACE('',(#4628),#2626,.T.);
#33603=ADVANCED_FACE('',(#4629),#124,.T.);
#33604=ADVANCED_FACE('',(#4630),#32014,.T.);
#33605=ADVANCED_FACE('',(#4631),#125,.T.);
#33606=ADVANCED_FACE('',(#4632),#2627,.T.);
#33607=ADVANCED_FACE('',(#4633),#2628,.T.);
#33608=ADVANCED_FACE('',(#4634),#126,.T.);
#33609=ADVANCED_FACE('',(#4635),#32015,.T.);
#33610=ADVANCED_FACE('',(#4636),#127,.T.);
#33611=ADVANCED_FACE('',(#4637),#2629,.T.);
#33612=ADVANCED_FACE('',(#4638),#2630,.T.);
#33613=ADVANCED_FACE('',(#4639),#128,.T.);
#33614=ADVANCED_FACE('',(#4640),#32016,.T.);
#33615=ADVANCED_FACE('',(#4641),#129,.T.);
#33616=ADVANCED_FACE('',(#4642),#2631,.T.);
#33617=ADVANCED_FACE('',(#4643),#2632,.T.);
#33618=ADVANCED_FACE('',(#4644),#130,.T.);
#33619=ADVANCED_FACE('',(#4645),#32017,.T.);
#33620=ADVANCED_FACE('',(#4646),#131,.T.);
#33621=ADVANCED_FACE('',(#4647),#2633,.T.);
#33622=ADVANCED_FACE('',(#4648),#2634,.T.);
#33623=ADVANCED_FACE('',(#4649),#132,.T.);
#33624=ADVANCED_FACE('',(#4650),#32018,.T.);
#33625=ADVANCED_FACE('',(#4651),#133,.T.);
#33626=ADVANCED_FACE('',(#4652),#2635,.T.);
#33627=ADVANCED_FACE('',(#4653),#2636,.T.);
#33628=ADVANCED_FACE('',(#4654),#134,.T.);
#33629=ADVANCED_FACE('',(#4655),#32019,.T.);
#33630=ADVANCED_FACE('',(#4656),#135,.T.);
#33631=ADVANCED_FACE('',(#4657),#2637,.T.);
#33632=ADVANCED_FACE('',(#4658),#2638,.T.);
#33633=ADVANCED_FACE('',(#4659),#136,.T.);
#33634=ADVANCED_FACE('',(#4660),#32020,.T.);
#33635=ADVANCED_FACE('',(#4661),#137,.T.);
#33636=ADVANCED_FACE('',(#4662),#2639,.T.);
#33637=ADVANCED_FACE('',(#4663),#2640,.T.);
#33638=ADVANCED_FACE('',(#4664),#138,.T.);
#33639=ADVANCED_FACE('',(#4665),#32021,.T.);
#33640=ADVANCED_FACE('',(#4666),#139,.T.);
#33641=ADVANCED_FACE('',(#4667),#2641,.T.);
#33642=ADVANCED_FACE('',(#4668),#2642,.T.);
#33643=ADVANCED_FACE('',(#4669),#32022,.T.);
#33644=ADVANCED_FACE('',(#4670,#1242,#1243,#1244,#1245,#1246,#1247,#1248,
#1249,#1250,#1251,#1252,#1253,#1254,#1255,#1256,#1257,#1258,#1259,#1260,
#1261,#1262),#32023,.T.);
#33645=ADVANCED_FACE('',(#4671),#32024,.T.);
#33646=ADVANCED_FACE('',(#4672,#1263),#2643,.T.);
#33647=ADVANCED_FACE('',(#4673),#32025,.F.);
#33648=ADVANCED_FACE('',(#4674),#3063,.F.);
#33649=ADVANCED_FACE('',(#4675),#32026,.F.);
#33650=ADVANCED_FACE('',(#4676,#1264),#2644,.T.);
#34212=CLOSED_SHELL('',(#33527,#33528,#33529,#33530,#33531,#33532,#33533,
#33534,#33535,#33536,#33537,#33538,#33539,#33540,#33541,#33542,#33543,#33544,
#33545,#33546,#33547,#33548,#33549,#33550,#33551,#33552,#33553,#33554,#33555,
#33556,#33557,#33558,#33559,#33560,#33561,#33562,#33563,#33564,#33565,#33566,
#33567,#33568,#33569,#33570,#33571,#33572,#33573,#33574,#33575,#33576,#33577,
#33578,#33579,#33580,#33581,#33582,#33583,#33584,#33585,#33586,#33587,#33588,
#33589,#33590,#33591,#33592,#33593,#33594,#33595,#33596,#33597,#33598,#33599,
#33600,#33601,#33602,#33603,#33604,#33605,#33606,#33607,#33608,#33609,#33610,
#33611,#33612,#33613,#33614,#33615,#33616,#33617,#33618,#33619,#33620,#33621,
#33622,#33623,#33624,#33625,#33626,#33627,#33628,#33629,#33630,#33631,#33632,
#33633,#33634,#33635,#33636,#33637,#33638,#33639,#33640,#33641,#33642,#33643,
#33644,#33645,#33646,#33647,#33648,#33649,#33650));
#36394=AXIS2_PLACEMENT_3D('',#58046,#44120,#44121);
#36395=AXIS2_PLACEMENT_3D('',#58047,#44122,#44123);
#36396=AXIS2_PLACEMENT_3D('',#58050,#44124,#44125);
#36397=AXIS2_PLACEMENT_3D('',#58051,#44126,#44127);
#36398=AXIS2_PLACEMENT_3D('',#58054,#44129,#44130);
#36399=AXIS2_PLACEMENT_3D('',#58055,#44131,#44132);
#36400=AXIS2_PLACEMENT_3D('',#58057,#44133,#44134);
#36401=AXIS2_PLACEMENT_3D('',#58058,#44135,#44136);
#36402=AXIS2_PLACEMENT_3D('',#58060,#44137,#44138);
#36403=AXIS2_PLACEMENT_3D('',#58062,#44140,#44141);
#36404=AXIS2_PLACEMENT_3D('',#58064,#44142,#44143);
#36405=AXIS2_PLACEMENT_3D('',#58068,#44145,#44146);
#36406=AXIS2_PLACEMENT_3D('',#58069,#44147,#44148);
#36407=AXIS2_PLACEMENT_3D('',#58070,#44149,#44150);
#36408=AXIS2_PLACEMENT_3D('',#58073,#44152,#44153);
#36409=AXIS2_PLACEMENT_3D('',#58074,#44154,#44155);
#36410=AXIS2_PLACEMENT_3D('',#58076,#44156,#44157);
#36411=AXIS2_PLACEMENT_3D('',#58077,#44158,#44159);
#36412=AXIS2_PLACEMENT_3D('',#58109,#44160,#44161);
#36413=AXIS2_PLACEMENT_3D('',#58111,#44162,#44163);
#36414=AXIS2_PLACEMENT_3D('',#58112,#44164,#44165);
#36415=AXIS2_PLACEMENT_3D('',#58113,#44166,#44167);
#36416=AXIS2_PLACEMENT_3D('',#58114,#44168,#44169);
#36417=AXIS2_PLACEMENT_3D('',#58121,#44170,#44171);
#36418=AXIS2_PLACEMENT_3D('',#58123,#44172,#44173);
#36419=AXIS2_PLACEMENT_3D('',#58128,#44174,#44175);
#36420=AXIS2_PLACEMENT_3D('',#58130,#44176,#44177);
#36421=AXIS2_PLACEMENT_3D('',#58131,#44178,#44179);
#36422=AXIS2_PLACEMENT_3D('',#58161,#44180,#44181);
#36423=AXIS2_PLACEMENT_3D('',#58162,#44182,#44183);
#36424=AXIS2_PLACEMENT_3D('',#58163,#44184,#44185);
#36425=AXIS2_PLACEMENT_3D('',#58199,#44186,#44187);
#36426=AXIS2_PLACEMENT_3D('',#58201,#44188,#44189);
#36427=AXIS2_PLACEMENT_3D('',#58202,#44190,#44191);
#36428=AXIS2_PLACEMENT_3D('',#58203,#44192,#44193);
#36429=AXIS2_PLACEMENT_3D('',#58204,#44194,#44195);
#36430=AXIS2_PLACEMENT_3D('',#58211,#44196,#44197);
#36431=AXIS2_PLACEMENT_3D('',#58213,#44198,#44199);
#36432=AXIS2_PLACEMENT_3D('',#58218,#44200,#44201);
#36433=AXIS2_PLACEMENT_3D('',#58220,#44202,#44203);
#36434=AXIS2_PLACEMENT_3D('',#58221,#44204,#44205);
#36435=AXIS2_PLACEMENT_3D('',#58255,#44206,#44207);
#36436=AXIS2_PLACEMENT_3D('',#58256,#44208,#44209);
#36437=AXIS2_PLACEMENT_3D('',#58257,#44210,#44211);
#36438=AXIS2_PLACEMENT_3D('',#58293,#44212,#44213);
#36439=AXIS2_PLACEMENT_3D('',#58295,#44214,#44215);
#36440=AXIS2_PLACEMENT_3D('',#58296,#44216,#44217);
#36441=AXIS2_PLACEMENT_3D('',#58297,#44218,#44219);
#36442=AXIS2_PLACEMENT_3D('',#58298,#44220,#44221);
#36443=AXIS2_PLACEMENT_3D('',#58305,#44222,#44223);
#36444=AXIS2_PLACEMENT_3D('',#58307,#44224,#44225);
#36445=AXIS2_PLACEMENT_3D('',#58312,#44226,#44227);
#36446=AXIS2_PLACEMENT_3D('',#58314,#44228,#44229);
#36447=AXIS2_PLACEMENT_3D('',#58315,#44230,#44231);
#36448=AXIS2_PLACEMENT_3D('',#58349,#44232,#44233);
#36449=AXIS2_PLACEMENT_3D('',#58350,#44234,#44235);
#36450=AXIS2_PLACEMENT_3D('',#58351,#44236,#44237);
#36451=AXIS2_PLACEMENT_3D('',#58387,#44238,#44239);
#36452=AXIS2_PLACEMENT_3D('',#58389,#44240,#44241);
#36453=AXIS2_PLACEMENT_3D('',#58390,#44242,#44243);
#36454=AXIS2_PLACEMENT_3D('',#58391,#44244,#44245);
#36455=AXIS2_PLACEMENT_3D('',#58392,#44246,#44247);
#36456=AXIS2_PLACEMENT_3D('',#58399,#44248,#44249);
#36457=AXIS2_PLACEMENT_3D('',#58401,#44250,#44251);
#36458=AXIS2_PLACEMENT_3D('',#58406,#44252,#44253);
#36459=AXIS2_PLACEMENT_3D('',#58408,#44254,#44255);
#36460=AXIS2_PLACEMENT_3D('',#58409,#44256,#44257);
#36461=AXIS2_PLACEMENT_3D('',#58439,#44258,#44259);
#36462=AXIS2_PLACEMENT_3D('',#58440,#44260,#44261);
#36463=AXIS2_PLACEMENT_3D('',#58441,#44262,#44263);
#36464=AXIS2_PLACEMENT_3D('',#58473,#44264,#44265);
#36465=AXIS2_PLACEMENT_3D('',#58475,#44266,#44267);
#36466=AXIS2_PLACEMENT_3D('',#58476,#44268,#44269);
#36467=AXIS2_PLACEMENT_3D('',#58477,#44270,#44271);
#36468=AXIS2_PLACEMENT_3D('',#58478,#44272,#44273);
#36469=AXIS2_PLACEMENT_3D('',#58485,#44274,#44275);
#36470=AXIS2_PLACEMENT_3D('',#58487,#44276,#44277);
#36471=AXIS2_PLACEMENT_3D('',#58492,#44278,#44279);
#36472=AXIS2_PLACEMENT_3D('',#58494,#44280,#44281);
#36473=AXIS2_PLACEMENT_3D('',#58495,#44282,#44283);
#36474=AXIS2_PLACEMENT_3D('',#58523,#44284,#44285);
#36475=AXIS2_PLACEMENT_3D('',#58524,#44286,#44287);
#36476=AXIS2_PLACEMENT_3D('',#58525,#44288,#44289);
#36477=AXIS2_PLACEMENT_3D('',#58557,#44290,#44291);
#36478=AXIS2_PLACEMENT_3D('',#58559,#44292,#44293);
#36479=AXIS2_PLACEMENT_3D('',#58560,#44294,#44295);
#36480=AXIS2_PLACEMENT_3D('',#58561,#44296,#44297);
#36481=AXIS2_PLACEMENT_3D('',#58562,#44298,#44299);
#36482=AXIS2_PLACEMENT_3D('',#58569,#44300,#44301);
#36483=AXIS2_PLACEMENT_3D('',#58571,#44302,#44303);
#36484=AXIS2_PLACEMENT_3D('',#58576,#44304,#44305);
#36485=AXIS2_PLACEMENT_3D('',#58578,#44306,#44307);
#36486=AXIS2_PLACEMENT_3D('',#58579,#44308,#44309);
#36487=AXIS2_PLACEMENT_3D('',#58607,#44310,#44311);
#36488=AXIS2_PLACEMENT_3D('',#58608,#44312,#44313);
#36489=AXIS2_PLACEMENT_3D('',#58609,#44314,#44315);
#36490=AXIS2_PLACEMENT_3D('',#58645,#44316,#44317);
#36491=AXIS2_PLACEMENT_3D('',#58647,#44318,#44319);
#36492=AXIS2_PLACEMENT_3D('',#58648,#44320,#44321);
#36493=AXIS2_PLACEMENT_3D('',#58649,#44322,#44323);
#36494=AXIS2_PLACEMENT_3D('',#58650,#44324,#44325);
#36495=AXIS2_PLACEMENT_3D('',#58657,#44326,#44327);
#36496=AXIS2_PLACEMENT_3D('',#58659,#44328,#44329);
#36497=AXIS2_PLACEMENT_3D('',#58664,#44330,#44331);
#36498=AXIS2_PLACEMENT_3D('',#58666,#44332,#44333);
#36499=AXIS2_PLACEMENT_3D('',#58667,#44334,#44335);
#36500=AXIS2_PLACEMENT_3D('',#58697,#44336,#44337);
#36501=AXIS2_PLACEMENT_3D('',#58698,#44338,#44339);
#36502=AXIS2_PLACEMENT_3D('',#58699,#44340,#44341);
#36503=AXIS2_PLACEMENT_3D('',#58735,#44342,#44343);
#36504=AXIS2_PLACEMENT_3D('',#58737,#44344,#44345);
#36505=AXIS2_PLACEMENT_3D('',#58738,#44346,#44347);
#36506=AXIS2_PLACEMENT_3D('',#58739,#44348,#44349);
#36507=AXIS2_PLACEMENT_3D('',#58740,#44350,#44351);
#36508=AXIS2_PLACEMENT_3D('',#58747,#44352,#44353);
#36509=AXIS2_PLACEMENT_3D('',#58749,#44354,#44355);
#36510=AXIS2_PLACEMENT_3D('',#58754,#44356,#44357);
#36511=AXIS2_PLACEMENT_3D('',#58756,#44358,#44359);
#36512=AXIS2_PLACEMENT_3D('',#58757,#44360,#44361);
#36513=AXIS2_PLACEMENT_3D('',#58791,#44362,#44363);
#36514=AXIS2_PLACEMENT_3D('',#58792,#44364,#44365);
#36515=AXIS2_PLACEMENT_3D('',#58793,#44366,#44367);
#36516=AXIS2_PLACEMENT_3D('',#58829,#44368,#44369);
#36517=AXIS2_PLACEMENT_3D('',#58831,#44370,#44371);
#36518=AXIS2_PLACEMENT_3D('',#58832,#44372,#44373);
#36519=AXIS2_PLACEMENT_3D('',#58833,#44374,#44375);
#36520=AXIS2_PLACEMENT_3D('',#58834,#44376,#44377);
#36521=AXIS2_PLACEMENT_3D('',#58841,#44378,#44379);
#36522=AXIS2_PLACEMENT_3D('',#58843,#44380,#44381);
#36523=AXIS2_PLACEMENT_3D('',#58848,#44382,#44383);
#36524=AXIS2_PLACEMENT_3D('',#58850,#44384,#44385);
#36525=AXIS2_PLACEMENT_3D('',#58851,#44386,#44387);
#36526=AXIS2_PLACEMENT_3D('',#58885,#44388,#44389);
#36527=AXIS2_PLACEMENT_3D('',#58886,#44390,#44391);
#36528=AXIS2_PLACEMENT_3D('',#58887,#44392,#44393);
#36529=AXIS2_PLACEMENT_3D('',#58919,#44394,#44395);
#36530=AXIS2_PLACEMENT_3D('',#58921,#44396,#44397);
#36531=AXIS2_PLACEMENT_3D('',#58922,#44398,#44399);
#36532=AXIS2_PLACEMENT_3D('',#58923,#44400,#44401);
#36533=AXIS2_PLACEMENT_3D('',#58924,#44402,#44403);
#36534=AXIS2_PLACEMENT_3D('',#58931,#44404,#44405);
#36535=AXIS2_PLACEMENT_3D('',#58933,#44406,#44407);
#36536=AXIS2_PLACEMENT_3D('',#58938,#44408,#44409);
#36537=AXIS2_PLACEMENT_3D('',#58940,#44410,#44411);
#36538=AXIS2_PLACEMENT_3D('',#58941,#44412,#44413);
#36539=AXIS2_PLACEMENT_3D('',#58971,#44414,#44415);
#36540=AXIS2_PLACEMENT_3D('',#58972,#44416,#44417);
#36541=AXIS2_PLACEMENT_3D('',#58973,#44418,#44419);
#36542=AXIS2_PLACEMENT_3D('',#58993,#44420,#44421);
#36543=AXIS2_PLACEMENT_3D('',#58995,#44422,#44423);
#36544=AXIS2_PLACEMENT_3D('',#58996,#44424,#44425);
#36545=AXIS2_PLACEMENT_3D('',#58998,#44426,#44427);
#36546=AXIS2_PLACEMENT_3D('',#59015,#44428,#44429);
#36547=AXIS2_PLACEMENT_3D('',#59022,#44430,#44431);
#36548=AXIS2_PLACEMENT_3D('',#59024,#44432,#44433);
#36549=AXIS2_PLACEMENT_3D('',#59029,#44434,#44435);
#36550=AXIS2_PLACEMENT_3D('',#59031,#44436,#44437);
#36551=AXIS2_PLACEMENT_3D('',#59032,#44438,#44439);
#36552=AXIS2_PLACEMENT_3D('',#59069,#44440,#44441);
#36553=AXIS2_PLACEMENT_3D('',#59070,#44442,#44443);
#36554=AXIS2_PLACEMENT_3D('',#59071,#44444,#44445);
#36555=AXIS2_PLACEMENT_3D('',#59103,#44446,#44447);
#36556=AXIS2_PLACEMENT_3D('',#59105,#44448,#44449);
#36557=AXIS2_PLACEMENT_3D('',#59106,#44450,#44451);
#36558=AXIS2_PLACEMENT_3D('',#59107,#44452,#44453);
#36559=AXIS2_PLACEMENT_3D('',#59108,#44454,#44455);
#36560=AXIS2_PLACEMENT_3D('',#59115,#44456,#44457);
#36561=AXIS2_PLACEMENT_3D('',#59117,#44458,#44459);
#36562=AXIS2_PLACEMENT_3D('',#59122,#44460,#44461);
#36563=AXIS2_PLACEMENT_3D('',#59124,#44462,#44463);
#36564=AXIS2_PLACEMENT_3D('',#59125,#44464,#44465);
#36565=AXIS2_PLACEMENT_3D('',#59155,#44466,#44467);
#36566=AXIS2_PLACEMENT_3D('',#59156,#44468,#44469);
#36567=AXIS2_PLACEMENT_3D('',#59157,#44470,#44471);
#36568=AXIS2_PLACEMENT_3D('',#59193,#44472,#44473);
#36569=AXIS2_PLACEMENT_3D('',#59195,#44474,#44475);
#36570=AXIS2_PLACEMENT_3D('',#59196,#44476,#44477);
#36571=AXIS2_PLACEMENT_3D('',#59197,#44478,#44479);
#36572=AXIS2_PLACEMENT_3D('',#59198,#44480,#44481);
#36573=AXIS2_PLACEMENT_3D('',#59205,#44482,#44483);
#36574=AXIS2_PLACEMENT_3D('',#59207,#44484,#44485);
#36575=AXIS2_PLACEMENT_3D('',#59212,#44486,#44487);
#36576=AXIS2_PLACEMENT_3D('',#59214,#44488,#44489);
#36577=AXIS2_PLACEMENT_3D('',#59215,#44490,#44491);
#36578=AXIS2_PLACEMENT_3D('',#59249,#44492,#44493);
#36579=AXIS2_PLACEMENT_3D('',#59250,#44494,#44495);
#36580=AXIS2_PLACEMENT_3D('',#59251,#44496,#44497);
#36581=AXIS2_PLACEMENT_3D('',#59287,#44498,#44499);
#36582=AXIS2_PLACEMENT_3D('',#59289,#44500,#44501);
#36583=AXIS2_PLACEMENT_3D('',#59290,#44502,#44503);
#36584=AXIS2_PLACEMENT_3D('',#59291,#44504,#44505);
#36585=AXIS2_PLACEMENT_3D('',#59292,#44506,#44507);
#36586=AXIS2_PLACEMENT_3D('',#59299,#44508,#44509);
#36587=AXIS2_PLACEMENT_3D('',#59301,#44510,#44511);
#36588=AXIS2_PLACEMENT_3D('',#59306,#44512,#44513);
#36589=AXIS2_PLACEMENT_3D('',#59308,#44514,#44515);
#36590=AXIS2_PLACEMENT_3D('',#59309,#44516,#44517);
#36591=AXIS2_PLACEMENT_3D('',#59343,#44518,#44519);
#36592=AXIS2_PLACEMENT_3D('',#59344,#44520,#44521);
#36593=AXIS2_PLACEMENT_3D('',#59345,#44522,#44523);
#36594=AXIS2_PLACEMENT_3D('',#59381,#44524,#44525);
#36595=AXIS2_PLACEMENT_3D('',#59383,#44526,#44527);
#36596=AXIS2_PLACEMENT_3D('',#59384,#44528,#44529);
#36597=AXIS2_PLACEMENT_3D('',#59385,#44530,#44531);
#36598=AXIS2_PLACEMENT_3D('',#59386,#44532,#44533);
#36599=AXIS2_PLACEMENT_3D('',#59393,#44534,#44535);
#36600=AXIS2_PLACEMENT_3D('',#59395,#44536,#44537);
#36601=AXIS2_PLACEMENT_3D('',#59400,#44538,#44539);
#36602=AXIS2_PLACEMENT_3D('',#59402,#44540,#44541);
#36603=AXIS2_PLACEMENT_3D('',#59403,#44542,#44543);
#36604=AXIS2_PLACEMENT_3D('',#59433,#44544,#44545);
#36605=AXIS2_PLACEMENT_3D('',#59434,#44546,#44547);
#36606=AXIS2_PLACEMENT_3D('',#59435,#44548,#44549);
#36607=AXIS2_PLACEMENT_3D('',#59467,#44550,#44551);
#36608=AXIS2_PLACEMENT_3D('',#59469,#44552,#44553);
#36609=AXIS2_PLACEMENT_3D('',#59470,#44554,#44555);
#36610=AXIS2_PLACEMENT_3D('',#59471,#44556,#44557);
#36611=AXIS2_PLACEMENT_3D('',#59472,#44558,#44559);
#36612=AXIS2_PLACEMENT_3D('',#59479,#44560,#44561);
#36613=AXIS2_PLACEMENT_3D('',#59481,#44562,#44563);
#36614=AXIS2_PLACEMENT_3D('',#59486,#44564,#44565);
#36615=AXIS2_PLACEMENT_3D('',#59488,#44566,#44567);
#36616=AXIS2_PLACEMENT_3D('',#59489,#44568,#44569);
#36617=AXIS2_PLACEMENT_3D('',#59517,#44570,#44571);
#36618=AXIS2_PLACEMENT_3D('',#59518,#44572,#44573);
#36619=AXIS2_PLACEMENT_3D('',#59519,#44574,#44575);
#36620=AXIS2_PLACEMENT_3D('',#59551,#44576,#44577);
#36621=AXIS2_PLACEMENT_3D('',#59553,#44578,#44579);
#36622=AXIS2_PLACEMENT_3D('',#59554,#44580,#44581);
#36623=AXIS2_PLACEMENT_3D('',#59555,#44582,#44583);
#36624=AXIS2_PLACEMENT_3D('',#59556,#44584,#44585);
#36625=AXIS2_PLACEMENT_3D('',#59563,#44586,#44587);
#36626=AXIS2_PLACEMENT_3D('',#59565,#44588,#44589);
#36627=AXIS2_PLACEMENT_3D('',#59570,#44590,#44591);
#36628=AXIS2_PLACEMENT_3D('',#59572,#44592,#44593);
#36629=AXIS2_PLACEMENT_3D('',#59573,#44594,#44595);
#36630=AXIS2_PLACEMENT_3D('',#59601,#44596,#44597);
#36631=AXIS2_PLACEMENT_3D('',#59602,#44598,#44599);
#36632=AXIS2_PLACEMENT_3D('',#59603,#44600,#44601);
#36633=AXIS2_PLACEMENT_3D('',#59639,#44602,#44603);
#36634=AXIS2_PLACEMENT_3D('',#59641,#44604,#44605);
#36635=AXIS2_PLACEMENT_3D('',#59642,#44606,#44607);
#36636=AXIS2_PLACEMENT_3D('',#59643,#44608,#44609);
#36637=AXIS2_PLACEMENT_3D('',#59644,#44610,#44611);
#36638=AXIS2_PLACEMENT_3D('',#59651,#44612,#44613);
#36639=AXIS2_PLACEMENT_3D('',#59653,#44614,#44615);
#36640=AXIS2_PLACEMENT_3D('',#59658,#44616,#44617);
#36641=AXIS2_PLACEMENT_3D('',#59660,#44618,#44619);
#36642=AXIS2_PLACEMENT_3D('',#59661,#44620,#44621);
#36643=AXIS2_PLACEMENT_3D('',#59691,#44622,#44623);
#36644=AXIS2_PLACEMENT_3D('',#59692,#44624,#44625);
#36645=AXIS2_PLACEMENT_3D('',#59693,#44626,#44627);
#36646=AXIS2_PLACEMENT_3D('',#59729,#44628,#44629);
#36647=AXIS2_PLACEMENT_3D('',#59731,#44630,#44631);
#36648=AXIS2_PLACEMENT_3D('',#59732,#44632,#44633);
#36649=AXIS2_PLACEMENT_3D('',#59733,#44634,#44635);
#36650=AXIS2_PLACEMENT_3D('',#59734,#44636,#44637);
#36651=AXIS2_PLACEMENT_3D('',#59741,#44638,#44639);
#36652=AXIS2_PLACEMENT_3D('',#59743,#44640,#44641);
#36653=AXIS2_PLACEMENT_3D('',#59748,#44642,#44643);
#36654=AXIS2_PLACEMENT_3D('',#59750,#44644,#44645);
#36655=AXIS2_PLACEMENT_3D('',#59751,#44646,#44647);
#36656=AXIS2_PLACEMENT_3D('',#59785,#44648,#44649);
#36657=AXIS2_PLACEMENT_3D('',#59786,#44650,#44651);
#36658=AXIS2_PLACEMENT_3D('',#59787,#44652,#44653);
#36659=AXIS2_PLACEMENT_3D('',#59823,#44654,#44655);
#36660=AXIS2_PLACEMENT_3D('',#59825,#44656,#44657);
#36661=AXIS2_PLACEMENT_3D('',#59826,#44658,#44659);
#36662=AXIS2_PLACEMENT_3D('',#59827,#44660,#44661);
#36663=AXIS2_PLACEMENT_3D('',#59828,#44662,#44663);
#36664=AXIS2_PLACEMENT_3D('',#59835,#44664,#44665);
#36665=AXIS2_PLACEMENT_3D('',#59837,#44666,#44667);
#36666=AXIS2_PLACEMENT_3D('',#59842,#44668,#44669);
#36667=AXIS2_PLACEMENT_3D('',#59844,#44670,#44671);
#36668=AXIS2_PLACEMENT_3D('',#59845,#44672,#44673);
#36669=AXIS2_PLACEMENT_3D('',#59879,#44674,#44675);
#36670=AXIS2_PLACEMENT_3D('',#59880,#44676,#44677);
#36671=AXIS2_PLACEMENT_3D('',#59881,#44678,#44679);
#36672=AXIS2_PLACEMENT_3D('',#59913,#44680,#44681);
#36673=AXIS2_PLACEMENT_3D('',#59915,#44682,#44683);
#36674=AXIS2_PLACEMENT_3D('',#59916,#44684,#44685);
#36675=AXIS2_PLACEMENT_3D('',#59917,#44686,#44687);
#36676=AXIS2_PLACEMENT_3D('',#59918,#44688,#44689);
#36677=AXIS2_PLACEMENT_3D('',#59925,#44690,#44691);
#36678=AXIS2_PLACEMENT_3D('',#59927,#44692,#44693);
#36679=AXIS2_PLACEMENT_3D('',#59932,#44694,#44695);
#36680=AXIS2_PLACEMENT_3D('',#59934,#44696,#44697);
#36681=AXIS2_PLACEMENT_3D('',#59935,#44698,#44699);
#36682=AXIS2_PLACEMENT_3D('',#59965,#44700,#44701);
#36683=AXIS2_PLACEMENT_3D('',#59966,#44702,#44703);
#36684=AXIS2_PLACEMENT_3D('',#59967,#44704,#44705);
#36685=AXIS2_PLACEMENT_3D('',#59999,#44706,#44707);
#36686=AXIS2_PLACEMENT_3D('',#60001,#44708,#44709);
#36687=AXIS2_PLACEMENT_3D('',#60002,#44710,#44711);
#36688=AXIS2_PLACEMENT_3D('',#60003,#44712,#44713);
#36689=AXIS2_PLACEMENT_3D('',#60004,#44714,#44715);
#36690=AXIS2_PLACEMENT_3D('',#60011,#44716,#44717);
#36691=AXIS2_PLACEMENT_3D('',#60013,#44718,#44719);
#36692=AXIS2_PLACEMENT_3D('',#60018,#44720,#44721);
#36693=AXIS2_PLACEMENT_3D('',#60020,#44722,#44723);
#36694=AXIS2_PLACEMENT_3D('',#60021,#44724,#44725);
#36695=AXIS2_PLACEMENT_3D('',#60053,#44726,#44727);
#36696=AXIS2_PLACEMENT_3D('',#60054,#44728,#44729);
#36697=AXIS2_PLACEMENT_3D('',#60055,#44730,#44731);
#36698=AXIS2_PLACEMENT_3D('',#60058,#44733,#44734);
#36699=AXIS2_PLACEMENT_3D('',#60059,#44735,#44736);
#36700=AXIS2_PLACEMENT_3D('',#60062,#44739,#44740);
#36701=AXIS2_PLACEMENT_3D('',#60064,#44741,#44742);
#36702=AXIS2_PLACEMENT_3D('',#60066,#44744,#44745);
#36703=AXIS2_PLACEMENT_3D('',#60068,#44746,#44747);
#36704=AXIS2_PLACEMENT_3D('',#60069,#44748,#44749);
#36705=AXIS2_PLACEMENT_3D('',#60072,#44751,#44752);
#36706=AXIS2_PLACEMENT_3D('',#60073,#44753,#44754);
#36707=AXIS2_PLACEMENT_3D('',#60076,#44756,#44757);
#36708=AXIS2_PLACEMENT_3D('',#60077,#44758,#44759);
#36709=AXIS2_PLACEMENT_3D('',#60080,#44761,#44762);
#36710=AXIS2_PLACEMENT_3D('',#60081,#44763,#44764);
#44120=DIRECTION('axis',(0.,0.,1.));
#44121=DIRECTION('refdir',(1.,0.,0.));
#44122=DIRECTION('center_axis',(1.,0.,0.));
#44123=DIRECTION('ref_axis',(0.,-1.,0.));
#44124=DIRECTION('center_axis',(-1.,0.,0.));
#44125=DIRECTION('ref_axis',(0.,-1.,0.));
#44126=DIRECTION('center_axis',(-1.,0.,0.));
#44127=DIRECTION('ref_axis',(0.,-1.,0.));
#44128=DIRECTION('',(-0.707106781186549,-0.707106781186546,-8.65956056235491E-17));
#44129=DIRECTION('center_axis',(1.,0.,0.));
#44130=DIRECTION('ref_axis',(0.,-1.,0.));
#44131=DIRECTION('center_axis',(-1.,0.,0.));
#44132=DIRECTION('ref_axis',(0.,0.,1.));
#44133=DIRECTION('center_axis',(1.,0.,0.));
#44134=DIRECTION('ref_axis',(0.,0.,-1.));
#44135=DIRECTION('center_axis',(1.,0.,0.));
#44136=DIRECTION('ref_axis',(0.,1.,0.));
#44137=DIRECTION('center_axis',(1.,0.,0.));
#44138=DIRECTION('ref_axis',(0.,0.,-1.));
#44139=DIRECTION('',(-1.,0.,0.));
#44140=DIRECTION('center_axis',(-1.,0.,0.));
#44141=DIRECTION('ref_axis',(0.,-1.,0.));
#44142=DIRECTION('center_axis',(-1.,0.,0.));
#44143=DIRECTION('ref_axis',(0.,-1.,0.));
#44144=DIRECTION('',(-0.707106781186549,0.707106781186546,8.65956056235492E-17));
#44145=DIRECTION('center_axis',(1.,0.,0.));
#44146=DIRECTION('ref_axis',(0.,-1.,0.));
#44147=DIRECTION('center_axis',(1.,0.,0.));
#44148=DIRECTION('ref_axis',(0.,-1.,0.));
#44149=DIRECTION('center_axis',(1.,0.,0.));
#44150=DIRECTION('ref_axis',(0.,1.,0.));
#44151=DIRECTION('',(-1.,0.,0.));
#44152=DIRECTION('center_axis',(1.,0.,0.));
#44153=DIRECTION('ref_axis',(0.,0.,-1.));
#44154=DIRECTION('center_axis',(1.,0.,0.));
#44155=DIRECTION('ref_axis',(0.,0.,-1.));
#44156=DIRECTION('center_axis',(1.,0.,0.));
#44157=DIRECTION('ref_axis',(0.,0.,-1.));
#44158=DIRECTION('center_axis',(0.992546151641322,0.116932778696252,-0.0343345617181185));
#44159=DIRECTION('ref_axis',(0.,-0.28173255684143,-0.959492973614497));
#44160=DIRECTION('center_axis',(-0.992546151641322,-0.116932778696252,0.0343345617181191));
#44161=DIRECTION('ref_axis',(0.121869343405148,-0.952341058487958,0.279632565085031));
#44162=DIRECTION('center_axis',(0.121869343405148,-0.952341058487958,0.279632565085031));
#44163=DIRECTION('ref_axis',(0.,0.281732556841429,0.959492973614497));
#44164=DIRECTION('center_axis',(0.992546151641322,0.116932778696252,-0.0343345617181185));
#44165=DIRECTION('ref_axis',(0.121869343405148,-0.952341058487958,0.279632565085031));
#44166=DIRECTION('center_axis',(-0.992546151641322,-0.116932778696252,0.0343345617181191));
#44167=DIRECTION('ref_axis',(0.121869343405148,-0.952341058487958,0.279632565085031));
#44168=DIRECTION('center_axis',(0.992546151641322,0.116932778696252,-0.0343345617181185));
#44169=DIRECTION('ref_axis',(-0.121869343405146,0.952341058487958,-0.279632565085031));
#44170=DIRECTION('center_axis',(0.992546151641322,0.116932778696252,-0.0343345617181179));
#44171=DIRECTION('ref_axis',(0.121869343405148,-0.952341058487958,0.279632565085031));
#44172=DIRECTION('center_axis',(0.992546151641322,0.116932778696252,-0.0343345617181179));
#44173=DIRECTION('ref_axis',(0.121869343405148,-0.952341058487958,0.279632565085031));
#44174=DIRECTION('center_axis',(0.992546151641322,0.116932778696252,-0.0343345617181185));
#44175=DIRECTION('ref_axis',(0.,-0.28173255684143,-0.959492973614497));
#44176=DIRECTION('center_axis',(-0.992546151641322,-0.116932778696252,0.0343345617181185));
#44177=DIRECTION('ref_axis',(0.121869343405148,-0.952341058487958,0.279632565085031));
#44178=DIRECTION('center_axis',(0.121869343405148,-0.952341058487958,0.279632565085031));
#44179=DIRECTION('ref_axis',(0.,0.28173255684143,0.959492973614497));
#44180=DIRECTION('center_axis',(0.992546151641322,0.116932778696252,-0.0343345617181185));
#44181=DIRECTION('ref_axis',(0.,-0.28173255684143,-0.959492973614497));
#44182=DIRECTION('center_axis',(-0.992546151641322,-0.116932778696252,0.0343345617181185));
#44183=DIRECTION('ref_axis',(0.,0.28173255684143,0.959492973614497));
#44184=DIRECTION('center_axis',(0.992546151641322,0.102523015683397,-0.0658875414413361));
#44185=DIRECTION('ref_axis',(0.,-0.540640817455598,-0.841253532831181));
#44186=DIRECTION('center_axis',(-0.992546151641322,-0.102523015683397,0.0658875414413366));
#44187=DIRECTION('ref_axis',(0.121869343405148,-0.834982956566255,0.536610962785772));
#44188=DIRECTION('center_axis',(0.121869343405148,-0.834982956566256,0.536610962785772));
#44189=DIRECTION('ref_axis',(0.,0.540640817455598,0.841253532831181));
#44190=DIRECTION('center_axis',(0.992546151641322,0.102523015683397,-0.0658875414413361));
#44191=DIRECTION('ref_axis',(0.121869343405148,-0.834982956566255,0.536610962785772));
#44192=DIRECTION('center_axis',(-0.992546151641322,-0.102523015683397,0.0658875414413366));
#44193=DIRECTION('ref_axis',(0.121869343405148,-0.834982956566255,0.536610962785772));
#44194=DIRECTION('center_axis',(0.992546151641322,0.102523015683397,-0.0658875414413361));
#44195=DIRECTION('ref_axis',(-0.121869343405146,0.834982956566256,-0.536610962785772));
#44196=DIRECTION('center_axis',(0.992546151641322,0.102523015683398,-0.0658875414413355));
#44197=DIRECTION('ref_axis',(0.121869343405148,-0.834982956566256,0.536610962785772));
#44198=DIRECTION('center_axis',(0.992546151641322,0.102523015683398,-0.0658875414413355));
#44199=DIRECTION('ref_axis',(0.121869343405148,-0.834982956566256,0.536610962785772));
#44200=DIRECTION('center_axis',(0.992546151641322,0.102523015683397,-0.0658875414413361));
#44201=DIRECTION('ref_axis',(0.,-0.540640817455597,-0.841253532831181));
#44202=DIRECTION('center_axis',(-0.992546151641322,-0.102523015683397,0.0658875414413361));
#44203=DIRECTION('ref_axis',(0.121869343405148,-0.834982956566255,0.536610962785772));
#44204=DIRECTION('center_axis',(0.121869343405148,-0.834982956566256,0.536610962785772));
#44205=DIRECTION('ref_axis',(0.,0.540640817455597,0.841253532831181));
#44206=DIRECTION('center_axis',(0.992546151641322,0.102523015683397,-0.0658875414413361));
#44207=DIRECTION('ref_axis',(0.,-0.540640817455597,-0.841253532831181));
#44208=DIRECTION('center_axis',(-0.992546151641322,-0.102523015683397,0.0658875414413361));
#44209=DIRECTION('ref_axis',(0.,0.540640817455597,0.841253532831181));
#44210=DIRECTION('center_axis',(0.992546151641322,0.0798074476677251,-0.0921027044052734));
#44211=DIRECTION('ref_axis',(0.,-0.755749574354258,-0.654860733945285));
#44212=DIRECTION('center_axis',(-0.992546151641322,-0.0798074476677248,
0.0921027044052738));
#44213=DIRECTION('ref_axis',(0.121869343405148,-0.649979501338405,0.750116331629886));
#44214=DIRECTION('center_axis',(0.121869343405148,-0.649979501338405,0.750116331629886));
#44215=DIRECTION('ref_axis',(0.,0.755749574354258,0.654860733945286));
#44216=DIRECTION('center_axis',(0.992546151641322,0.0798074476677251,-0.0921027044052734));
#44217=DIRECTION('ref_axis',(0.121869343405148,-0.649979501338405,0.750116331629886));
#44218=DIRECTION('center_axis',(-0.992546151641322,-0.0798074476677248,
0.0921027044052738));
#44219=DIRECTION('ref_axis',(0.121869343405148,-0.649979501338405,0.750116331629886));
#44220=DIRECTION('center_axis',(0.992546151641322,0.0798074476677251,-0.0921027044052734));
#44221=DIRECTION('ref_axis',(-0.121869343405146,0.649979501338405,-0.750116331629886));
#44222=DIRECTION('center_axis',(0.992546151641322,0.0798074476677259,-0.092102704405273));
#44223=DIRECTION('ref_axis',(0.121869343405148,-0.649979501338404,0.750116331629886));
#44224=DIRECTION('center_axis',(0.992546151641322,0.0798074476677259,-0.092102704405273));
#44225=DIRECTION('ref_axis',(0.121869343405148,-0.649979501338404,0.750116331629886));
#44226=DIRECTION('center_axis',(0.992546151641322,0.0798074476677251,-0.0921027044052734));
#44227=DIRECTION('ref_axis',(0.,-0.755749574354258,-0.654860733945286));
#44228=DIRECTION('center_axis',(-0.992546151641322,-0.0798074476677251,
0.0921027044052734));
#44229=DIRECTION('ref_axis',(0.121869343405148,-0.649979501338405,0.750116331629886));
#44230=DIRECTION('center_axis',(0.121869343405148,-0.649979501338405,0.750116331629886));
#44231=DIRECTION('ref_axis',(0.,0.755749574354258,0.654860733945286));
#44232=DIRECTION('center_axis',(0.992546151641322,0.0798074476677251,-0.0921027044052734));
#44233=DIRECTION('ref_axis',(0.,-0.755749574354258,-0.654860733945285));
#44234=DIRECTION('center_axis',(-0.992546151641322,-0.0798074476677251,
0.0921027044052734));
#44235=DIRECTION('ref_axis',(0.,0.755749574354258,0.654860733945285));
#44236=DIRECTION('center_axis',(0.992546151641322,0.0506263548751808,-0.11085625401417));
#44237=DIRECTION('ref_axis',(0.,-0.909631995354518,-0.415415013001887));
#44238=DIRECTION('center_axis',(-0.992546151641322,-0.0506263548751804,
0.11085625401417));
#44239=DIRECTION('ref_axis',(0.121869343405148,-0.412318572489052,0.902851736398944));
#44240=DIRECTION('center_axis',(0.121869343405148,-0.412318572489052,0.902851736398944));
#44241=DIRECTION('ref_axis',(0.,0.909631995354519,0.415415013001886));
#44242=DIRECTION('center_axis',(0.992546151641322,0.0506263548751808,-0.11085625401417));
#44243=DIRECTION('ref_axis',(0.121869343405148,-0.412318572489052,0.902851736398944));
#44244=DIRECTION('center_axis',(-0.992546151641322,-0.0506263548751804,
0.11085625401417));
#44245=DIRECTION('ref_axis',(0.121869343405148,-0.412318572489052,0.902851736398944));
#44246=DIRECTION('center_axis',(0.992546151641322,0.0506263548751808,-0.11085625401417));
#44247=DIRECTION('ref_axis',(-0.121869343405146,0.412318572489052,-0.902851736398945));
#44248=DIRECTION('center_axis',(0.992546151641322,0.0506263548751816,-0.11085625401417));
#44249=DIRECTION('ref_axis',(0.121869343405148,-0.412318572489052,0.902851736398944));
#44250=DIRECTION('center_axis',(0.992546151641322,0.0506263548751816,-0.11085625401417));
#44251=DIRECTION('ref_axis',(0.121869343405148,-0.412318572489052,0.902851736398944));
#44252=DIRECTION('center_axis',(0.992546151641322,0.0506263548751808,-0.11085625401417));
#44253=DIRECTION('ref_axis',(0.,-0.909631995354518,-0.415415013001887));
#44254=DIRECTION('center_axis',(-0.992546151641322,-0.0506263548751808,
0.11085625401417));
#44255=DIRECTION('ref_axis',(0.121869343405148,-0.412318572489052,0.902851736398944));
#44256=DIRECTION('center_axis',(0.121869343405148,-0.412318572489052,0.902851736398944));
#44257=DIRECTION('ref_axis',(0.,0.909631995354519,0.415415013001886));
#44258=DIRECTION('center_axis',(0.992546151641322,0.0506263548751808,-0.11085625401417));
#44259=DIRECTION('ref_axis',(0.,-0.909631995354519,-0.415415013001886));
#44260=DIRECTION('center_axis',(-0.992546151641322,-0.0506263548751808,
0.11085625401417));
#44261=DIRECTION('ref_axis',(0.,0.909631995354519,0.415415013001886));
#44262=DIRECTION('center_axis',(0.992546151641322,0.017343815897175,-0.120628889210366));
#44263=DIRECTION('ref_axis',(0.,-0.989821441880933,-0.142314838273285));
#44264=DIRECTION('center_axis',(-0.992546151641322,-0.0173438158971745,
0.120628889210366));
#44265=DIRECTION('ref_axis',(0.121869343405148,-0.141254045049606,0.982443462950984));
#44266=DIRECTION('center_axis',(0.121869343405148,-0.141254045049607,0.982443462950984));
#44267=DIRECTION('ref_axis',(0.,0.989821441880933,0.142314838273285));
#44268=DIRECTION('center_axis',(0.992546151641322,0.017343815897175,-0.120628889210366));
#44269=DIRECTION('ref_axis',(0.121869343405148,-0.141254045049606,0.982443462950984));
#44270=DIRECTION('center_axis',(-0.992546151641322,-0.0173438158971745,
0.120628889210366));
#44271=DIRECTION('ref_axis',(0.121869343405148,-0.141254045049606,0.982443462950984));
#44272=DIRECTION('center_axis',(0.992546151641322,0.017343815897175,-0.120628889210366));
#44273=DIRECTION('ref_axis',(-0.121869343405146,0.141254045049606,-0.982443462950985));
#44274=DIRECTION('center_axis',(0.992546151641322,0.0173438158971758,-0.120628889210366));
#44275=DIRECTION('ref_axis',(0.121869343405148,-0.141254045049606,0.982443462950984));
#44276=DIRECTION('center_axis',(0.992546151641322,0.0173438158971758,-0.120628889210366));
#44277=DIRECTION('ref_axis',(0.121869343405148,-0.141254045049606,0.982443462950984));
#44278=DIRECTION('center_axis',(0.992546151641322,0.017343815897175,-0.120628889210366));
#44279=DIRECTION('ref_axis',(0.,-0.989821441880933,-0.142314838273284));
#44280=DIRECTION('center_axis',(-0.992546151641322,-0.017343815897175,0.120628889210366));
#44281=DIRECTION('ref_axis',(0.121869343405148,-0.141254045049606,0.982443462950984));
#44282=DIRECTION('center_axis',(0.121869343405148,-0.141254045049606,0.982443462950984));
#44283=DIRECTION('ref_axis',(0.,0.989821441880933,0.142314838273285));
#44284=DIRECTION('center_axis',(0.992546151641322,0.017343815897175,-0.120628889210366));
#44285=DIRECTION('ref_axis',(0.,-0.989821441880933,-0.142314838273285));
#44286=DIRECTION('center_axis',(-0.992546151641322,-0.017343815897175,0.120628889210366));
#44287=DIRECTION('ref_axis',(0.,0.989821441880933,0.142314838273285));
#44288=DIRECTION('center_axis',(0.992546151641322,-0.0173438158971751,-0.120628889210366));
#44289=DIRECTION('ref_axis',(0.,-0.989821441880933,0.142314838273285));
#44290=DIRECTION('center_axis',(-0.992546151641322,0.0173438158971756,0.120628889210366));
#44291=DIRECTION('ref_axis',(0.121869343405148,0.141254045049606,0.982443462950984));
#44292=DIRECTION('center_axis',(0.121869343405148,0.141254045049607,0.982443462950984));
#44293=DIRECTION('ref_axis',(0.,0.989821441880933,-0.142314838273285));
#44294=DIRECTION('center_axis',(0.992546151641322,-0.0173438158971751,-0.120628889210366));
#44295=DIRECTION('ref_axis',(0.121869343405148,0.141254045049606,0.982443462950984));
#44296=DIRECTION('center_axis',(-0.992546151641322,0.0173438158971756,0.120628889210366));
#44297=DIRECTION('ref_axis',(0.121869343405148,0.141254045049606,0.982443462950984));
#44298=DIRECTION('center_axis',(0.992546151641322,-0.0173438158971751,-0.120628889210366));
#44299=DIRECTION('ref_axis',(-0.121869343405146,-0.141254045049606,-0.982443462950985));
#44300=DIRECTION('center_axis',(0.992546151641322,-0.0173438158971743,-0.120628889210366));
#44301=DIRECTION('ref_axis',(0.121869343405148,0.141254045049606,0.982443462950984));
#44302=DIRECTION('center_axis',(0.992546151641322,-0.0173438158971743,-0.120628889210366));
#44303=DIRECTION('ref_axis',(0.121869343405148,0.141254045049606,0.982443462950984));
#44304=DIRECTION('center_axis',(0.992546151641322,-0.0173438158971751,-0.120628889210366));
#44305=DIRECTION('ref_axis',(0.,-0.989821441880933,0.142314838273286));
#44306=DIRECTION('center_axis',(-0.992546151641322,0.0173438158971751,0.120628889210366));
#44307=DIRECTION('ref_axis',(0.121869343405148,0.141254045049606,0.982443462950984));
#44308=DIRECTION('center_axis',(0.121869343405148,0.141254045049607,0.982443462950984));
#44309=DIRECTION('ref_axis',(0.,0.989821441880933,-0.142314838273285));
#44310=DIRECTION('center_axis',(0.992546151641322,-0.0173438158971751,-0.120628889210366));
#44311=DIRECTION('ref_axis',(0.,-0.989821441880933,0.142314838273285));
#44312=DIRECTION('center_axis',(-0.992546151641322,0.0173438158971751,0.120628889210366));
#44313=DIRECTION('ref_axis',(0.,0.989821441880933,-0.142314838273285));
#44314=DIRECTION('center_axis',(0.992546151641322,-0.0506263548751808,-0.11085625401417));
#44315=DIRECTION('ref_axis',(0.,-0.909631995354518,0.415415013001887));
#44316=DIRECTION('center_axis',(-0.992546151641322,0.0506263548751814,0.11085625401417));
#44317=DIRECTION('ref_axis',(0.121869343405148,0.412318572489052,0.902851736398944));
#44318=DIRECTION('center_axis',(0.121869343405148,0.412318572489052,0.902851736398944));
#44319=DIRECTION('ref_axis',(0.,0.909631995354519,-0.415415013001886));
#44320=DIRECTION('center_axis',(0.992546151641322,-0.0506263548751808,-0.11085625401417));
#44321=DIRECTION('ref_axis',(0.121869343405148,0.412318572489052,0.902851736398944));
#44322=DIRECTION('center_axis',(-0.992546151641322,0.0506263548751814,0.11085625401417));
#44323=DIRECTION('ref_axis',(0.121869343405148,0.412318572489052,0.902851736398944));
#44324=DIRECTION('center_axis',(0.992546151641322,-0.0506263548751808,-0.11085625401417));
#44325=DIRECTION('ref_axis',(-0.121869343405146,-0.412318572489052,-0.902851736398944));
#44326=DIRECTION('center_axis',(0.992546151641322,-0.0506263548751802,-0.11085625401417));
#44327=DIRECTION('ref_axis',(0.121869343405148,0.412318572489052,0.902851736398944));
#44328=DIRECTION('center_axis',(0.992546151641322,-0.0506263548751802,-0.11085625401417));
#44329=DIRECTION('ref_axis',(0.121869343405148,0.412318572489052,0.902851736398944));
#44330=DIRECTION('center_axis',(0.992546151641322,-0.0506263548751808,-0.11085625401417));
#44331=DIRECTION('ref_axis',(0.,-0.909631995354518,0.415415013001887));
#44332=DIRECTION('center_axis',(-0.992546151641322,0.0506263548751808,0.11085625401417));
#44333=DIRECTION('ref_axis',(0.121869343405148,0.412318572489052,0.902851736398944));
#44334=DIRECTION('center_axis',(0.121869343405148,0.412318572489052,0.902851736398944));
#44335=DIRECTION('ref_axis',(0.,0.909631995354519,-0.415415013001886));
#44336=DIRECTION('center_axis',(0.992546151641322,-0.0506263548751808,-0.11085625401417));
#44337=DIRECTION('ref_axis',(0.,-0.909631995354518,0.415415013001886));
#44338=DIRECTION('center_axis',(-0.992546151641322,0.0506263548751808,0.11085625401417));
#44339=DIRECTION('ref_axis',(0.,0.909631995354518,-0.415415013001886));
#44340=DIRECTION('center_axis',(0.992546151641322,-0.0798074476677251,-0.0921027044052734));
#44341=DIRECTION('ref_axis',(0.,-0.755749574354258,0.654860733945286));
#44342=DIRECTION('center_axis',(-0.992546151641322,0.0798074476677256,0.0921027044052731));
#44343=DIRECTION('ref_axis',(0.121869343405148,0.649979501338405,0.750116331629886));
#44344=DIRECTION('center_axis',(0.121869343405148,0.649979501338405,0.750116331629886));
#44345=DIRECTION('ref_axis',(0.,0.755749574354258,-0.654860733945286));
#44346=DIRECTION('center_axis',(0.992546151641322,-0.0798074476677251,-0.0921027044052734));
#44347=DIRECTION('ref_axis',(0.121869343405148,0.649979501338404,0.750116331629886));
#44348=DIRECTION('center_axis',(-0.992546151641322,0.0798074476677256,0.0921027044052731));
#44349=DIRECTION('ref_axis',(0.121869343405148,0.649979501338405,0.750116331629886));
#44350=DIRECTION('center_axis',(0.992546151641322,-0.0798074476677251,-0.0921027044052734));
#44351=DIRECTION('ref_axis',(-0.121869343405146,-0.649979501338405,-0.750116331629886));
#44352=DIRECTION('center_axis',(0.992546151641322,-0.0798074476677247,-0.092102704405274));
#44353=DIRECTION('ref_axis',(0.121869343405148,0.649979501338404,0.750116331629886));
#44354=DIRECTION('center_axis',(0.992546151641322,-0.0798074476677247,-0.092102704405274));
#44355=DIRECTION('ref_axis',(0.121869343405148,0.649979501338404,0.750116331629886));
#44356=DIRECTION('center_axis',(0.992546151641322,-0.0798074476677251,-0.0921027044052734));
#44357=DIRECTION('ref_axis',(0.,-0.755749574354258,0.654860733945286));
#44358=DIRECTION('center_axis',(-0.992546151641322,0.0798074476677251,0.0921027044052734));
#44359=DIRECTION('ref_axis',(0.121869343405148,0.649979501338404,0.750116331629886));
#44360=DIRECTION('center_axis',(0.121869343405148,0.649979501338404,0.750116331629886));
#44361=DIRECTION('ref_axis',(0.,0.755749574354258,-0.654860733945285));
#44362=DIRECTION('center_axis',(0.992546151641322,-0.0798074476677251,-0.0921027044052734));
#44363=DIRECTION('ref_axis',(0.,-0.755749574354258,0.654860733945285));
#44364=DIRECTION('center_axis',(-0.992546151641322,0.0798074476677251,0.0921027044052734));
#44365=DIRECTION('ref_axis',(0.,0.755749574354258,-0.654860733945285));
#44366=DIRECTION('center_axis',(0.992546151641322,-0.102523015683397,-0.0658875414413361));
#44367=DIRECTION('ref_axis',(0.,-0.540640817455598,0.841253532831181));
#44368=DIRECTION('center_axis',(-0.992546151641322,0.102523015683397,0.0658875414413357));
#44369=DIRECTION('ref_axis',(0.121869343405148,0.834982956566255,0.536610962785772));
#44370=DIRECTION('center_axis',(0.121869343405148,0.834982956566256,0.536610962785772));
#44371=DIRECTION('ref_axis',(0.,0.540640817455598,-0.841253532831181));
#44372=DIRECTION('center_axis',(0.992546151641322,-0.102523015683397,-0.0658875414413361));
#44373=DIRECTION('ref_axis',(0.121869343405148,0.834982956566256,0.536610962785772));
#44374=DIRECTION('center_axis',(-0.992546151641322,0.102523015683397,0.0658875414413357));
#44375=DIRECTION('ref_axis',(0.121869343405148,0.834982956566255,0.536610962785772));
#44376=DIRECTION('center_axis',(0.992546151641322,-0.102523015683397,-0.0658875414413361));
#44377=DIRECTION('ref_axis',(-0.121869343405146,-0.834982956566256,-0.536610962785772));
#44378=DIRECTION('center_axis',(0.992546151641322,-0.102523015683397,-0.0658875414413368));
#44379=DIRECTION('ref_axis',(0.121869343405148,0.834982956566255,0.536610962785772));
#44380=DIRECTION('center_axis',(0.992546151641322,-0.102523015683397,-0.0658875414413368));
#44381=DIRECTION('ref_axis',(0.121869343405148,0.834982956566255,0.536610962785772));
#44382=DIRECTION('center_axis',(0.992546151641322,-0.102523015683397,-0.0658875414413361));
#44383=DIRECTION('ref_axis',(0.,-0.540640817455598,0.841253532831181));
#44384=DIRECTION('center_axis',(-0.992546151641322,0.102523015683397,0.0658875414413361));
#44385=DIRECTION('ref_axis',(0.121869343405148,0.834982956566255,0.536610962785772));
#44386=DIRECTION('center_axis',(0.121869343405148,0.834982956566256,0.536610962785772));
#44387=DIRECTION('ref_axis',(0.,0.540640817455597,-0.841253532831181));
#44388=DIRECTION('center_axis',(0.992546151641322,-0.102523015683397,-0.0658875414413361));
#44389=DIRECTION('ref_axis',(0.,-0.540640817455598,0.841253532831181));
#44390=DIRECTION('center_axis',(-0.992546151641322,0.102523015683397,0.0658875414413361));
#44391=DIRECTION('ref_axis',(0.,0.540640817455598,-0.841253532831181));
#44392=DIRECTION('center_axis',(0.992546151641322,-0.116932778696252,-0.0343345617181185));
#44393=DIRECTION('ref_axis',(0.,-0.281732556841429,0.959492973614498));
#44394=DIRECTION('center_axis',(-0.992546151641322,0.116932778696252,0.034334561718118));
#44395=DIRECTION('ref_axis',(0.121869343405148,0.952341058487958,0.279632565085031));
#44396=DIRECTION('center_axis',(0.121869343405148,0.952341058487958,0.279632565085031));
#44397=DIRECTION('ref_axis',(0.,0.281732556841429,-0.959492973614497));
#44398=DIRECTION('center_axis',(0.992546151641322,-0.116932778696252,-0.0343345617181185));
#44399=DIRECTION('ref_axis',(0.121869343405148,0.952341058487958,0.279632565085031));
#44400=DIRECTION('center_axis',(-0.992546151641322,0.116932778696252,0.034334561718118));
#44401=DIRECTION('ref_axis',(0.121869343405148,0.952341058487958,0.279632565085031));
#44402=DIRECTION('center_axis',(0.992546151641322,-0.116932778696252,-0.0343345617181185));
#44403=DIRECTION('ref_axis',(-0.121869343405146,-0.952341058487958,-0.279632565085031));
#44404=DIRECTION('center_axis',(0.992546151641322,-0.116932778696252,-0.0343345617181193));
#44405=DIRECTION('ref_axis',(0.121869343405148,0.952341058487958,0.279632565085031));
#44406=DIRECTION('center_axis',(0.992546151641322,-0.116932778696252,-0.0343345617181193));
#44407=DIRECTION('ref_axis',(0.121869343405148,0.952341058487958,0.279632565085031));
#44408=DIRECTION('center_axis',(0.992546151641322,-0.116932778696252,-0.0343345617181185));
#44409=DIRECTION('ref_axis',(0.,-0.281732556841429,0.959492973614498));
#44410=DIRECTION('center_axis',(-0.992546151641322,0.116932778696252,0.0343345617181185));
#44411=DIRECTION('ref_axis',(0.121869343405148,0.952341058487958,0.279632565085031));
#44412=DIRECTION('center_axis',(0.121869343405148,0.952341058487958,0.279632565085031));
#44413=DIRECTION('ref_axis',(0.,0.28173255684143,-0.959492973614497));
#44414=DIRECTION('center_axis',(0.992546151641322,-0.116932778696252,-0.0343345617181185));
#44415=DIRECTION('ref_axis',(0.,-0.281732556841429,0.959492973614497));
#44416=DIRECTION('center_axis',(-0.992546151641322,0.116932778696252,0.0343345617181185));
#44417=DIRECTION('ref_axis',(0.,0.281732556841429,-0.959492973614497));
#44418=DIRECTION('center_axis',(0.992546151641322,-0.121869343405148,1.49246901315304E-17));
#44419=DIRECTION('ref_axis',(0.,0.,1.));
#44420=DIRECTION('center_axis',(-0.992546151641322,0.121869343405148,-5.59450180107848E-16));
#44421=DIRECTION('ref_axis',(0.121869343405148,0.992546151641322,-6.03195068039892E-17));
#44422=DIRECTION('center_axis',(0.121869343405148,0.992546151641322,0.));
#44423=DIRECTION('ref_axis',(0.,0.,-1.));
#44424=DIRECTION('center_axis',(0.992546151641322,-0.121869343405148,1.49246901315304E-17));
#44425=DIRECTION('ref_axis',(0.121869343405148,0.992546151641322,-1.21551846761357E-16));
#44426=DIRECTION('center_axis',(-0.992546151641322,0.121869343405148,-5.59450180107848E-16));
#44427=DIRECTION('ref_axis',(0.121869343405148,0.992546151641322,-6.03195068039892E-17));
#44428=DIRECTION('center_axis',(0.992546151641322,-0.121869343405148,1.49246901315304E-17));
#44429=DIRECTION('ref_axis',(-0.121869343405146,-0.992546151641322,1.21551846761357E-16));
#44430=DIRECTION('center_axis',(0.992546151641322,-0.121869343405148,-7.53073054377815E-16));
#44431=DIRECTION('ref_axis',(0.121869343405148,0.992546151641322,-6.03195068039892E-17));
#44432=DIRECTION('center_axis',(0.992546151641322,-0.121869343405148,-7.53073054377815E-16));
#44433=DIRECTION('ref_axis',(0.121869343405148,0.992546151641322,-6.03195068039892E-17));
#44434=DIRECTION('center_axis',(0.992546151641322,-0.121869343405148,1.49246901315304E-17));
#44435=DIRECTION('ref_axis',(0.,0.,1.));
#44436=DIRECTION('center_axis',(-0.992546151641322,0.121869343405148,-1.49246901315304E-17));
#44437=DIRECTION('ref_axis',(0.121869343405148,0.992546151641322,-1.21551846761357E-16));
#44438=DIRECTION('center_axis',(0.121869343405148,0.992546151641322,0.));
#44439=DIRECTION('ref_axis',(0.,0.,-1.));
#44440=DIRECTION('center_axis',(0.992546151641322,-0.121869343405148,1.49246901315304E-17));
#44441=DIRECTION('ref_axis',(0.,1.22464679914735E-16,1.));
#44442=DIRECTION('center_axis',(-0.992546151641322,0.121869343405148,-1.49246901315304E-17));
#44443=DIRECTION('ref_axis',(0.,-1.22464679914735E-16,-1.));
#44444=DIRECTION('center_axis',(0.992546151641322,-0.116932778696252,0.0343345617181185));
#44445=DIRECTION('ref_axis',(0.,0.281732556841431,0.959492973614497));
#44446=DIRECTION('center_axis',(-0.992546151641322,0.116932778696252,-0.0343345617181191));
#44447=DIRECTION('ref_axis',(0.121869343405148,0.952341058487958,-0.279632565085031));
#44448=DIRECTION('center_axis',(0.121869343405148,0.952341058487958,-0.279632565085031));
#44449=DIRECTION('ref_axis',(0.,-0.281732556841429,-0.959492973614497));
#44450=DIRECTION('center_axis',(0.992546151641322,-0.116932778696252,0.0343345617181185));
#44451=DIRECTION('ref_axis',(0.121869343405148,0.952341058487958,-0.279632565085031));
#44452=DIRECTION('center_axis',(-0.992546151641322,0.116932778696252,-0.0343345617181191));
#44453=DIRECTION('ref_axis',(0.121869343405148,0.952341058487958,-0.279632565085031));
#44454=DIRECTION('center_axis',(0.992546151641322,-0.116932778696252,0.0343345617181185));
#44455=DIRECTION('ref_axis',(-0.121869343405146,-0.952341058487958,0.279632565085031));
#44456=DIRECTION('center_axis',(0.992546151641322,-0.116932778696252,0.0343345617181179));
#44457=DIRECTION('ref_axis',(0.121869343405148,0.952341058487958,-0.279632565085031));
#44458=DIRECTION('center_axis',(0.992546151641322,-0.116932778696252,0.0343345617181179));
#44459=DIRECTION('ref_axis',(0.121869343405148,0.952341058487958,-0.279632565085031));
#44460=DIRECTION('center_axis',(0.992546151641322,-0.116932778696252,0.0343345617181185));
#44461=DIRECTION('ref_axis',(0.,0.28173255684143,0.959492973614497));
#44462=DIRECTION('center_axis',(-0.992546151641322,0.116932778696252,-0.0343345617181185));
#44463=DIRECTION('ref_axis',(0.121869343405148,0.952341058487958,-0.279632565085031));
#44464=DIRECTION('center_axis',(0.121869343405148,0.952341058487958,-0.279632565085031));
#44465=DIRECTION('ref_axis',(0.,-0.28173255684143,-0.959492973614497));
#44466=DIRECTION('center_axis',(0.992546151641322,-0.116932778696252,0.0343345617181185));
#44467=DIRECTION('ref_axis',(0.,0.28173255684143,0.959492973614497));
#44468=DIRECTION('center_axis',(-0.992546151641322,0.116932778696252,-0.0343345617181185));
#44469=DIRECTION('ref_axis',(0.,-0.28173255684143,-0.959492973614497));
#44470=DIRECTION('center_axis',(0.992546151641322,-0.102523015683397,0.0658875414413361));
#44471=DIRECTION('ref_axis',(0.,0.540640817455598,0.841253532831181));
#44472=DIRECTION('center_axis',(-0.992546151641322,0.102523015683397,-0.0658875414413366));
#44473=DIRECTION('ref_axis',(0.121869343405148,0.834982956566255,-0.536610962785772));
#44474=DIRECTION('center_axis',(0.121869343405148,0.834982956566256,-0.536610962785772));
#44475=DIRECTION('ref_axis',(0.,-0.540640817455598,-0.841253532831181));
#44476=DIRECTION('center_axis',(0.992546151641322,-0.102523015683397,0.0658875414413361));
#44477=DIRECTION('ref_axis',(0.121869343405148,0.834982956566255,-0.536610962785772));
#44478=DIRECTION('center_axis',(-0.992546151641322,0.102523015683397,-0.0658875414413366));
#44479=DIRECTION('ref_axis',(0.121869343405148,0.834982956566255,-0.536610962785772));
#44480=DIRECTION('center_axis',(0.992546151641322,-0.102523015683397,0.0658875414413361));
#44481=DIRECTION('ref_axis',(-0.121869343405146,-0.834982956566256,0.536610962785772));
#44482=DIRECTION('center_axis',(0.992546151641322,-0.102523015683398,0.0658875414413355));
#44483=DIRECTION('ref_axis',(0.121869343405148,0.834982956566255,-0.536610962785772));
#44484=DIRECTION('center_axis',(0.992546151641322,-0.102523015683398,0.0658875414413355));
#44485=DIRECTION('ref_axis',(0.121869343405148,0.834982956566255,-0.536610962785772));
#44486=DIRECTION('center_axis',(0.992546151641322,-0.102523015683397,0.0658875414413361));
#44487=DIRECTION('ref_axis',(0.,0.540640817455597,0.841253532831181));
#44488=DIRECTION('center_axis',(-0.992546151641322,0.102523015683397,-0.0658875414413361));
#44489=DIRECTION('ref_axis',(0.121869343405148,0.834982956566255,-0.536610962785772));
#44490=DIRECTION('center_axis',(0.121869343405148,0.834982956566256,-0.536610962785772));
#44491=DIRECTION('ref_axis',(0.,-0.540640817455597,-0.841253532831181));
#44492=DIRECTION('center_axis',(0.992546151641322,-0.102523015683397,0.0658875414413361));
#44493=DIRECTION('ref_axis',(0.,0.540640817455598,0.841253532831181));
#44494=DIRECTION('center_axis',(-0.992546151641322,0.102523015683397,-0.0658875414413361));
#44495=DIRECTION('ref_axis',(0.,-0.540640817455598,-0.841253532831181));
#44496=DIRECTION('center_axis',(0.992546151641322,-0.0798074476677251,0.0921027044052734));
#44497=DIRECTION('ref_axis',(0.,0.755749574354258,0.654860733945285));
#44498=DIRECTION('center_axis',(-0.992546151641322,0.0798074476677248,-0.0921027044052739));
#44499=DIRECTION('ref_axis',(0.121869343405148,0.649979501338404,-0.750116331629886));
#44500=DIRECTION('center_axis',(0.121869343405148,0.649979501338404,-0.750116331629886));
#44501=DIRECTION('ref_axis',(0.,-0.755749574354258,-0.654860733945285));
#44502=DIRECTION('center_axis',(0.992546151641322,-0.0798074476677251,0.0921027044052734));
#44503=DIRECTION('ref_axis',(0.121869343405148,0.649979501338404,-0.750116331629886));
#44504=DIRECTION('center_axis',(-0.992546151641322,0.0798074476677248,-0.0921027044052739));
#44505=DIRECTION('ref_axis',(0.121869343405148,0.649979501338404,-0.750116331629886));
#44506=DIRECTION('center_axis',(0.992546151641322,-0.0798074476677251,0.0921027044052734));
#44507=DIRECTION('ref_axis',(-0.121869343405146,-0.649979501338404,0.750116331629886));
#44508=DIRECTION('center_axis',(0.992546151641322,-0.0798074476677258,0.0921027044052731));
#44509=DIRECTION('ref_axis',(0.121869343405148,0.649979501338404,-0.750116331629886));
#44510=DIRECTION('center_axis',(0.992546151641322,-0.0798074476677258,0.0921027044052731));
#44511=DIRECTION('ref_axis',(0.121869343405148,0.649979501338404,-0.750116331629886));
#44512=DIRECTION('center_axis',(0.992546151641322,-0.0798074476677251,0.0921027044052734));
#44513=DIRECTION('ref_axis',(0.,0.755749574354258,0.654860733945285));
#44514=DIRECTION('center_axis',(-0.992546151641322,0.0798074476677251,-0.0921027044052734));
#44515=DIRECTION('ref_axis',(0.121869343405148,0.649979501338404,-0.750116331629886));
#44516=DIRECTION('center_axis',(0.121869343405148,0.649979501338404,-0.750116331629886));
#44517=DIRECTION('ref_axis',(0.,-0.755749574354258,-0.654860733945285));
#44518=DIRECTION('center_axis',(0.992546151641322,-0.0798074476677251,0.0921027044052734));
#44519=DIRECTION('ref_axis',(0.,0.755749574354258,0.654860733945285));
#44520=DIRECTION('center_axis',(-0.992546151641322,0.0798074476677251,-0.0921027044052734));
#44521=DIRECTION('ref_axis',(0.,-0.755749574354258,-0.654860733945285));
#44522=DIRECTION('center_axis',(0.992546151641322,-0.0506263548751808,0.11085625401417));
#44523=DIRECTION('ref_axis',(0.,0.909631995354518,0.415415013001887));
#44524=DIRECTION('center_axis',(-0.992546151641322,0.0506263548751804,-0.11085625401417));
#44525=DIRECTION('ref_axis',(0.121869343405148,0.412318572489052,-0.902851736398944));
#44526=DIRECTION('center_axis',(0.121869343405148,0.412318572489051,-0.902851736398945));
#44527=DIRECTION('ref_axis',(0.,-0.909631995354519,-0.415415013001886));
#44528=DIRECTION('center_axis',(0.992546151641322,-0.0506263548751808,0.11085625401417));
#44529=DIRECTION('ref_axis',(0.121869343405148,0.412318572489052,-0.902851736398944));
#44530=DIRECTION('center_axis',(-0.992546151641322,0.0506263548751804,-0.11085625401417));
#44531=DIRECTION('ref_axis',(0.121869343405148,0.412318572489052,-0.902851736398944));
#44532=DIRECTION('center_axis',(0.992546151641322,-0.0506263548751808,0.11085625401417));
#44533=DIRECTION('ref_axis',(-0.121869343405146,-0.412318572489052,0.902851736398944));
#44534=DIRECTION('center_axis',(0.992546151641322,-0.0506263548751816,0.11085625401417));
#44535=DIRECTION('ref_axis',(0.121869343405148,0.412318572489052,-0.902851736398944));
#44536=DIRECTION('center_axis',(0.992546151641322,-0.0506263548751816,0.11085625401417));
#44537=DIRECTION('ref_axis',(0.121869343405148,0.412318572489052,-0.902851736398944));
#44538=DIRECTION('center_axis',(0.992546151641322,-0.0506263548751808,0.11085625401417));
#44539=DIRECTION('ref_axis',(0.,0.909631995354518,0.415415013001887));
#44540=DIRECTION('center_axis',(-0.992546151641322,0.0506263548751808,-0.11085625401417));
#44541=DIRECTION('ref_axis',(0.121869343405148,0.412318572489052,-0.902851736398944));
#44542=DIRECTION('center_axis',(0.121869343405148,0.412318572489052,-0.902851736398944));
#44543=DIRECTION('ref_axis',(0.,-0.909631995354519,-0.415415013001886));
#44544=DIRECTION('center_axis',(0.992546151641322,-0.0506263548751808,0.11085625401417));
#44545=DIRECTION('ref_axis',(0.,0.909631995354519,0.415415013001886));
#44546=DIRECTION('center_axis',(-0.992546151641322,0.0506263548751808,-0.11085625401417));
#44547=DIRECTION('ref_axis',(0.,-0.909631995354519,-0.415415013001886));
#44548=DIRECTION('center_axis',(0.992546151641322,-0.017343815897175,0.120628889210366));
#44549=DIRECTION('ref_axis',(0.,0.989821441880933,0.142314838273285));
#44550=DIRECTION('center_axis',(-0.992546151641322,0.0173438158971745,-0.120628889210366));
#44551=DIRECTION('ref_axis',(0.121869343405148,0.141254045049606,-0.982443462950984));
#44552=DIRECTION('center_axis',(0.121869343405148,0.141254045049607,-0.982443462950984));
#44553=DIRECTION('ref_axis',(0.,-0.989821441880933,-0.142314838273285));
#44554=DIRECTION('center_axis',(0.992546151641322,-0.017343815897175,0.120628889210366));
#44555=DIRECTION('ref_axis',(0.121869343405148,0.141254045049606,-0.982443462950984));
#44556=DIRECTION('center_axis',(-0.992546151641322,0.0173438158971745,-0.120628889210366));
#44557=DIRECTION('ref_axis',(0.121869343405148,0.141254045049606,-0.982443462950984));
#44558=DIRECTION('center_axis',(0.992546151641322,-0.017343815897175,0.120628889210366));
#44559=DIRECTION('ref_axis',(-0.121869343405146,-0.141254045049606,0.982443462950985));
#44560=DIRECTION('center_axis',(0.992546151641322,-0.0173438158971758,0.120628889210366));
#44561=DIRECTION('ref_axis',(0.121869343405148,0.141254045049606,-0.982443462950984));
#44562=DIRECTION('center_axis',(0.992546151641322,-0.0173438158971758,0.120628889210366));
#44563=DIRECTION('ref_axis',(0.121869343405148,0.141254045049606,-0.982443462950984));
#44564=DIRECTION('center_axis',(0.992546151641322,-0.017343815897175,0.120628889210366));
#44565=DIRECTION('ref_axis',(0.,0.989821441880933,0.142314838273284));
#44566=DIRECTION('center_axis',(-0.992546151641322,0.017343815897175,-0.120628889210366));
#44567=DIRECTION('ref_axis',(0.121869343405148,0.141254045049606,-0.982443462950984));
#44568=DIRECTION('center_axis',(0.121869343405148,0.141254045049606,-0.982443462950984));
#44569=DIRECTION('ref_axis',(0.,-0.989821441880933,-0.142314838273285));
#44570=DIRECTION('center_axis',(0.992546151641322,-0.017343815897175,0.120628889210366));
#44571=DIRECTION('ref_axis',(0.,0.989821441880933,0.142314838273285));
#44572=DIRECTION('center_axis',(-0.992546151641322,0.017343815897175,-0.120628889210366));
#44573=DIRECTION('ref_axis',(0.,-0.989821441880933,-0.142314838273285));
#44574=DIRECTION('center_axis',(0.992546151641322,0.0173438158971751,0.120628889210366));
#44575=DIRECTION('ref_axis',(0.,0.989821441880933,-0.142314838273285));
#44576=DIRECTION('center_axis',(-0.992546151641322,-0.0173438158971756,
-0.120628889210366));
#44577=DIRECTION('ref_axis',(0.121869343405148,-0.141254045049606,-0.982443462950984));
#44578=DIRECTION('center_axis',(0.121869343405148,-0.141254045049607,-0.982443462950984));
#44579=DIRECTION('ref_axis',(0.,-0.989821441880933,0.142314838273285));
#44580=DIRECTION('center_axis',(0.992546151641322,0.0173438158971751,0.120628889210366));
#44581=DIRECTION('ref_axis',(0.121869343405148,-0.141254045049606,-0.982443462950984));
#44582=DIRECTION('center_axis',(-0.992546151641322,-0.0173438158971756,
-0.120628889210366));
#44583=DIRECTION('ref_axis',(0.121869343405148,-0.141254045049606,-0.982443462950984));
#44584=DIRECTION('center_axis',(0.992546151641322,0.0173438158971751,0.120628889210366));
#44585=DIRECTION('ref_axis',(-0.121869343405146,0.141254045049606,0.982443462950985));
#44586=DIRECTION('center_axis',(0.992546151641322,0.0173438158971743,0.120628889210366));
#44587=DIRECTION('ref_axis',(0.121869343405148,-0.141254045049606,-0.982443462950984));
#44588=DIRECTION('center_axis',(0.992546151641322,0.0173438158971743,0.120628889210366));
#44589=DIRECTION('ref_axis',(0.121869343405148,-0.141254045049606,-0.982443462950984));
#44590=DIRECTION('center_axis',(0.992546151641322,0.0173438158971751,0.120628889210366));
#44591=DIRECTION('ref_axis',(0.,0.989821441880933,-0.142314838273284));
#44592=DIRECTION('center_axis',(-0.992546151641322,-0.0173438158971751,
-0.120628889210366));
#44593=DIRECTION('ref_axis',(0.121869343405148,-0.141254045049606,-0.982443462950984));
#44594=DIRECTION('center_axis',(0.121869343405148,-0.141254045049606,-0.982443462950984));
#44595=DIRECTION('ref_axis',(0.,-0.989821441880933,0.142314838273285));
#44596=DIRECTION('center_axis',(0.992546151641322,0.0173438158971751,0.120628889210366));
#44597=DIRECTION('ref_axis',(0.,0.989821441880933,-0.142314838273285));
#44598=DIRECTION('center_axis',(-0.992546151641322,-0.0173438158971751,
-0.120628889210366));
#44599=DIRECTION('ref_axis',(0.,-0.989821441880933,0.142314838273285));
#44600=DIRECTION('center_axis',(0.992546151641322,0.0506263548751809,0.11085625401417));
#44601=DIRECTION('ref_axis',(0.,0.909631995354518,-0.415415013001887));
#44602=DIRECTION('center_axis',(-0.992546151641322,-0.0506263548751814,
-0.11085625401417));
#44603=DIRECTION('ref_axis',(0.121869343405148,-0.412318572489052,-0.902851736398944));
#44604=DIRECTION('center_axis',(0.121869343405148,-0.412318572489052,-0.902851736398944));
#44605=DIRECTION('ref_axis',(0.,-0.909631995354519,0.415415013001886));
#44606=DIRECTION('center_axis',(0.992546151641322,0.0506263548751809,0.11085625401417));
#44607=DIRECTION('ref_axis',(0.121869343405148,-0.412318572489052,-0.902851736398944));
#44608=DIRECTION('center_axis',(-0.992546151641322,-0.0506263548751814,
-0.11085625401417));
#44609=DIRECTION('ref_axis',(0.121869343405148,-0.412318572489052,-0.902851736398944));
#44610=DIRECTION('center_axis',(0.992546151641322,0.0506263548751809,0.11085625401417));
#44611=DIRECTION('ref_axis',(-0.121869343405146,0.412318572489052,0.902851736398944));
#44612=DIRECTION('center_axis',(0.992546151641322,0.0506263548751802,0.11085625401417));
#44613=DIRECTION('ref_axis',(0.121869343405148,-0.412318572489052,-0.902851736398944));
#44614=DIRECTION('center_axis',(0.992546151641322,0.0506263548751802,0.11085625401417));
#44615=DIRECTION('ref_axis',(0.121869343405148,-0.412318572489052,-0.902851736398944));
#44616=DIRECTION('center_axis',(0.992546151641322,0.0506263548751809,0.11085625401417));
#44617=DIRECTION('ref_axis',(0.,0.909631995354518,-0.415415013001887));
#44618=DIRECTION('center_axis',(-0.992546151641322,-0.0506263548751809,
-0.11085625401417));
#44619=DIRECTION('ref_axis',(0.121869343405148,-0.412318572489052,-0.902851736398944));
#44620=DIRECTION('center_axis',(0.121869343405148,-0.412318572489052,-0.902851736398944));
#44621=DIRECTION('ref_axis',(0.,-0.909631995354519,0.415415013001886));
#44622=DIRECTION('center_axis',(0.992546151641322,0.0506263548751809,0.11085625401417));
#44623=DIRECTION('ref_axis',(0.,0.909631995354518,-0.415415013001886));
#44624=DIRECTION('center_axis',(-0.992546151641322,-0.0506263548751809,
-0.11085625401417));
#44625=DIRECTION('ref_axis',(0.,-0.909631995354518,0.415415013001886));
#44626=DIRECTION('center_axis',(0.992546151641322,0.0798074476677251,0.0921027044052734));
#44627=DIRECTION('ref_axis',(0.,0.755749574354258,-0.654860733945286));
#44628=DIRECTION('center_axis',(-0.992546151641322,-0.0798074476677256,
-0.0921027044052731));
#44629=DIRECTION('ref_axis',(0.121869343405148,-0.649979501338404,-0.750116331629886));
#44630=DIRECTION('center_axis',(0.121869343405148,-0.649979501338404,-0.750116331629887));
#44631=DIRECTION('ref_axis',(0.,-0.755749574354259,0.654860733945285));
#44632=DIRECTION('center_axis',(0.992546151641322,0.0798074476677251,0.0921027044052734));
#44633=DIRECTION('ref_axis',(0.121869343405148,-0.649979501338404,-0.750116331629886));
#44634=DIRECTION('center_axis',(-0.992546151641322,-0.0798074476677256,
-0.0921027044052731));
#44635=DIRECTION('ref_axis',(0.121869343405148,-0.649979501338404,-0.750116331629886));
#44636=DIRECTION('center_axis',(0.992546151641322,0.0798074476677251,0.0921027044052734));
#44637=DIRECTION('ref_axis',(-0.121869343405146,0.649979501338405,0.750116331629886));
#44638=DIRECTION('center_axis',(0.992546151641322,0.0798074476677247,0.0921027044052741));
#44639=DIRECTION('ref_axis',(0.121869343405148,-0.649979501338404,-0.750116331629886));
#44640=DIRECTION('center_axis',(0.992546151641322,0.0798074476677247,0.0921027044052741));
#44641=DIRECTION('ref_axis',(0.121869343405148,-0.649979501338404,-0.750116331629886));
#44642=DIRECTION('center_axis',(0.992546151641322,0.0798074476677251,0.0921027044052734));
#44643=DIRECTION('ref_axis',(0.,0.755749574354258,-0.654860733945286));
#44644=DIRECTION('center_axis',(-0.992546151641322,-0.0798074476677251,
-0.0921027044052734));
#44645=DIRECTION('ref_axis',(0.121869343405148,-0.649979501338404,-0.750116331629886));
#44646=DIRECTION('center_axis',(0.121869343405148,-0.649979501338405,-0.750116331629886));
#44647=DIRECTION('ref_axis',(0.,-0.755749574354258,0.654860733945286));
#44648=DIRECTION('center_axis',(0.992546151641322,0.0798074476677251,0.0921027044052734));
#44649=DIRECTION('ref_axis',(0.,0.755749574354258,-0.654860733945285));
#44650=DIRECTION('center_axis',(-0.992546151641322,-0.0798074476677251,
-0.0921027044052734));
#44651=DIRECTION('ref_axis',(0.,-0.755749574354258,0.654860733945285));
#44652=DIRECTION('center_axis',(0.992546151641322,0.102523015683397,0.0658875414413361));
#44653=DIRECTION('ref_axis',(0.,0.540640817455598,-0.841253532831181));
#44654=DIRECTION('center_axis',(-0.992546151641322,-0.102523015683397,-0.0658875414413357));
#44655=DIRECTION('ref_axis',(0.121869343405148,-0.834982956566255,-0.536610962785772));
#44656=DIRECTION('center_axis',(0.121869343405148,-0.834982956566256,-0.536610962785772));
#44657=DIRECTION('ref_axis',(0.,-0.540640817455598,0.841253532831181));
#44658=DIRECTION('center_axis',(0.992546151641322,0.102523015683397,0.0658875414413361));
#44659=DIRECTION('ref_axis',(0.121869343405148,-0.834982956566256,-0.536610962785772));
#44660=DIRECTION('center_axis',(-0.992546151641322,-0.102523015683397,-0.0658875414413357));
#44661=DIRECTION('ref_axis',(0.121869343405148,-0.834982956566255,-0.536610962785772));
#44662=DIRECTION('center_axis',(0.992546151641322,0.102523015683397,0.0658875414413361));
#44663=DIRECTION('ref_axis',(-0.121869343405146,0.834982956566256,0.536610962785772));
#44664=DIRECTION('center_axis',(0.992546151641322,0.102523015683397,0.0658875414413368));
#44665=DIRECTION('ref_axis',(0.121869343405148,-0.834982956566255,-0.536610962785772));
#44666=DIRECTION('center_axis',(0.992546151641322,0.102523015683397,0.0658875414413368));
#44667=DIRECTION('ref_axis',(0.121869343405148,-0.834982956566255,-0.536610962785772));
#44668=DIRECTION('center_axis',(0.992546151641322,0.102523015683397,0.0658875414413361));
#44669=DIRECTION('ref_axis',(0.,0.540640817455598,-0.841253532831181));
#44670=DIRECTION('center_axis',(-0.992546151641322,-0.102523015683397,-0.0658875414413361));
#44671=DIRECTION('ref_axis',(0.121869343405148,-0.834982956566255,-0.536610962785772));
#44672=DIRECTION('center_axis',(0.121869343405148,-0.834982956566256,-0.536610962785772));
#44673=DIRECTION('ref_axis',(0.,-0.540640817455597,0.841253532831181));
#44674=DIRECTION('center_axis',(0.992546151641322,0.102523015683397,0.0658875414413361));
#44675=DIRECTION('ref_axis',(0.,0.540640817455598,-0.841253532831181));
#44676=DIRECTION('center_axis',(-0.992546151641322,-0.102523015683397,-0.0658875414413361));
#44677=DIRECTION('ref_axis',(0.,-0.540640817455598,0.841253532831181));
#44678=DIRECTION('center_axis',(0.992546151641322,0.116932778696252,0.0343345617181185));
#44679=DIRECTION('ref_axis',(0.,0.281732556841431,-0.959492973614497));
#44680=DIRECTION('center_axis',(-0.992546151641322,-0.116932778696252,-0.034334561718118));
#44681=DIRECTION('ref_axis',(0.121869343405148,-0.952341058487958,-0.279632565085031));
#44682=DIRECTION('center_axis',(0.121869343405148,-0.952341058487958,-0.279632565085031));
#44683=DIRECTION('ref_axis',(0.,-0.281732556841429,0.959492973614497));
#44684=DIRECTION('center_axis',(0.992546151641322,0.116932778696252,0.0343345617181185));
#44685=DIRECTION('ref_axis',(0.121869343405148,-0.952341058487958,-0.279632565085031));
#44686=DIRECTION('center_axis',(-0.992546151641322,-0.116932778696252,-0.034334561718118));
#44687=DIRECTION('ref_axis',(0.121869343405148,-0.952341058487958,-0.279632565085031));
#44688=DIRECTION('center_axis',(0.992546151641322,0.116932778696252,0.0343345617181185));
#44689=DIRECTION('ref_axis',(-0.121869343405146,0.952341058487958,0.279632565085031));
#44690=DIRECTION('center_axis',(0.992546151641322,0.116932778696252,0.0343345617181193));
#44691=DIRECTION('ref_axis',(0.121869343405148,-0.952341058487958,-0.279632565085031));
#44692=DIRECTION('center_axis',(0.992546151641322,0.116932778696252,0.0343345617181193));
#44693=DIRECTION('ref_axis',(0.121869343405148,-0.952341058487958,-0.279632565085031));
#44694=DIRECTION('center_axis',(0.992546151641322,0.116932778696252,0.0343345617181185));
#44695=DIRECTION('ref_axis',(0.,0.28173255684143,-0.959492973614497));
#44696=DIRECTION('center_axis',(-0.992546151641322,-0.116932778696252,-0.0343345617181185));
#44697=DIRECTION('ref_axis',(0.121869343405148,-0.952341058487958,-0.279632565085031));
#44698=DIRECTION('center_axis',(0.121869343405148,-0.952341058487958,-0.279632565085031));
#44699=DIRECTION('ref_axis',(0.,-0.28173255684143,0.959492973614497));
#44700=DIRECTION('center_axis',(0.992546151641322,0.116932778696252,0.0343345617181185));
#44701=DIRECTION('ref_axis',(0.,0.28173255684143,-0.959492973614497));
#44702=DIRECTION('center_axis',(-0.992546151641322,-0.116932778696252,-0.0343345617181185));
#44703=DIRECTION('ref_axis',(0.,-0.28173255684143,0.959492973614497));
#44704=DIRECTION('center_axis',(0.992546151641322,0.121869343405148,0.));
#44705=DIRECTION('ref_axis',(0.,0.,-1.));
#44706=DIRECTION('center_axis',(-0.992546151641322,-0.121869343405148,5.44525489976318E-16));
#44707=DIRECTION('ref_axis',(0.121869343405148,-0.992546151641322,-6.12323399573676E-17));
#44708=DIRECTION('center_axis',(0.121869343405148,-0.992546151641322,0.));
#44709=DIRECTION('ref_axis',(0.,0.,1.));
#44710=DIRECTION('center_axis',(0.992546151641322,0.121869343405148,0.));
#44711=DIRECTION('ref_axis',(0.121869343405148,-0.992546151641322,0.));
#44712=DIRECTION('center_axis',(-0.992546151641322,-0.121869343405148,5.44525489976318E-16));
#44713=DIRECTION('ref_axis',(0.121869343405148,-0.992546151641322,-6.12323399573676E-17));
#44714=DIRECTION('center_axis',(0.992546151641322,0.121869343405148,0.));
#44715=DIRECTION('ref_axis',(-0.121869343405146,0.992546151641322,0.));
#44716=DIRECTION('center_axis',(0.992546151641322,0.121869343405148,7.67997744509345E-16));
#44717=DIRECTION('ref_axis',(0.121869343405148,-0.992546151641322,-6.12323399573676E-17));
#44718=DIRECTION('center_axis',(0.992546151641322,0.121869343405148,7.67997744509345E-16));
#44719=DIRECTION('ref_axis',(0.121869343405148,-0.992546151641322,-6.12323399573676E-17));
#44720=DIRECTION('center_axis',(0.992546151641322,0.121869343405148,0.));
#44721=DIRECTION('ref_axis',(0.,0.,-1.));
#44722=DIRECTION('center_axis',(-0.992546151641322,-0.121869343405148,0.));
#44723=DIRECTION('ref_axis',(0.121869343405148,-0.992546151641322,0.));
#44724=DIRECTION('center_axis',(0.121869343405148,-0.992546151641322,0.));
#44725=DIRECTION('ref_axis',(0.,0.,1.));
#44726=DIRECTION('center_axis',(0.992546151641322,0.121869343405148,0.));
#44727=DIRECTION('ref_axis',(0.,0.,-1.));
#44728=DIRECTION('center_axis',(-0.992546151641322,-0.121869343405148,0.));
#44729=DIRECTION('ref_axis',(0.,0.,1.));
#44730=DIRECTION('center_axis',(1.,0.,0.));
#44731=DIRECTION('ref_axis',(0.,1.,0.));
#44732=DIRECTION('',(-0.707106781186551,0.707106781186544,8.65956056235489E-17));
#44733=DIRECTION('center_axis',(1.,0.,0.));
#44734=DIRECTION('ref_axis',(0.,0.,-1.));
#44735=DIRECTION('center_axis',(1.,0.,0.));
#44736=DIRECTION('ref_axis',(0.,1.,0.));
#44737=DIRECTION('',(-0.996194698091746,0.0871557427476584,1.0673500138323E-17));
#44738=DIRECTION('',(-0.996194698091746,0.0871557427476584,1.0673500138323E-17));
#44739=DIRECTION('center_axis',(-1.,0.,0.));
#44740=DIRECTION('ref_axis',(0.,1.,0.));
#44741=DIRECTION('center_axis',(1.,0.,0.));
#44742=DIRECTION('ref_axis',(0.,0.,-1.));
#44743=DIRECTION('',(-0.707106781186547,-0.707106781186547,-8.65956056235493E-17));
#44744=DIRECTION('center_axis',(1.,0.,0.));
#44745=DIRECTION('ref_axis',(0.,0.,-1.));
#44746=DIRECTION('center_axis',(1.,0.,0.));
#44747=DIRECTION('ref_axis',(0.,0.,-1.));
#44748=DIRECTION('center_axis',(1.,0.,0.));
#44749=DIRECTION('ref_axis',(0.,1.,0.));
#44750=DIRECTION('',(-0.707106781186547,0.707106781186547,8.65956056235493E-17));
#44751=DIRECTION('center_axis',(1.,0.,0.));
#44752=DIRECTION('ref_axis',(0.,0.,-1.));
#44753=DIRECTION('center_axis',(1.,0.,0.));
#44754=DIRECTION('ref_axis',(0.,1.,0.));
#44755=DIRECTION('',(-1.,0.,0.));
#44756=DIRECTION('center_axis',(1.,0.,0.));
#44757=DIRECTION('ref_axis',(0.,0.,-1.));
#44758=DIRECTION('center_axis',(-1.,0.,0.));
#44759=DIRECTION('ref_axis',(0.,1.,0.));
#44760=DIRECTION('',(-0.707106781186547,-0.707106781186548,-8.65956056235494E-17));
#44761=DIRECTION('center_axis',(1.,0.,0.));
#44762=DIRECTION('ref_axis',(0.,0.,-1.));
#44763=DIRECTION('center_axis',(-1.,0.,0.));
#44764=DIRECTION('ref_axis',(0.,0.,1.));
#58046=CARTESIAN_POINT('',(0.,0.,0.));
#58047=CARTESIAN_POINT('Origin',(12.3795635938087,0.,0.));
#58048=CARTESIAN_POINT('',(12.6295635938087,25.8846416389917,-3.16995435302675E-15));
#58049=CARTESIAN_POINT('',(12.6295635938087,-25.8846416389917,-3.16995435302675E-15));
#58050=CARTESIAN_POINT('Origin',(12.6295635938087,0.,0.));
#58051=CARTESIAN_POINT('Origin',(12.6295635938087,0.,0.));
#58052=CARTESIAN_POINT('',(12.1295635938087,25.3846416389917,3.10872201306938E-15));
#58053=CARTESIAN_POINT('',(12.3795635938087,25.6346416389917,3.13933818304807E-15));
#58054=CARTESIAN_POINT('Origin',(12.1295635938087,0.,0.));
#58055=CARTESIAN_POINT('Origin',(12.1295635938087,25.8846416389917,0.));
#58056=CARTESIAN_POINT('',(12.1295635938087,-22.4888907487754,-2.75409480718623E-15));
#58057=CARTESIAN_POINT('Origin',(12.1295635938087,0.,0.));
#58058=CARTESIAN_POINT('Origin',(13.7522817969044,0.,0.));
#58059=CARTESIAN_POINT('',(15.375,-25.8846416389917,-3.16995435302675E-15));
#58060=CARTESIAN_POINT('Origin',(15.375,0.,0.));
#58061=CARTESIAN_POINT('',(13.7522817969044,-25.8846416389917,-3.16995435302675E-15));
#58062=CARTESIAN_POINT('Origin',(0.967576169359906,0.,0.));
#58063=CARTESIAN_POINT('',(1.21757616935991,22.2743990607509,-2.72782715126794E-15));
#58064=CARTESIAN_POINT('Origin',(1.21757616935991,0.,0.));
#58065=CARTESIAN_POINT('',(0.717576169359905,22.7743990607509,2.7890594912253E-15));
#58066=CARTESIAN_POINT('',(0.967576169359906,22.5243990607509,2.75844332124662E-15));
#58067=CARTESIAN_POINT('',(0.717576169359905,-22.7743990607509,-2.7890594912253E-15));
#58068=CARTESIAN_POINT('Origin',(0.717576169359905,0.,0.));
#58069=CARTESIAN_POINT('Origin',(0.717576169359905,0.,0.));
#58070=CARTESIAN_POINT('Origin',(0.364288084679953,0.,0.));
#58071=CARTESIAN_POINT('',(-0.488999999999999,-22.7743990607509,-2.7890594912253E-15));
#58072=CARTESIAN_POINT('',(0.364288084679953,-22.7743990607509,-2.7890594912253E-15));
#58073=CARTESIAN_POINT('Origin',(-0.488999999999999,0.,0.));
#58074=CARTESIAN_POINT('Origin',(1.21757616935991,21.5342155525986,0.));
#58075=CARTESIAN_POINT('',(1.2175761693599,-21.5342155525986,-2.63718081486391E-15));
#58076=CARTESIAN_POINT('Origin',(1.21757616935991,0.,0.));
#58077=CARTESIAN_POINT('Origin',(1.6653400148523,23.0866647604201,-6.77885640724594));
#58078=CARTESIAN_POINT('',(1.95776807072638,20.8526247727479,-5.62882899907203));
#58079=CARTESIAN_POINT('',(1.95776807072638,20.5855189702533,-6.53850782206135));
#58080=CARTESIAN_POINT('Ctrl Pts',(1.95776807072638,20.8526247727479,-5.62882899907201));
#58081=CARTESIAN_POINT('Ctrl Pts',(1.95134808310818,20.8520805812057,-5.62868975053389));
#58082=CARTESIAN_POINT('Ctrl Pts',(1.94501708164843,20.8512847270698,-5.62951292444653));
#58083=CARTESIAN_POINT('Ctrl Pts',(1.9295422670367,20.8487299346928,-5.63377986718356));
#58084=CARTESIAN_POINT('Ctrl Pts',(1.92098940734527,20.8467620801163,-5.63819408082448));
#58085=CARTESIAN_POINT('Ctrl Pts',(1.90083817144694,20.8410870108713,-5.65240862845873));
#58086=CARTESIAN_POINT('Ctrl Pts',(1.89018614013566,20.8369650214857,-5.6640399065301));
#58087=CARTESIAN_POINT('Ctrl Pts',(1.86077829278501,20.8234001483396,-5.70403903582823));
#58088=CARTESIAN_POINT('Ctrl Pts',(1.84665745875297,20.8126796100669,-5.73837519874369));
#58089=CARTESIAN_POINT('Ctrl Pts',(1.82247517384126,20.7910284502552,-5.80859546078155));
#58090=CARTESIAN_POINT('Ctrl Pts',(1.81230887642825,20.776390275316,-5.85747914655454));
#58091=CARTESIAN_POINT('Ctrl Pts',(1.79934881945703,20.7493484902442,-5.94843125987379));
#58092=CARTESIAN_POINT('Ctrl Pts',(1.79572382774354,20.7358065149718,-5.99432875769191));
#58093=CARTESIAN_POINT('Ctrl Pts',(1.79301769946662,20.7096735628667,-6.08315330650854));
#58094=CARTESIAN_POINT('Ctrl Pts',(1.79378222861462,20.696526800513,-6.12796795345379));
#58095=CARTESIAN_POINT('Ctrl Pts',(1.79982187672896,20.6703299712419,-6.2176096395351));
#58096=CARTESIAN_POINT('Ctrl Pts',(1.80545072973348,20.6566260406507,-6.26467818891722));
#58097=CARTESIAN_POINT('Ctrl Pts',(1.82510992022638,20.6280881697227,-6.3639304020438));
#58098=CARTESIAN_POINT('Ctrl Pts',(1.83960979647508,20.6150406765473,-6.4102079966474));
#58099=CARTESIAN_POINT('Ctrl Pts',(1.86695154341759,20.5997934931305,-6.4669505500946));
#58100=CARTESIAN_POINT('Ctrl Pts',(1.88252298601333,20.5925565805752,-6.49448704978994));
#58101=CARTESIAN_POINT('Ctrl Pts',(1.91281431352082,20.5866187437557,-6.52203861053669));
#58102=CARTESIAN_POINT('Ctrl Pts',(1.92253441500054,20.5853643741097,-6.52880678000705));
#58103=CARTESIAN_POINT('Ctrl Pts',(1.93813933311725,20.5847740821371,-6.53517979671551));
#58104=CARTESIAN_POINT('Ctrl Pts',(1.9431128878361,20.584762433612,-6.53665410256436));
#58105=CARTESIAN_POINT('Ctrl Pts',(1.95140011040206,20.5850644550901,-6.53809843282379));
#58106=CARTESIAN_POINT('Ctrl Pts',(1.95458052096174,20.5852542906539,-6.53841990666983));
#58107=CARTESIAN_POINT('Ctrl Pts',(1.95776807072638,20.5855189702533,-6.53850782206139));
#58108=CARTESIAN_POINT('',(1.65494820650842,23.7981126208907,-4.35135855429466));
#58109=CARTESIAN_POINT('Origin',(1.65494820650842,23.0854404918828,-6.7784969295689));
#58110=CARTESIAN_POINT('',(1.36757616935991,23.6797887759252,-4.62909020638214));
#58111=CARTESIAN_POINT('Origin',(1.6653400148523,23.714868609534,-4.63939057489758));
#58112=CARTESIAN_POINT('Origin',(1.36757616935991,23.0515849268112,-6.7685560387305));
#58113=CARTESIAN_POINT('Origin',(1.65494820650842,23.0854404918828,-6.7784969295689));
#58114=CARTESIAN_POINT('Origin',(6.4980472271939,23.6560104598922,-6.94603138825146));
#58115=CARTESIAN_POINT('',(11.664677238709,21.6751526289,-5.84039987251776));
#58116=CARTESIAN_POINT('Ctrl Pts',(11.664677238709,21.6751526289,-5.84039987251776));
#58117=CARTESIAN_POINT('Ctrl Pts',(8.45037669575293,21.402871216531,-5.77002260034825));
#58118=CARTESIAN_POINT('Ctrl Pts',(5.17722936343352,21.1255230570061,-5.69865861638706));
#58119=CARTESIAN_POINT('Ctrl Pts',(1.95776807072638,20.8526247727479,-5.62882899907202));
#58120=CARTESIAN_POINT('',(11.3203626311916,25.0326095573615,-4.35942481973593));
#58121=CARTESIAN_POINT('Origin',(11.3203626311916,24.2241318908269,-7.11284689157994));
#58122=CARTESIAN_POINT('',(11.664677238709,21.3918572850628,-6.80521520986101));
#58123=CARTESIAN_POINT('Origin',(11.3203626311916,24.2241318908269,-7.11284689157994));
#58124=CARTESIAN_POINT('Ctrl Pts',(1.95776807072638,20.5855189702533,-6.53850782206136));
#58125=CARTESIAN_POINT('Ctrl Pts',(5.17722935754855,20.8528483568881,-6.62730336112007));
#58126=CARTESIAN_POINT('Ctrl Pts',(8.45037668926195,21.1247507584877,-6.71721389316579));
#58127=CARTESIAN_POINT('Ctrl Pts',(11.664677238709,21.3918572850628,-6.80521520986103));
#58128=CARTESIAN_POINT('Origin',(11.3307544395355,24.2253561593642,-7.11320636925698));
#58129=CARTESIAN_POINT('',(11.6285182850279,24.9844453796138,-4.65775720885429));
#58130=CARTESIAN_POINT('Origin',(11.6285182850279,24.2604359929731,-7.12350673777241));
#58131=CARTESIAN_POINT('Origin',(11.3307544395355,24.9493655460049,-4.64745684033885));
#58132=CARTESIAN_POINT('Ctrl Pts',(11.664677238709,21.3918572850628,-6.80521520986105));
#58133=CARTESIAN_POINT('Ctrl Pts',(11.66817568376,21.392148003834,-6.80531099050326));
#58134=CARTESIAN_POINT('Ctrl Pts',(11.6716557442405,21.3925320801382,-6.80510802126784));
#58135=CARTESIAN_POINT('Ctrl Pts',(11.6751111337893,21.3930057822509,-6.80461609443976));
#58136=CARTESIAN_POINT('Ctrl Pts',(11.6834492137324,21.394148856289,-6.80342904297689));
#58137=CARTESIAN_POINT('Ctrl Pts',(11.691252831794,21.3957587099621,-6.80061996099569));
#58138=CARTESIAN_POINT('Ctrl Pts',(11.709123952862,21.4004306123475,-6.79107647501344));
#58139=CARTESIAN_POINT('Ctrl Pts',(11.7184891157759,21.403813335391,-6.78312340780538));
#58140=CARTESIAN_POINT('Ctrl Pts',(11.7423632180108,21.4140531027239,-6.75768907273798));
#58141=CARTESIAN_POINT('Ctrl Pts',(11.7550185107736,21.4219230191941,-6.73640225084232));
#58142=CARTESIAN_POINT('Ctrl Pts',(11.7829456066502,21.4426696595899,-6.67837363135184));
#58143=CARTESIAN_POINT('Ctrl Pts',(11.7977324484732,21.4588425587731,-6.63074355011391));
#58144=CARTESIAN_POINT('Ctrl Pts',(11.8194386441992,21.4943291980106,-6.521319716713));
#58145=CARTESIAN_POINT('Ctrl Pts',(11.825673894872,21.5120261889324,-6.46460165559978));
#58146=CARTESIAN_POINT('Ctrl Pts',(11.8317749863308,21.5456655992248,-6.3534917234499));
#58147=CARTESIAN_POINT('Ctrl Pts',(11.8316012176116,21.5626634804396,-6.29550105310408));
#58148=CARTESIAN_POINT('Ctrl Pts',(11.824941361477,21.5942940881578,-6.18401117291967));
#58149=CARTESIAN_POINT('Ctrl Pts',(11.8183083548574,21.6099774638489,-6.126836323049));
#58150=CARTESIAN_POINT('Ctrl Pts',(11.7958216244891,21.6390644648081,-6.01598903175142));
#58151=CARTESIAN_POINT('Ctrl Pts',(11.7805655796945,21.6509055854707,-5.96804659261267));
#58152=CARTESIAN_POINT('Ctrl Pts',(11.7536264417729,21.6637010911389,-5.91239047179336));
#58153=CARTESIAN_POINT('Ctrl Pts',(11.7402881749122,21.6689390523323,-5.88871674863419));
#58154=CARTESIAN_POINT('Ctrl Pts',(11.7136982696186,21.6740487842635,-5.86095365010973));
#58155=CARTESIAN_POINT('Ctrl Pts',(11.7035133274599,21.6753527807432,-5.85270707163253));
#58156=CARTESIAN_POINT('Ctrl Pts',(11.6842762528669,21.6760998603139,-5.84347561415645));
#58157=CARTESIAN_POINT('Ctrl Pts',(11.6760378533014,21.6759905549143,-5.84111037910662));
#58158=CARTESIAN_POINT('Ctrl Pts',(11.6665534479108,21.6753057278234,-5.8404626022536));
#58159=CARTESIAN_POINT('Ctrl Pts',(11.6656136423373,21.6752319510726,-5.84042037512234));
#58160=CARTESIAN_POINT('Ctrl Pts',(11.664677238709,21.6751526289,-5.84039987251776));
#58161=CARTESIAN_POINT('Origin',(11.6285182850279,24.2604359929731,-7.12350673777241));
#58162=CARTESIAN_POINT('Origin',(1.06052702375292,25.4510030262676,-7.47308876036672));
#58163=CARTESIAN_POINT('Origin',(1.6653400148523,20.2416680737422,-13.0085301837882));
#58164=CARTESIAN_POINT('',(1.95776807072638,18.4221225649395,-11.2756851683684));
#58165=CARTESIAN_POINT('',(1.95776807072638,17.9095502835289,-12.0732632065885));
#58166=CARTESIAN_POINT('Ctrl Pts',(1.95776807072638,18.4221225649395,-11.2756851683684));
#58167=CARTESIAN_POINT('Ctrl Pts',(1.95134736181873,18.4216395935691,-11.2753982116637));
#58168=CARTESIAN_POINT('Ctrl Pts',(1.9450156712346,18.4206438937207,-11.2759639830928));
#58169=CARTESIAN_POINT('Ctrl Pts',(1.92948836979285,18.4169777842863,-11.2793502116275));
#58170=CARTESIAN_POINT('Ctrl Pts',(1.92089186233944,18.4138230903948,-11.2830613241244));
#58171=CARTESIAN_POINT('Ctrl Pts',(1.90046800930148,18.404219117633,-11.2953067736055));
#58172=CARTESIAN_POINT('Ctrl Pts',(1.88964186308571,18.3968030080759,-11.3055760598063));
#58173=CARTESIAN_POINT('Ctrl Pts',(1.85810283833446,18.3704851710231,-11.3430782725488));
#58174=CARTESIAN_POINT('Ctrl Pts',(1.84335629303651,18.3481042542479,-11.3767845480163));
#58175=CARTESIAN_POINT('Ctrl Pts',(1.8185401058917,18.3040341652241,-11.4435429822488));
#58176=CARTESIAN_POINT('Ctrl Pts',(1.80836917826471,18.2726985595787,-11.4918522175943));
#58177=CARTESIAN_POINT('Ctrl Pts',(1.79896764765288,18.2274018269566,-11.5619364610544));
#58178=CARTESIAN_POINT('Ctrl Pts',(1.79670145400055,18.2114630036209,-11.5866568740709));
#58179=CARTESIAN_POINT('Ctrl Pts',(1.79434535609111,18.1842435918479,-11.6289286489362));
#58180=CARTESIAN_POINT('Ctrl Pts',(1.79381557303811,18.1727761179958,-11.6467551189361));
#58181=CARTESIAN_POINT('Ctrl Pts',(1.79365032105972,18.1502654058704,-11.6817769814638));
#58182=CARTESIAN_POINT('Ctrl Pts',(1.79398945985935,18.1391347052039,-11.6991076651005));
#58183=CARTESIAN_POINT('Ctrl Pts',(1.79575501944582,18.1136547229068,-11.7388159539015));
#58184=CARTESIAN_POINT('Ctrl Pts',(1.79749007695653,18.0991705776075,-11.7614139961328));
#58185=CARTESIAN_POINT('Ctrl Pts',(1.80455267776998,18.0593401604995,-11.8236744660539));
#58186=CARTESIAN_POINT('Ctrl Pts',(1.8118645191381,18.0330203540234,-11.8649367864138));
#58187=CARTESIAN_POINT('Ctrl Pts',(1.83578355229011,17.9799323185428,-11.9490437490375));
#58188=CARTESIAN_POINT('Ctrl Pts',(1.85214505346392,17.9570952779814,-11.9858397344734));
#58189=CARTESIAN_POINT('Ctrl Pts',(1.88061329933208,17.9321806919607,-12.0275219208858));
#58190=CARTESIAN_POINT('Ctrl Pts',(1.89448595076435,17.9221533057526,-12.0446318207675));
#58191=CARTESIAN_POINT('Ctrl Pts',(1.92022261571983,17.9130069990605,-12.0622553637806));
#58192=CARTESIAN_POINT('Ctrl Pts',(1.92864558703621,17.9109234054499,-12.0666669158282));
#58193=CARTESIAN_POINT('Ctrl Pts',(1.9419227872126,17.9094652452642,-12.0709092294435));
#58194=CARTESIAN_POINT('Ctrl Pts',(1.94616291414738,17.9092382087298,-12.0719097149397));
#58195=CARTESIAN_POINT('Ctrl Pts',(1.95291207284946,17.9092807395708,-12.0729030082249));
#58196=CARTESIAN_POINT('Ctrl Pts',(1.95533909577677,17.9093756366031,-12.0731421041236));
#58197=CARTESIAN_POINT('Ctrl Pts',(1.95776807072638,17.9095502835289,-12.0732632065885));
#58198=CARTESIAN_POINT('',(1.65494820650842,21.6082024737958,-10.8798010752069));
#58199=CARTESIAN_POINT('Origin',(1.65494820650842,20.2405946732479,-13.0078403511776));
#58200=CARTESIAN_POINT('',(1.36757616935991,21.416425527482,-11.1129469645577));
#58201=CARTESIAN_POINT('Origin',(1.6653400148523,21.447182432187,-11.1327132269901));
#58202=CARTESIAN_POINT('Origin',(1.36757616935991,20.2109111690372,-12.9887639213558));
#58203=CARTESIAN_POINT('Origin',(1.65494820650842,20.2405946732479,-13.0078403511776));
#58204=CARTESIAN_POINT('Origin',(6.4980472271939,20.7408526371047,-13.3293366230661));
#58205=CARTESIAN_POINT('',(11.664677238709,19.1517258603906,-11.7104188108481));
#58206=CARTESIAN_POINT('Ctrl Pts',(11.664677238709,19.1517258603906,-11.7104188108481));
#58207=CARTESIAN_POINT('Ctrl Pts',(8.44760841234031,18.9100934028027,-11.566057551542));
#58208=CARTESIAN_POINT('Ctrl Pts',(5.17558411912346,18.6641695178434,-11.4194969970449));
#58209=CARTESIAN_POINT('Ctrl Pts',(1.95776807072638,18.4221225649395,-11.2756851683684));
#58210=CARTESIAN_POINT('',(11.3203626311916,22.7904210807013,-11.2353385785459));
#58211=CARTESIAN_POINT('Origin',(11.3203626311916,21.2389637999728,-13.6494532297333));
#58212=CARTESIAN_POINT('',(11.664677238709,18.6080860766515,-12.5563388263038));
#58213=CARTESIAN_POINT('Origin',(11.3203626311916,21.2389637999728,-13.6494532297333));
#58214=CARTESIAN_POINT('Ctrl Pts',(1.95776807072638,17.9095502835289,-12.0732632065885));
#58215=CARTESIAN_POINT('Ctrl Pts',(5.17558411308691,18.1409160618572,-12.2336952663475));
#58216=CARTESIAN_POINT('Ctrl Pts',(8.44760840593807,18.3763927053254,-12.3965120458592));
#58217=CARTESIAN_POINT('Ctrl Pts',(11.664677238709,18.6080860766515,-12.5563388263038));
#58218=CARTESIAN_POINT('Origin',(11.3307544395355,21.2400372004671,-13.6501430623439));
#58219=CARTESIAN_POINT('',(11.6285182850279,22.6601579437975,-11.5080169927616));
#58220=CARTESIAN_POINT('Origin',(11.6285182850279,21.2707941051722,-13.6699093247763));
#58221=CARTESIAN_POINT('Origin',(11.3307544395355,22.6294010390925,-11.4882507303292));
#58222=CARTESIAN_POINT('Ctrl Pts',(11.664677238709,18.6080860766515,-12.5563388263038));
#58223=CARTESIAN_POINT('Ctrl Pts',(11.6681719057554,18.6083377626526,-12.5565124444052));
#58224=CARTESIAN_POINT('Ctrl Pts',(11.6716519636862,18.6087630873824,-12.5564264617449));
#58225=CARTESIAN_POINT('Ctrl Pts',(11.6751111337893,18.6093568419532,-12.5560875483161));
#58226=CARTESIAN_POINT('Ctrl Pts',(11.6833639439589,18.6107734082434,-12.5552789762861));
#58227=CARTESIAN_POINT('Ctrl Pts',(11.6912209922801,18.6131029323727,-12.5530553109812));
#58228=CARTESIAN_POINT('Ctrl Pts',(11.7092716451021,18.6203670705107,-12.5451050615272));
#58229=CARTESIAN_POINT('Ctrl Pts',(11.7188321121789,18.6259692752841,-12.5382858333101));
#58230=CARTESIAN_POINT('Ctrl Pts',(11.7448362096954,18.6446600490309,-12.5145712192165));
#58231=CARTESIAN_POINT('Ctrl Pts',(11.7582763496129,18.6601414182571,-12.4935901023802));
#58232=CARTESIAN_POINT('Ctrl Pts',(11.7901173768954,18.7031288181136,-12.4342691481539));
#58233=CARTESIAN_POINT('Ctrl Pts',(11.807496900688,18.7427730168718,-12.3773456251789));
#58234=CARTESIAN_POINT('Ctrl Pts',(11.8229354401012,18.8072490251109,-12.2814049176089));
#58235=CARTESIAN_POINT('Ctrl Pts',(11.8261991991769,18.8268628597468,-12.2518426658348));
#58236=CARTESIAN_POINT('Ctrl Pts',(11.8295237141305,18.8585151047524,-12.2035704025212));
#58237=CARTESIAN_POINT('Ctrl Pts',(11.8303434615844,18.8708529717768,-12.1846162306134));
#58238=CARTESIAN_POINT('Ctrl Pts',(11.8309946485842,18.8938873215581,-12.1489677324933));
#58239=CARTESIAN_POINT('Ctrl Pts',(11.8309459330901,18.9046640233566,-12.1321843072664));
#58240=CARTESIAN_POINT('Ctrl Pts',(11.8300359252892,18.9280174953952,-12.0955751475506));
#58241=CARTESIAN_POINT('Ctrl Pts',(11.8290394062419,18.9406788268584,-12.0755774687242));
#58242=CARTESIAN_POINT('Ctrl Pts',(11.8249644421306,18.9736962566426,-12.023004023433));
#58243=CARTESIAN_POINT('Ctrl Pts',(11.8209395722477,18.9943695927783,-11.9896581821858));
#58244=CARTESIAN_POINT('Ctrl Pts',(11.8028867656277,19.0556901070888,-11.8891741309915));
#58245=CARTESIAN_POINT('Ctrl Pts',(11.7841990134601,19.0898144719035,-11.831040921109));
#58246=CARTESIAN_POINT('Ctrl Pts',(11.7507704380576,19.1229326946467,-11.7717678295022));
#58247=CARTESIAN_POINT('Ctrl Pts',(11.7371459986439,19.1343448984335,-11.7509308503553));
#58248=CARTESIAN_POINT('Ctrl Pts',(11.7101248465183,19.1461490561111,-11.7271518112195));
#58249=CARTESIAN_POINT('Ctrl Pts',(11.700195678653,19.1493048584522,-11.7203319567739));
#58250=CARTESIAN_POINT('Ctrl Pts',(11.6812735959896,19.1520152885414,-11.7127291553658));
#58251=CARTESIAN_POINT('Ctrl Pts',(11.6731643433663,19.1523622516496,-11.7108014088155));
#58252=CARTESIAN_POINT('Ctrl Pts',(11.6646867061662,19.1517265711868,-11.7104192361762));
#58253=CARTESIAN_POINT('Ctrl Pts',(11.6646819724071,19.1517262159363,-11.7104190232658));
#58254=CARTESIAN_POINT('Ctrl Pts',(11.664677238709,19.1517258603906,-11.7104188108481));
#58255=CARTESIAN_POINT('Origin',(11.6285182850279,21.2707941051722,-13.6699093247763));
#58256=CARTESIAN_POINT('Origin',(1.06052702375292,22.314646171184,-14.3407523135387));
#58257=CARTESIAN_POINT('Origin',(1.6653400148523,15.756811821565,-18.1843302095478));
#58258=CARTESIAN_POINT('',(1.95776807072638,14.4991695475011,-16.0090523844052));
#58259=CARTESIAN_POINT('',(1.95776807072638,13.7826563450298,-16.6299146085788));
#58260=CARTESIAN_POINT('Ctrl Pts',(1.95776807072638,14.4991695475011,-16.0090523844052));
#58261=CARTESIAN_POINT('Ctrl Pts',(1.95134736175434,14.4987869849071,-16.0086409827002));
#58262=CARTESIAN_POINT('Ctrl Pts',(1.9450156711341,14.4976722216424,-16.0089033153653));
#58263=CARTESIAN_POINT('Ctrl Pts',(1.92948836979141,14.4932006046047,-16.0111195154529));
#58264=CARTESIAN_POINT('Ctrl Pts',(1.92089186233797,14.4891281567692,-16.013791521842));
#58265=CARTESIAN_POINT('Ctrl Pts',(1.90046800929961,14.4764632705929,-16.0228351927764));
#58266=CARTESIAN_POINT('Ctrl Pts',(1.88964186308364,14.4664543733224,-16.0305991412233));
#58267=CARTESIAN_POINT('Ctrl Pts',(1.85810283833147,14.430636999304,-16.0591676593232));
#58268=CARTESIAN_POINT('Ctrl Pts',(1.84335629303329,14.3996665117438,-16.0852031608956));
#58269=CARTESIAN_POINT('Ctrl Pts',(1.81854010589001,14.3385735466119,-16.1368414306103));
#58270=CARTESIAN_POINT('Ctrl Pts',(1.80836917826375,14.2948969687799,-16.1743655421849));
#58271=CARTESIAN_POINT('Ctrl Pts',(1.79896764765251,14.2316900589987,-16.2288493170464));
#58272=CARTESIAN_POINT('Ctrl Pts',(1.79670145400032,14.2094323248355,-16.2480778941888));
#58273=CARTESIAN_POINT('Ctrl Pts',(1.79434535609101,14.171406155279,-16.2809687706792));
#58274=CARTESIAN_POINT('Ctrl Pts',(1.79381557303806,14.1553808977203,-16.2948423826596));
#58275=CARTESIAN_POINT('Ctrl Pts',(1.79365032105974,14.1239152287297,-16.3221036131944));
#58276=CARTESIAN_POINT('Ctrl Pts',(1.79398945985941,14.1083527818359,-16.3355964016136));
#58277=CARTESIAN_POINT('Ctrl Pts',(1.79575501944599,14.0727178001221,-16.3665176851518));
#58278=CARTESIAN_POINT('Ctrl Pts',(1.7974900769568,14.0524537602606,-16.3841196926017));
#58279=CARTESIAN_POINT('Ctrl Pts',(1.80455267777069,13.9966959535269,-16.4326366507742));
#58280=CARTESIAN_POINT('Ctrl Pts',(1.81186451913932,13.9598173451288,-16.4648124108617));
#58281=CARTESIAN_POINT('Ctrl Pts',(1.83578355229297,13.8851840784728,-16.5305558225588));
#58282=CARTESIAN_POINT('Ctrl Pts',(1.85214505346792,13.852905471457,-16.5594273742142));
#58283=CARTESIAN_POINT('Ctrl Pts',(1.88061329933735,13.8172568722789,-16.592401889178));
#58284=CARTESIAN_POINT('Ctrl Pts',(1.89448595076901,13.8028152498295,-16.6059936767371));
#58285=CARTESIAN_POINT('Ctrl Pts',(1.92022261572312,13.7890743069924,-16.6203265300565));
#58286=CARTESIAN_POINT('Ctrl Pts',(1.92864558703888,13.7858322357257,-16.623972367093));
#58287=CARTESIAN_POINT('Ctrl Pts',(1.94192278721444,13.7832379434119,-16.6276320260008));
#58288=CARTESIAN_POINT('Ctrl Pts',(1.94616291414881,13.7827382341155,-16.6285280212212));
#58289=CARTESIAN_POINT('Ctrl Pts',(1.9529120727631,13.782499199105,-16.629493061459));
#58290=CARTESIAN_POINT('Ctrl Pts',(1.95533909571058,13.782522891035,-16.6297492078852));
#58291=CARTESIAN_POINT('Ctrl Pts',(1.95776807072638,13.7826563450298,-16.6299146085789));
#58292=CARTESIAN_POINT('',(1.65494820650842,17.6677242712023,-16.5268268176743));
#58293=CARTESIAN_POINT('Origin',(1.65494820650842,15.755976249638,-18.1833659081392));
#58294=CARTESIAN_POINT('',(1.36757616935991,17.418030851189,-16.6964988509053));
#58295=CARTESIAN_POINT('Origin',(1.6653400148523,17.4419730854894,-16.7241296622268));
#58296=CARTESIAN_POINT('Origin',(1.36757616935991,15.7328695872647,-18.1566993982262));
#58297=CARTESIAN_POINT('Origin',(1.65494820650842,15.755976249638,-18.1833659081392));
#58298=CARTESIAN_POINT('Origin',(6.4980472271939,16.1453942842592,-18.6327782772971));
#58299=CARTESIAN_POINT('',(11.664677238709,15.0767401623716,-16.6317292616657));
#58300=CARTESIAN_POINT('Ctrl Pts',(11.664677238709,15.0767401623716,-16.6317292616657));
#58301=CARTESIAN_POINT('Ctrl Pts',(8.44646649976651,14.8854989259897,-16.425066587821));
#58302=CARTESIAN_POINT('Ctrl Pts',(5.17487115867276,14.6908529438561,-16.2151856480993));
#58303=CARTESIAN_POINT('Ctrl Pts',(1.95776807072638,14.4991695475011,-16.0090523844052));
#58304=CARTESIAN_POINT('',(11.3203626311916,18.7018882279357,-17.2010320248535));
#58305=CARTESIAN_POINT('Origin',(11.3203626311916,16.5331411750263,-19.0802620436377));
#58306=CARTESIAN_POINT('',(11.664677238709,14.316798400859,-17.2902225464619));
#58307=CARTESIAN_POINT('Origin',(11.3203626311916,16.5331411750263,-19.0802620436377));
#58308=CARTESIAN_POINT('Ctrl Pts',(1.95776807072638,13.7826563450298,-16.6299146085789));
#58309=CARTESIAN_POINT('Ctrl Pts',(5.17487115257265,13.959412077432,-16.8489827660136));
#58310=CARTESIAN_POINT('Ctrl Pts',(8.44646649340719,14.1394557203275,-17.0715167046817));
#58311=CARTESIAN_POINT('Ctrl Pts',(11.664677238709,14.316798400859,-17.2902225464619));
#58312=CARTESIAN_POINT('Origin',(11.3307544395355,16.5339767469533,-19.0812263450464));
#58313=CARTESIAN_POINT('',(11.6285182850279,18.5000792765231,-17.4259656807277));
#58314=CARTESIAN_POINT('Origin',(11.6285182850279,16.5579189812536,-19.1088571563679));
#58315=CARTESIAN_POINT('Origin',(11.3307544395355,18.4761370422228,-17.3983348694061));
#58316=CARTESIAN_POINT('Ctrl Pts',(11.664677238709,14.316798400859,-17.2902225464619));
#58317=CARTESIAN_POINT('Ctrl Pts',(11.6681719057554,14.316990977937,-17.2904600399508));
#58318=CARTESIAN_POINT('Ctrl Pts',(11.6716519636862,14.3174232981415,-17.2904973680161));
#58319=CARTESIAN_POINT('Ctrl Pts',(11.6751111337893,14.3180884844271,-17.2903394629558));
#58320=CARTESIAN_POINT('Ctrl Pts',(11.6833639439589,14.3196754708946,-17.2899627366173));
#58321=CARTESIAN_POINT('Ctrl Pts',(11.6912209922801,14.3225371118404,-17.2884854481706));
#58322=CARTESIAN_POINT('Ctrl Pts',(11.7092716451021,14.3317468454494,-17.282903783892));
#58323=CARTESIAN_POINT('Ctrl Pts',(11.7188321121788,14.3390433201674,-17.2779391058069));
#58324=CARTESIAN_POINT('Ctrl Pts',(11.7448362096952,14.3636581651119,-17.2604508996893));
#58325=CARTESIAN_POINT('Ctrl Pts',(11.7582763496127,14.3844234937979,-17.2446812712418));
#58326=CARTESIAN_POINT('Ctrl Pts',(11.7901173768955,14.442382246023,-17.1998741825469));
#58327=CARTESIAN_POINT('Ctrl Pts',(11.807496900688,14.4964577858483,-17.1564255236989));
#58328=CARTESIAN_POINT('Ctrl Pts',(11.8229354401012,14.5853516835692,-17.0825360795582));
#58329=CARTESIAN_POINT('Ctrl Pts',(11.8261991991769,14.6124996688663,-17.0596971624782));
#58330=CARTESIAN_POINT('Ctrl Pts',(11.8295237141305,14.656469643716,-17.0222977329236));
#58331=CARTESIAN_POINT('Ctrl Pts',(11.8303434615844,14.6736477477497,-17.0075873169801));
#58332=CARTESIAN_POINT('Ctrl Pts',(11.8309946485842,14.7057923870397,-16.979872359773));
#58333=CARTESIAN_POINT('Ctrl Pts',(11.8309459330901,14.7208609939958,-16.9668049289466));
#58334=CARTESIAN_POINT('Ctrl Pts',(11.8300359252892,14.7535824784968,-16.938258130818));
#58335=CARTESIAN_POINT('Ctrl Pts',(11.8290394062419,14.771364934259,-16.9226376077816));
#58336=CARTESIAN_POINT('Ctrl Pts',(11.8249644421306,14.8178565773077,-16.8814958413394));
#58337=CARTESIAN_POINT('Ctrl Pts',(11.8209395722478,14.8470871071857,-16.8553250928114));
#58338=CARTESIAN_POINT('Ctrl Pts',(11.8028867656278,14.9342333384695,-16.7761873370138));
#58339=CARTESIAN_POINT('Ctrl Pts',(11.7841990134602,14.983353444596,-16.7300228751476));
#58340=CARTESIAN_POINT('Ctrl Pts',(11.7507704380578,15.0318293062667,-16.6824812417983));
#58341=CARTESIAN_POINT('Ctrl Pts',(11.7371459986441,15.0486496910258,-16.6657034960673));
#58342=CARTESIAN_POINT('Ctrl Pts',(11.7101248465183,15.0666750268719,-16.6462132906209));
#58343=CARTESIAN_POINT('Ctrl Pts',(11.700195678653,15.0716243720746,-16.6405587804617));
#58344=CARTESIAN_POINT('Ctrl Pts',(11.6812735959896,15.0763669673805,-16.6340275623301));
#58345=CARTESIAN_POINT('Ctrl Pts',(11.6731643433662,15.0772429850095,-16.6322756538638));
#58346=CARTESIAN_POINT('Ctrl Pts',(11.6646867061662,15.0767407245468,-16.6317298700195));
#58347=CARTESIAN_POINT('Ctrl Pts',(11.664681972407,15.0767404436703,-16.6317295656479));
#58348=CARTESIAN_POINT('Ctrl Pts',(11.664677238709,15.0767401623716,-16.6317292616657));
#58349=CARTESIAN_POINT('Origin',(11.6285182850279,16.5579189812536,-19.1088571563679));
#58350=CARTESIAN_POINT('Origin',(1.06052702375292,17.3704893936218,-20.0466134020057));
#58351=CARTESIAN_POINT('Origin',(1.6653400148523,9.99543238497271,-21.8869439481057));
#58352=CARTESIAN_POINT('',(1.95776807072638,9.40158004320574,-19.4454613857581));
#58353=CARTESIAN_POINT('',(1.95776807072638,8.5391735580698,-19.8393092308925));
#58354=CARTESIAN_POINT('Ctrl Pts',(1.95776807072638,9.40158004320574,-19.4454613857581));
#58355=CARTESIAN_POINT('Ctrl Pts',(1.95134736182033,9.40132888234158,-19.4449588683802));
#58356=CARTESIAN_POINT('Ctrl Pts',(1.9450156712371,9.4001853671993,-19.4448965096135));
#58357=CARTESIAN_POINT('Ctrl Pts',(1.9294883697929,9.39527050632201,-19.4457631379299));
#58358=CARTESIAN_POINT('Ctrl Pts',(1.9208918623395,9.39061023004678,-19.4471795681443));
#58359=CARTESIAN_POINT('Ctrl Pts',(1.90046800930151,9.37591046421419,-19.4522887960966));
#58360=CARTESIAN_POINT('Ctrl Pts',(1.88964186308573,9.36411964056307,-19.4569184178595));
#58361=CARTESIAN_POINT('Ctrl Pts',(1.85810283833451,9.32170444021247,-19.4742387898801));
#58362=CARTESIAN_POINT('Ctrl Pts',(1.84335629303657,9.28465342658525,-19.490494276055));
#58363=CARTESIAN_POINT('Ctrl Pts',(1.81854010589175,9.21148697404632,-19.5228289557441));
#58364=CARTESIAN_POINT('Ctrl Pts',(1.80836917826474,9.15900784060588,-19.5465279631953));
#58365=CARTESIAN_POINT('Ctrl Pts',(1.79896764765288,9.08301140158671,-19.5809973180491));
#58366=CARTESIAN_POINT('Ctrl Pts',(1.79670145400056,9.05623794584522,-19.5931762743548));
#58367=CARTESIAN_POINT('Ctrl Pts',(1.7943453560911,9.01048567261109,-19.6140216292677));
#58368=CARTESIAN_POINT('Ctrl Pts',(1.79381557303811,8.99120090240708,-19.6228184256956));
#58369=CARTESIAN_POINT('Ctrl Pts',(1.79365032105972,8.95332943791956,-19.6401104814682));
#58370=CARTESIAN_POINT('Ctrl Pts',(1.79398945985935,8.93459602169254,-19.6486722691968));
#58371=CARTESIAN_POINT('Ctrl Pts',(1.79575501944581,8.89169297485158,-19.6683014889754));
#58372=CARTESIAN_POINT('Ctrl Pts',(1.79749007695653,8.86729071242359,-19.6794814516828));
#58373=CARTESIAN_POINT('Ctrl Pts',(1.80455267776997,8.80012268196408,-19.7103243426947));
#58374=CARTESIAN_POINT('Ctrl Pts',(1.81186451913807,8.75567295717316,-19.7308068537818));
#58375=CARTESIAN_POINT('Ctrl Pts',(1.83578355228958,8.6655408027493,-19.7728605743246));
#58376=CARTESIAN_POINT('Ctrl Pts',(1.85214505346309,8.62643565005177,-19.7914686907894));
#58377=CARTESIAN_POINT('Ctrl Pts',(1.8806132993318,8.58294107520657,-19.8130641352126));
#58378=CARTESIAN_POINT('Ctrl Pts',(1.89448595076413,8.56525519087511,-19.822036684658));
#58379=CARTESIAN_POINT('Ctrl Pts',(1.92022261571973,8.54803282135688,-19.8319176857522));
#58380=CARTESIAN_POINT('Ctrl Pts',(1.92864558703613,8.54389492576569,-19.8345024437446));
#58381=CARTESIAN_POINT('Ctrl Pts',(1.94192278721276,8.54037467545705,-19.8372829641461));
#58382=CARTESIAN_POINT('Ctrl Pts',(1.94616291414744,8.5396427768739,-19.8380018808868));
#58383=CARTESIAN_POINT('Ctrl Pts',(1.9529120728908,8.53914154119746,-19.838860486286));
#58384=CARTESIAN_POINT('Ctrl Pts',(1.95533909580839,8.53909210866309,-19.8391129317619));
#58385=CARTESIAN_POINT('Ctrl Pts',(1.95776807072638,8.53917355806979,-19.8393092308925));
#58386=CARTESIAN_POINT('',(1.65494820650842,12.2959121221581,-20.8349473401973));
#58387=CARTESIAN_POINT('Origin',(1.65494820650842,9.9949023346812,-21.8857832998643));
#58388=CARTESIAN_POINT('',(1.36757616935991,12.0085309043509,-20.9273996982545));
#58389=CARTESIAN_POINT('Origin',(1.6653400148523,12.0237188108134,-20.9606565744588));
#58390=CARTESIAN_POINT('Origin',(1.36757616935991,9.98024447851015,-21.8536870719015));
#58391=CARTESIAN_POINT('Origin',(1.65494820650842,9.9949023346812,-21.8857832998643));
#58392=CARTESIAN_POINT('Origin',(6.4980472271939,10.24193210686,-22.4267030489007));
#58393=CARTESIAN_POINT('',(11.664677238709,9.78032664122358,-20.2056359204057));
#58394=CARTESIAN_POINT('Ctrl Pts',(11.664677238709,9.78032664122358,-20.2056359204057));
#58395=CARTESIAN_POINT('Ctrl Pts',(8.44908820479151,9.65515767378835,-19.9536710841398));
#58396=CARTESIAN_POINT('Ctrl Pts',(5.17648536371073,9.52748760709607,-19.697374593167));
#58397=CARTESIAN_POINT('Ctrl Pts',(1.95776807072638,9.40158004320575,-19.4454613857581));
#58398=CARTESIAN_POINT('',(11.3203626311916,13.0982396153547,-21.7732001549839));
#58399=CARTESIAN_POINT('Origin',(11.3203626311916,10.4879017784557,-22.9653015014543));
#58400=CARTESIAN_POINT('',(11.664677238709,8.86564886390742,-20.6233552648184));
#58401=CARTESIAN_POINT('Origin',(11.3203626311916,10.4879017784557,-22.9653015014543));
#58402=CARTESIAN_POINT('Ctrl Pts',(1.95776807072638,8.5391735580698,-19.8393092308925));
#58403=CARTESIAN_POINT('Ctrl Pts',(5.17648535775567,8.64710493744507,-20.0994318861236));
#58404=CARTESIAN_POINT('Ctrl Pts',(8.44908819833864,8.75719478781139,-20.3637569928305));
#58405=CARTESIAN_POINT('Ctrl Pts',(11.664677238709,8.86564886390743,-20.6233552648184));
#58406=CARTESIAN_POINT('Origin',(11.3307544395355,10.4884318287472,-22.9664621496957));
#58407=CARTESIAN_POINT('',(11.6285182850279,12.8412342104726,-21.9321662654496));
#58408=CARTESIAN_POINT('Origin',(11.6285182850279,10.5036197352098,-22.9997190259));
#58409=CARTESIAN_POINT('Origin',(11.3307544395355,12.8260463040101,-21.8989093892453));
#58410=CARTESIAN_POINT('Ctrl Pts',(11.664677238709,8.86564886390742,-20.6233552648184));
#58411=CARTESIAN_POINT('Ctrl Pts',(11.6681531449969,8.8657660978575,-20.6236358788069));
#58412=CARTESIAN_POINT('Ctrl Pts',(11.6716331726355,8.86616731353293,-20.623794813083));
#58413=CARTESIAN_POINT('Ctrl Pts',(11.6751111337893,8.86685375084357,-20.623830903915));
#58414=CARTESIAN_POINT('Ctrl Pts',(11.6835034416364,8.8685101216234,-20.623917990964));
#58415=CARTESIAN_POINT('Ctrl Pts',(11.6913221163004,8.87170945339749,-20.6232869878783));
#58416=CARTESIAN_POINT('Ctrl Pts',(11.7093237578239,8.88207391467146,-20.6205407109361));
#58417=CARTESIAN_POINT('Ctrl Pts',(11.7187565997267,8.89041824124016,-20.6178443174412));
#58418=CARTESIAN_POINT('Ctrl Pts',(11.7431727782355,8.91707792401492,-20.6086622526054));
#58419=CARTESIAN_POINT('Ctrl Pts',(11.7560898230284,8.93917319578265,-20.6003233906746));
#58420=CARTESIAN_POINT('Ctrl Pts',(11.7841758181733,8.9980591075342,-20.5773806426638));
#58421=CARTESIAN_POINT('Ctrl Pts',(11.7988195826631,9.04537291470594,-20.5580695606808));
#58422=CARTESIAN_POINT('Ctrl Pts',(11.8183861888449,9.14332972967495,-20.5165359590652));
#58423=CARTESIAN_POINT('Ctrl Pts',(11.8239771978735,9.18842241074054,-20.4969162334911));
#58424=CARTESIAN_POINT('Ctrl Pts',(11.8302306705076,9.27219438300242,-20.4597498600097));
#58425=CARTESIAN_POINT('Ctrl Pts',(11.8313291886565,9.31273094134296,-20.4414345067909));
#58426=CARTESIAN_POINT('Ctrl Pts',(11.8301000822046,9.39324349826456,-20.4044483831862));
#58427=CARTESIAN_POINT('Ctrl Pts',(11.8275983467483,9.43446674805166,-20.3851769035863));
#58428=CARTESIAN_POINT('Ctrl Pts',(11.8179490511515,9.51988766495169,-20.3445084778329));
#58429=CARTESIAN_POINT('Ctrl Pts',(11.8098404493788,9.56648167385506,-20.3218506008119));
#58430=CARTESIAN_POINT('Ctrl Pts',(11.7817370234729,9.66788637809238,-20.271128320578));
#58431=CARTESIAN_POINT('Ctrl Pts',(11.7608617911997,9.7115392210737,-20.2481472837836));
#58432=CARTESIAN_POINT('Ctrl Pts',(11.727864569176,9.75179858555556,-20.2255615388921));
#58433=CARTESIAN_POINT('Ctrl Pts',(11.7163738956147,9.76278438208106,-20.2191422746271));
#58434=CARTESIAN_POINT('Ctrl Pts',(11.6949981921876,9.77494241482742,-20.2111886963503));
#58435=CARTESIAN_POINT('Ctrl Pts',(11.6861739271887,9.77828873356615,-20.2087116448862));
#58436=CARTESIAN_POINT('Ctrl Pts',(11.6727399598045,9.7802682842181,-20.2064478679052));
#58437=CARTESIAN_POINT('Ctrl Pts',(11.6686987410324,9.78048318090824,-20.2059510344218));
#58438=CARTESIAN_POINT('Ctrl Pts',(11.664677238709,9.78032664122358,-20.2056359204057));
#58439=CARTESIAN_POINT('Origin',(11.6285182850279,10.5036197352098,-22.9997190259));
#58440=CARTESIAN_POINT('Origin',(1.06052702375292,11.0190788716665,-24.1284170944427));
#58441=CARTESIAN_POINT('Origin',(1.6653400148523,3.42428246167523,-23.8164076546558));
#58442=CARTESIAN_POINT('',(1.95776807072638,3.54233043715926,-21.3065147522487));
#58443=CARTESIAN_POINT('',(1.95776807072638,2.60389771385557,-21.4414410082343));
#58444=CARTESIAN_POINT('Ctrl Pts',(1.95776807072638,3.54233043715926,-21.3065147522487));
#58445=CARTESIAN_POINT('Ctrl Pts',(1.9513478551885,3.54223103321939,-21.3059618726496));
#58446=CARTESIAN_POINT('Ctrl Pts',(1.94501663599459,3.54115156508228,-21.3055798899085));
#58447=CARTESIAN_POINT('Ctrl Pts',(1.92952577557711,3.53620362915063,-21.3050279766058));
#58448=CARTESIAN_POINT('Ctrl Pts',(1.92095957337033,3.53135931038363,-21.3050724139772));
#58449=CARTESIAN_POINT('Ctrl Pts',(1.90072805817451,3.51599592158735,-21.3058205399649));
#58450=CARTESIAN_POINT('Ctrl Pts',(1.8900249560485,3.5036082187607,-21.3069139518805));
#58451=CARTESIAN_POINT('Ctrl Pts',(1.86013121923959,3.46075124654105,-21.3112847102786));
#58452=CARTESIAN_POINT('Ctrl Pts',(1.8458449021105,3.42403619031257,-21.3159449618369));
#58453=CARTESIAN_POINT('Ctrl Pts',(1.82200825445925,3.35110430677947,-21.3254531739389));
#58454=CARTESIAN_POINT('Ctrl Pts',(1.81203215259484,3.30105316932586,-21.3323795986619));
#58455=CARTESIAN_POINT('Ctrl Pts',(1.79984169249385,3.21193645609611,-21.3448875851979));
#58456=CARTESIAN_POINT('Ctrl Pts',(1.79638078494032,3.16936789071309,-21.3509444797466));
#58457=CARTESIAN_POINT('Ctrl Pts',(1.79327894813701,3.08828446690876,-21.3625442583892));
#58458=CARTESIAN_POINT('Ctrl Pts',(1.79337026915323,3.0484033806662,-21.36827974357));
#58459=CARTESIAN_POINT('Ctrl Pts',(1.79687828838528,2.96705307114344,-21.3800426367113));
#58460=CARTESIAN_POINT('Ctrl Pts',(1.80059938175367,2.92417828176263,-21.3862765917232));
#58461=CARTESIAN_POINT('Ctrl Pts',(1.81351118858405,2.83463727606645,-21.3994816448112));
#58462=CARTESIAN_POINT('Ctrl Pts',(1.82404219007374,2.78419034711656,-21.4070273995978));
#58463=CARTESIAN_POINT('Ctrl Pts',(1.84885798811629,2.71258004937781,-21.4183745299768));
#58464=CARTESIAN_POINT('Ctrl Pts',(1.86388962647713,2.67578411025394,-21.4243315771976));
#58465=CARTESIAN_POINT('Ctrl Pts',(1.89490216133537,2.63563438875233,-21.4320245979044));
#58466=CARTESIAN_POINT('Ctrl Pts',(1.90722460488475,2.62233152903849,-21.4347412883587));
#58467=CARTESIAN_POINT('Ctrl Pts',(1.92907437017015,2.60993293818406,-21.4381786237551));
#58468=CARTESIAN_POINT('Ctrl Pts',(1.93579728934589,2.60716195128725,-21.4391080543931));
#58469=CARTESIAN_POINT('Ctrl Pts',(1.94779808654533,2.60440407097883,-21.440500869962));
#58470=CARTESIAN_POINT('Ctrl Pts',(1.95276363818104,2.60385064352413,-21.4410056766482));
#58471=CARTESIAN_POINT('Ctrl Pts',(1.95776807072638,2.60389771385557,-21.4414410082343));
#58472=CARTESIAN_POINT('',(1.65494820650842,5.92795829958164,-23.4551443394205));
#58473=CARTESIAN_POINT('Origin',(1.65494820650842,3.42410087454151,-23.8151446883994));
#58474=CARTESIAN_POINT('',(1.36757616935991,5.62617120112542,-23.4628870820895));
#58475=CARTESIAN_POINT('Origin',(1.6653400148523,5.63137434589457,-23.4990757488526));
#58476=CARTESIAN_POINT('Origin',(1.36757616935991,3.41907931690607,-23.7802189878927));
#58477=CARTESIAN_POINT('Origin',(1.65494820650842,3.42410087454151,-23.8151446883994));
#58478=CARTESIAN_POINT('Origin',(6.4980472271939,3.50872950127857,-24.4037497162211));
#58479=CARTESIAN_POINT('',(11.664677238709,3.69156922144576,-22.1426021244183));
#58480=CARTESIAN_POINT('Ctrl Pts',(11.664677238709,3.69156922144575,-22.1426021244183));
#58481=CARTESIAN_POINT('Ctrl Pts',(8.45131537604982,3.64249119006552,-21.8657713317644));
#58482=CARTESIAN_POINT('Ctrl Pts',(5.17772237568178,3.5921848606183,-21.5838024904321));
#58483=CARTESIAN_POINT('Ctrl Pts',(1.95776807072638,3.54233043715926,-21.3065147522487));
#58484=CARTESIAN_POINT('',(11.3203626311916,6.43344952736807,-24.5814330987647));
#58485=CARTESIAN_POINT('Origin',(11.3203626311916,3.5929949537482,-24.98982881153));
#58486=CARTESIAN_POINT('',(11.664677238709,2.69625718204607,-22.2857063914358));
#58487=CARTESIAN_POINT('Origin',(11.3203626311916,3.5929949537482,-24.98982881153));
#58488=CARTESIAN_POINT('Ctrl Pts',(1.95776807072638,2.60389771385556,-21.4414410082343));
#58489=CARTESIAN_POINT('Ctrl Pts',(5.17772236984729,2.63418372824732,-21.7215422583742));
#58490=CARTESIAN_POINT('Ctrl Pts',(8.45131536953639,2.66535496122478,-22.0062623111724));
#58491=CARTESIAN_POINT('Ctrl Pts',(11.664677238709,2.69625718204608,-22.2857063914358));
#58492=CARTESIAN_POINT('Origin',(11.3307544395355,3.59317654088192,-24.9910917777863));
#58493=CARTESIAN_POINT('',(11.6285182850279,6.14206871845015,-24.6615531749599));
#58494=CARTESIAN_POINT('Origin',(11.6285182850279,3.59837968565107,-25.0272804445494));
#58495=CARTESIAN_POINT('Origin',(11.3307544395355,6.136865573681,-24.6253645081968));
#58496=CARTESIAN_POINT('Ctrl Pts',(11.664677238709,2.69625718204607,-22.2857063914358));
#58497=CARTESIAN_POINT('Ctrl Pts',(11.668173931419,2.6962908089996,-22.2860104748594));
#58498=CARTESIAN_POINT('Ctrl Pts',(11.6716539907387,2.69663467728562,-22.2862755639136));
#58499=CARTESIAN_POINT('Ctrl Pts',(11.6751111337893,2.69727925957648,-22.2865022196842));
#58500=CARTESIAN_POINT('Ctrl Pts',(11.6834715430146,2.69883805296517,-22.2870503413465));
#58501=CARTESIAN_POINT('Ctrl Pts',(11.6912510114763,2.70206385531498,-22.2873454247033));
#58502=CARTESIAN_POINT('Ctrl Pts',(11.709035822972,2.7126169387773,-22.2876313864347));
#58503=CARTESIAN_POINT('Ctrl Pts',(11.7183186554656,2.72116951930899,-22.2874079360076));
#58504=CARTESIAN_POINT('Ctrl Pts',(11.7418333015258,2.74801369053577,-22.2861920544586));
#58505=CARTESIAN_POINT('Ctrl Pts',(11.7542369034695,2.76996803543835,-22.2845703704499));
#58506=CARTESIAN_POINT('Ctrl Pts',(11.7824157539259,2.83096774741555,-22.2794147158946));
#58507=CARTESIAN_POINT('Ctrl Pts',(11.797437382068,2.88153241037196,-22.2742976507484));
#58508=CARTESIAN_POINT('Ctrl Pts',(11.8209603099608,3.00475150470494,-22.2601056375115));
#58509=CARTESIAN_POINT('Ctrl Pts',(11.8274214370012,3.07312747241092,-22.2513392489146));
#58510=CARTESIAN_POINT('Ctrl Pts',(11.8323708659761,3.20740533159247,-22.2328342493678));
#58511=CARTESIAN_POINT('Ctrl Pts',(11.8303885473322,3.27899188856699,-22.2222076907846));
#58512=CARTESIAN_POINT('Ctrl Pts',(11.8177935569394,3.40658761118923,-22.2018688414514));
#58513=CARTESIAN_POINT('Ctrl Pts',(11.8075558566742,3.46929474611099,-22.1912401030956));
#58514=CARTESIAN_POINT('Ctrl Pts',(11.7765253671339,3.57657231689514,-22.1714404504546));
#58515=CARTESIAN_POINT('Ctrl Pts',(11.7586671916648,3.61570515885657,-22.1634661165603));
#58516=CARTESIAN_POINT('Ctrl Pts',(11.7297382659252,3.65639661653937,-22.1542106095143));
#58517=CARTESIAN_POINT('Ctrl Pts',(11.7183817710579,3.66905637710907,-22.1511082048343));
#58518=CARTESIAN_POINT('Ctrl Pts',(11.6971067724022,3.68375234586319,-22.1467808943914));
#58519=CARTESIAN_POINT('Ctrl Pts',(11.688166617688,3.68804578318866,-22.1452727334554));
#58520=CARTESIAN_POINT('Ctrl Pts',(11.6739702938601,3.69116836143546,-22.1434932346172));
#58521=CARTESIAN_POINT('Ctrl Pts',(11.6693161741268,3.69164007241986,-22.1430017682255));
#58522=CARTESIAN_POINT('Ctrl Pts',(11.664677238709,3.69156922144579,-22.1426021244183));
#58523=CARTESIAN_POINT('Origin',(11.6285182850279,3.59837968565107,-25.0272804445494));
#58524=CARTESIAN_POINT('Origin',(1.06052702375292,3.7749681125142,-26.2554799311097));
#58525=CARTESIAN_POINT('Origin',(1.6653400148523,-3.42428246167523,-23.8164076546558));
#58526=CARTESIAN_POINT('',(1.95776807072638,-2.60389771385556,-21.4414410082343));
#58527=CARTESIAN_POINT('',(1.95776807072638,-3.54233043715928,-21.3065147522487));
#58528=CARTESIAN_POINT('Ctrl Pts',(1.95776807072638,-2.60389771385556,-21.4414410082343));
#58529=CARTESIAN_POINT('Ctrl Pts',(1.9513478551885,-2.60383732705435,-21.4408825188176));
#58530=CARTESIAN_POINT('Ctrl Pts',(1.94501663599459,-2.60476545217281,-21.4402118877432));
#58531=CARTESIAN_POINT('Ctrl Pts',(1.92952577557707,-2.60935746998721,-21.4382883361661));
#58532=CARTESIAN_POINT('Ctrl Pts',(1.92095957337023,-2.61401807926046,-21.4369661711994));
#58533=CARTESIAN_POINT('Ctrl Pts',(1.90072805817454,-2.62896991430867,-21.4333556260207));
#58534=CARTESIAN_POINT('Ctrl Pts',(1.89002495604859,-2.64116387786459,-21.4309147278802));
#58535=CARTESIAN_POINT('Ctrl Pts',(1.86013121924006,-2.68351622651802,-21.4230342354907));
#58536=CARTESIAN_POINT('Ctrl Pts',(1.84584490211098,-2.72005700958138,-21.4171618874505));
#58537=CARTESIAN_POINT('Ctrl Pts',(1.82200825445927,-2.79271341229176,-21.4057376641306));
#58538=CARTESIAN_POINT('Ctrl Pts',(1.81203215259485,-2.84268852634673,-21.398282485057));
#58539=CARTESIAN_POINT('Ctrl Pts',(1.79984169249383,-2.93171929355026,-21.3851767307768));
#58540=CARTESIAN_POINT('Ctrl Pts',(1.79638078494031,-2.97426995731992,-21.3789953277718));
#58541=CARTESIAN_POINT('Ctrl Pts',(1.793278948137,-3.05533696803266,-21.367281393569));
#58542=CARTESIAN_POINT('Ctrl Pts',(1.79337026915323,-3.09521846296713,-21.3615487509035));
#58543=CARTESIAN_POINT('Ctrl Pts',(1.79687828838528,-3.17658750331602,-21.3499161335203));
#58544=CARTESIAN_POINT('Ctrl Pts',(1.80059938175368,-3.21948187055685,-21.3438183455158));
#58545=CARTESIAN_POINT('Ctrl Pts',(1.81351118858406,-3.30911612974239,-21.331261884693));
#58546=CARTESIAN_POINT('Ctrl Pts',(1.82404219007374,-3.35964548839957,-21.3242894411135));
#58547=CARTESIAN_POINT('Ctrl Pts',(1.84885798811644,-3.43155192197327,-21.3150019807047));
#58548=CARTESIAN_POINT('Ctrl Pts',(1.86388962647725,-3.46853566116466,-21.3103511116458));
#58549=CARTESIAN_POINT('Ctrl Pts',(1.89490216133386,-3.50922641122945,-21.3064210272649));
#58550=CARTESIAN_POINT('Ctrl Pts',(1.90722460488324,-3.52275579180277,-21.3052798239866));
#58551=CARTESIAN_POINT('Ctrl Pts',(1.92907437017048,-3.53562056190136,-21.3050848364448));
#58552=CARTESIAN_POINT('Ctrl Pts',(1.93579728934604,-3.53854115522866,-21.305195941388));
#58553=CARTESIAN_POINT('Ctrl Pts',(1.94779808654517,-3.54157972349803,-21.3057553534691));
#58554=CARTESIAN_POINT('Ctrl Pts',(1.95276363818094,-3.54225295373074,-21.3060837934058));
#58555=CARTESIAN_POINT('Ctrl Pts',(1.95776807072638,-3.54233043715928,-21.3065147522487));
#58556=CARTESIAN_POINT('',(1.65494820650842,-0.920243449501391,-24.1751450373783));
#58557=CARTESIAN_POINT('Origin',(1.65494820650842,-3.42410087454152,-23.8151446883994));
#58558=CARTESIAN_POINT('',(1.36757616935991,-1.21198743268674,-24.0975508936959));
#58559=CARTESIAN_POINT('Origin',(1.6653400148523,-1.21719057745589,-24.133739560459));
#58560=CARTESIAN_POINT('Origin',(1.36757616935991,-3.41907931690608,-23.7802189878927));
#58561=CARTESIAN_POINT('Origin',(1.65494820650842,-3.42410087454152,-23.8151446883994));
#58562=CARTESIAN_POINT('Origin',(6.4980472271939,-3.50872950127858,-24.4037497162211));
#58563=CARTESIAN_POINT('',(11.664677238709,-2.69625718204607,-22.2857063914358));
#58564=CARTESIAN_POINT('Ctrl Pts',(11.664677238709,-2.69625718204607,-22.2857063914358));
#58565=CARTESIAN_POINT('Ctrl Pts',(8.45131537604982,-2.66535496128742,-22.0062623117388));
#58566=CARTESIAN_POINT('Ctrl Pts',(5.17772237568178,-2.6341837283022,-21.7215422588817));
#58567=CARTESIAN_POINT('Ctrl Pts',(1.95776807072638,-2.60389771385556,-21.4414410082343));
#58568=CARTESIAN_POINT('',(11.3203626311916,-0.752540380128349,-25.3982245242953));
#58569=CARTESIAN_POINT('Origin',(11.3203626311916,-3.59299495374821,-24.98982881153));
#58570=CARTESIAN_POINT('',(11.664677238709,-3.69156922144578,-22.1426021244183));
#58571=CARTESIAN_POINT('Origin',(11.3203626311916,-3.59299495374821,-24.98982881153));
#58572=CARTESIAN_POINT('Ctrl Pts',(1.95776807072638,-3.54233043715928,-21.3065147522487));
#58573=CARTESIAN_POINT('Ctrl Pts',(5.17772236984729,-3.59218486052798,-21.5838024899296));
#58574=CARTESIAN_POINT('Ctrl Pts',(8.45131536953638,-3.64249118996606,-21.8657713312033));
#58575=CARTESIAN_POINT('Ctrl Pts',(11.664677238709,-3.69156922144577,-22.1426021244183));
#58576=CARTESIAN_POINT('Origin',(11.3307544395355,-3.59317654088193,-24.9910917777863));
#58577=CARTESIAN_POINT('',(11.6285182850279,-1.054690652852,-25.393007714139));
#58578=CARTESIAN_POINT('Origin',(11.6285182850279,-3.59837968565108,-25.0272804445494));
#58579=CARTESIAN_POINT('Origin',(11.3307544395355,-1.04948750808285,-25.3568190473759));
#58580=CARTESIAN_POINT('Ctrl Pts',(11.664677238709,-3.69156922144578,-22.1426021244183));
#58581=CARTESIAN_POINT('Ctrl Pts',(11.6681739314189,-3.69162262682055,-22.1429033641341));
#58582=CARTESIAN_POINT('Ctrl Pts',(11.6716539907387,-3.69136737183329,-22.1432545941105));
#58583=CARTESIAN_POINT('Ctrl Pts',(11.6751111337893,-3.69081275596405,-22.1436536685467));
#58584=CARTESIAN_POINT('Ctrl Pts',(11.6834715430144,-3.68947152837769,-22.1446187502773));
#58585=CARTESIAN_POINT('Ctrl Pts',(11.691251011476,-3.68645952827763,-22.1458106942287));
#58586=CARTESIAN_POINT('Ctrl Pts',(11.7090358229721,-3.67641448357506,-22.1490582196872));
#58587=CARTESIAN_POINT('Ctrl Pts',(11.7183186554659,-3.66814538938815,-22.1512533609532));
#58588=CARTESIAN_POINT('Ctrl Pts',(11.7418333015258,-3.64204604229627,-22.1576496081462));
#58589=CARTESIAN_POINT('Ctrl Pts',(11.7542369034694,-3.62052412143989,-22.1622788674575));
#58590=CARTESIAN_POINT('Ctrl Pts',(11.7824157539265,-3.560542810664,-22.1745176579595));
#58591=CARTESIAN_POINT('Ctrl Pts',(11.7974373820683,-3.51058472799645,-22.1838535816868));
#58592=CARTESIAN_POINT('Ctrl Pts',(11.8209603099608,-3.38835852059437,-22.2049512752024));
#58593=CARTESIAN_POINT('Ctrl Pts',(11.8274214370012,-3.32028248294269,-22.215803723148));
#58594=CARTESIAN_POINT('Ctrl Pts',(11.8323708659761,-3.1862303597095,-22.2358787507005));
#58595=CARTESIAN_POINT('Ctrl Pts',(11.8303885473322,-3.11454971376705,-22.2458509061382));
#58596=CARTESIAN_POINT('Ctrl Pts',(11.8177935569394,-2.9863923984218,-22.2622837922879));
#58597=CARTESIAN_POINT('Ctrl Pts',(11.8075558566742,-2.92323088143592,-22.2697522339708));
#58598=CARTESIAN_POINT('Ctrl Pts',(11.7765253671338,-2.81472059927844,-22.2809781906907));
#58599=CARTESIAN_POINT('Ctrl Pts',(11.7586671916646,-2.774926282902,-22.2843518689721));
#58600=CARTESIAN_POINT('Ctrl Pts',(11.7297382659251,-2.73327553750453,-22.2869353834087));
#58601=CARTESIAN_POINT('Ctrl Pts',(11.7183817710579,-2.72025453778751,-22.2875253146313));
#58602=CARTESIAN_POINT('Ctrl Pts',(11.6971067724022,-2.70493471479219,-22.287513623519));
#58603=CARTESIAN_POINT('Ctrl Pts',(11.688166617688,-2.70039029380909,-22.2872761547732));
#58604=CARTESIAN_POINT('Ctrl Pts',(11.6739702938601,-2.69689285916415,-22.2864484700947));
#58605=CARTESIAN_POINT('Ctrl Pts',(11.6693161741268,-2.69630179370591,-22.2861098078869));
#58606=CARTESIAN_POINT('Ctrl Pts',(11.664677238709,-2.69625718204607,-22.2857063914358));
#58607=CARTESIAN_POINT('Origin',(11.6285182850279,-3.59837968565108,-25.0272804445494));
#58608=CARTESIAN_POINT('Origin',(1.06052702375292,-3.77496811251421,-26.2554799311097));
#58609=CARTESIAN_POINT('Origin',(1.6653400148523,-9.99543238497271,-21.8869439481057));
#58610=CARTESIAN_POINT('',(1.95776807072638,-8.5391735580698,-19.8393092308925));
#58611=CARTESIAN_POINT('',(1.95776807072638,-9.40158004320575,-19.4454613857581));
#58612=CARTESIAN_POINT('Ctrl Pts',(1.95776807072638,-8.53917355806981,-19.8393092308925));
#58613=CARTESIAN_POINT('Ctrl Pts',(1.95134736181011,-8.53895825616284,-19.8387903372766));
#58614=CARTESIAN_POINT('Ctrl Pts',(1.94501567122114,-8.53965997172107,-19.8378852898844));
#58615=CARTESIAN_POINT('Ctrl Pts',(1.92948836979265,-8.54353347509979,-19.8347384067269));
#58616=CARTESIAN_POINT('Ctrl Pts',(1.92089186233923,-8.54765577357349,-19.8321439694452));
#58617=CARTESIAN_POINT('Ctrl Pts',(1.90046800930119,-8.56114336986581,-19.8243804604408));
#58618=CARTESIAN_POINT('Ctrl Pts',(1.88964186308534,-8.57236355197267,-19.8185013079906));
#58619=CARTESIAN_POINT('Ctrl Pts',(1.85810283833392,-8.61322946498746,-19.7977884699129));
#58620=CARTESIAN_POINT('Ctrl Pts',(1.84335629303589,-8.64977779572316,-19.7804322617416));
#58621=CARTESIAN_POINT('Ctrl Pts',(1.81854010589147,-8.72212855294446,-19.7463114584516));
#58622=CARTESIAN_POINT('Ctrl Pts',(1.80836917826458,-8.7744055915797,-19.7221699251048));
#58623=CARTESIAN_POINT('Ctrl Pts',(1.79896764765284,-8.85022287567158,-19.6873082756821));
#58624=CARTESIAN_POINT('Ctrl Pts',(1.79670145400053,-8.87696000159258,-19.6750497681666));
#58625=CARTESIAN_POINT('Ctrl Pts',(1.79434535609109,-8.922675236925,-19.6541233115617));
#58626=CARTESIAN_POINT('Ctrl Pts',(1.7938155730381,-8.94195225085071,-19.6453095312537));
#58627=CARTESIAN_POINT('Ctrl Pts',(1.79365032105972,-8.97982124967063,-19.6280120764217));
#58628=CARTESIAN_POINT('Ctrl Pts',(1.79398945985935,-8.99855959580199,-19.6194610836778));
#58629=CARTESIAN_POINT('Ctrl Pts',(1.79575501944584,-9.04148989103746,-19.5998915295602));
#58630=CARTESIAN_POINT('Ctrl Pts',(1.79749007695657,-9.06591922657842,-19.588770848701));
#58631=CARTESIAN_POINT('Ctrl Pts',(1.80455267777008,-9.1332144340572,-19.5582064365159));
#58632=CARTESIAN_POINT('Ctrl Pts',(1.81186451913826,-9.17780246249345,-19.5380267681685));
#58633=CARTESIAN_POINT('Ctrl Pts',(1.83578355229033,-9.26860855269313,-19.4974487611261));
#58634=CARTESIAN_POINT('Ctrl Pts',(1.8521450534642,-9.3082800577872,-19.4800807834256));
#58635=CARTESIAN_POINT('Ctrl Pts',(1.88061329933269,-9.35308369492277,-19.4613517855849));
#58636=CARTESIAN_POINT('Ctrl Pts',(1.8944859507649,-9.37144648654039,-19.4538614563447));
#58637=CARTESIAN_POINT('Ctrl Pts',(1.92022261572022,-9.39019230245402,-19.4473163375408));
#58638=CARTESIAN_POINT('Ctrl Pts',(1.92864558703654,-9.39485547755033,-19.445881781225));
#58639=CARTESIAN_POINT('Ctrl Pts',(1.94192278721307,-9.39926212836097,-19.4450422071836));
#58640=CARTESIAN_POINT('Ctrl Pts',(1.94616291414767,-9.40028474102502,-19.4449598654854));
#58641=CARTESIAN_POINT('Ctrl Pts',(1.95291207288063,-9.4012618712514,-19.4451433237978));
#58642=CARTESIAN_POINT('Ctrl Pts',(1.95533909580059,-9.40148502823929,-19.4452712818103));
#58643=CARTESIAN_POINT('Ctrl Pts',(1.95776807072638,-9.40158004320576,-19.4454613857581));
#58644=CARTESIAN_POINT('',(1.65494820650842,-7.69389254720435,-22.9366192595313));
#58645=CARTESIAN_POINT('Origin',(1.65494820650842,-9.99490233468121,-21.8857832998643));
#58646=CARTESIAN_POINT('',(1.36757616935991,-7.95195805266942,-22.7799744455484));
#58647=CARTESIAN_POINT('Origin',(1.6653400148523,-7.96714595913197,-22.8132313217527));
#58648=CARTESIAN_POINT('Origin',(1.36757616935991,-9.98024447851016,-21.8536870719015));
#58649=CARTESIAN_POINT('Origin',(1.65494820650842,-9.99490233468121,-21.8857832998643));
#58650=CARTESIAN_POINT('Origin',(6.4980472271939,-10.24193210686,-22.4267030489007));
#58651=CARTESIAN_POINT('',(11.664677238709,-8.86564886390744,-20.6233552648184));
#58652=CARTESIAN_POINT('Ctrl Pts',(11.664677238709,-8.86564886390743,-20.6233552648184));
#58653=CARTESIAN_POINT('Ctrl Pts',(8.44908820479151,-8.75719478802904,-20.3637569933514));
#58654=CARTESIAN_POINT('Ctrl Pts',(5.17648536371073,-8.64710493764476,-20.0994318866049));
#58655=CARTESIAN_POINT('Ctrl Pts',(1.95776807072638,-8.5391735580698,-19.8393092308925));
#58656=CARTESIAN_POINT('',(11.3203626311916,-7.87756394155673,-24.1574028479247));
#58657=CARTESIAN_POINT('Origin',(11.3203626311916,-10.4879017784557,-22.9653015014543));
#58658=CARTESIAN_POINT('',(11.664677238709,-9.78032664122357,-20.2056359204057));
#58659=CARTESIAN_POINT('Origin',(11.3203626311916,-10.4879017784557,-22.9653015014543));
#58660=CARTESIAN_POINT('Ctrl Pts',(1.95776807072638,-9.40158004320575,-19.4454613857581));
#58661=CARTESIAN_POINT('Ctrl Pts',(5.17648535775567,-9.52748760686313,-19.6973745927009));
#58662=CARTESIAN_POINT('Ctrl Pts',(8.44908819833864,-9.65515767353718,-19.9536710836342));
#58663=CARTESIAN_POINT('Ctrl Pts',(11.664677238709,-9.78032664122359,-20.2056359204057));
#58664=CARTESIAN_POINT('Origin',(11.3307544395355,-10.4884318287472,-22.9664621496957));
#58665=CARTESIAN_POINT('',(11.6285182850279,-8.16600525994691,-24.0672717863504));
#58666=CARTESIAN_POINT('Origin',(11.6285182850279,-10.5036197352098,-22.9997190259));
#58667=CARTESIAN_POINT('Origin',(11.3307544395355,-8.15081735348436,-24.0340149101461));
#58668=CARTESIAN_POINT('Ctrl Pts',(11.664677238709,-9.78032664122358,-20.2056359204057));
#58669=CARTESIAN_POINT('Ctrl Pts',(11.6681531449969,-9.78046194321534,-20.205908282996));
#58670=CARTESIAN_POINT('Ctrl Pts',(11.6716331726355,-9.78031931733511,-20.2063155813886));
#58671=CARTESIAN_POINT('Ctrl Pts',(11.6751111337893,-9.77989707212503,-20.2068579905627));
#58672=CARTESIAN_POINT('Ctrl Pts',(11.6835034416364,-9.77887819594063,-20.2081668219633));
#58673=CARTESIAN_POINT('Ctrl Pts',(11.6913221163003,-9.77630619887358,-20.210171496446));
#58674=CARTESIAN_POINT('Ctrl Pts',(11.7093237578239,-9.76744342252662,-20.2162060047083));
#58675=CARTESIAN_POINT('Ctrl Pts',(11.7187565997267,-9.75994125246948,-20.2207464637378));
#58676=CARTESIAN_POINT('Ctrl Pts',(11.7431727782355,-9.73554353144944,-20.2348815339297));
#58677=CARTESIAN_POINT('Ctrl Pts',(11.7560898230284,-9.7147721142081,-20.2461192329191));
#58678=CARTESIAN_POINT('Ctrl Pts',(11.7841758181735,-9.65887107077546,-20.27559793086));
#58679=CARTESIAN_POINT('Ctrl Pts',(11.7988195826632,-9.61329277429603,-20.2987092511704));
#58680=CARTESIAN_POINT('Ctrl Pts',(11.8183861888449,-9.51775570080867,-20.3455413475508));
#58681=CARTESIAN_POINT('Ctrl Pts',(11.8239771978735,-9.47339867533899,-20.3667719341833));
#58682=CARTESIAN_POINT('Ctrl Pts',(11.8302306705076,-9.39045122916041,-20.405743767947));
#58683=CARTESIAN_POINT('Ctrl Pts',(11.8313291886565,-9.35006360841451,-20.4243852490074));
#58684=CARTESIAN_POINT('Ctrl Pts',(11.8301000822046,-9.26938684912614,-20.4610118195814));
#58685=CARTESIAN_POINT('Ctrl Pts',(11.8275983467482,-9.2278269490101,-20.4795461377865));
#58686=CARTESIAN_POINT('Ctrl Pts',(11.8179490511515,-9.14115299922197,-20.5174708042373));
#58687=CARTESIAN_POINT('Ctrl Pts',(11.8098404493788,-9.09351673143953,-20.5378464526579));
#58688=CARTESIAN_POINT('Ctrl Pts',(11.7817370234729,-8.9887774307,-20.5812669850615));
#58689=CARTESIAN_POINT('Ctrl Pts',(11.7608617911997,-8.94282298913096,-20.599208223942));
#58690=CARTESIAN_POINT('Ctrl Pts',(11.7278645691759,-8.89938954507,-20.6148437040365));
#58691=CARTESIAN_POINT('Ctrl Pts',(11.7163738956146,-8.88734402205839,-20.6189424909766));
#58692=CARTESIAN_POINT('Ctrl Pts',(11.6949981921877,-8.87337129041363,-20.6229224329418));
#58693=CARTESIAN_POINT('Ctrl Pts',(11.6861739271888,-8.86930788707863,-20.6238292881645));
#58694=CARTESIAN_POINT('Ctrl Pts',(11.6727399598044,-8.86630070859597,-20.6238428740718));
#58695=CARTESIAN_POINT('Ctrl Pts',(11.6686987410324,-8.86578449949814,-20.6236799254143));
#58696=CARTESIAN_POINT('Ctrl Pts',(11.664677238709,-8.86564886390742,-20.6233552648184));
#58697=CARTESIAN_POINT('Origin',(11.6285182850279,-10.5036197352098,-22.9997190259));
#58698=CARTESIAN_POINT('Origin',(1.06052702375292,-11.0190788716665,-24.1284170944427));
#58699=CARTESIAN_POINT('Origin',(1.6653400148523,-15.756811821565,-18.1843302095478));
#58700=CARTESIAN_POINT('',(1.95776807072638,-13.7826563450298,-16.6299146085789));
#58701=CARTESIAN_POINT('',(1.95776807072638,-14.4991695475011,-16.0090523844052));
#58702=CARTESIAN_POINT('Ctrl Pts',(1.95776807072638,-13.7826563450298,-16.6299146085789));
#58703=CARTESIAN_POINT('Ctrl Pts',(1.95134736176265,-13.7823035751351,-16.6294773913538));
#58704=CARTESIAN_POINT('Ctrl Pts',(1.94501567114707,-13.7827218849829,-16.6284113086055));
#58705=CARTESIAN_POINT('Ctrl Pts',(1.92948836979158,-13.7855519048069,-16.6243006043354));
#58706=CARTESIAN_POINT('Ctrl Pts',(1.92089186233812,-13.7887762837787,-16.6206498743041));
#58707=CARTESIAN_POINT('Ctrl Pts',(1.90046800929984,-13.7995303044108,-16.6094009469743));
#58708=CARTESIAN_POINT('Ctrl Pts',(1.88964186308388,-13.8086396416535,-16.600598850914));
#58709=CARTESIAN_POINT('Ctrl Pts',(1.85810283833188,-13.842014717222,-16.5692117701521));
#58710=CARTESIAN_POINT('Ctrl Pts',(1.84335629303374,-13.8721927748564,-16.5422617556955));
#58711=CARTESIAN_POINT('Ctrl Pts',(1.81854010589022,-13.9319998768941,-16.4891395208629));
#58712=CARTESIAN_POINT('Ctrl Pts',(1.80836917826387,-13.975357872229,-16.4512477454867));
#58713=CARTESIAN_POINT('Ctrl Pts',(1.79896764765255,-14.038282361965,-16.3964380405179));
#58714=CARTESIAN_POINT('Ctrl Pts',(1.79670145400034,-14.0604828257552,-16.3771433698416));
#58715=CARTESIAN_POINT('Ctrl Pts',(1.79434535609103,-14.0984506087182,-16.3441851116304));
#58716=CARTESIAN_POINT('Ctrl Pts',(1.79381557303806,-14.1144636392704,-16.3302973889325));
#58717=CARTESIAN_POINT('Ctrl Pts',(1.79365032105973,-14.1459254213794,-16.3030316726971));
#58718=CARTESIAN_POINT('Ctrl Pts',(1.7939894598594,-14.1614956397804,-16.2895478530753));
#58719=CARTESIAN_POINT('Ctrl Pts',(1.79575501944596,-14.1971735758964,-16.2586761415598));
#58720=CARTESIAN_POINT('Ctrl Pts',(1.79749007695676,-14.2174802938461,-16.2411233872494));
#58721=CARTESIAN_POINT('Ctrl Pts',(1.8045526777706,-14.2734385825878,-16.192837797648));
#58722=CARTESIAN_POINT('Ctrl Pts',(1.81186451913917,-14.3105352130209,-16.1609136484021));
#58723=CARTESIAN_POINT('Ctrl Pts',(1.83578355229256,-14.3862308728547,-16.0963963037919));
#58724=CARTESIAN_POINT('Ctrl Pts',(1.85214505346734,-14.4194022784807,-16.0685550966583));
#58725=CARTESIAN_POINT('Ctrl Pts',(1.88061329933679,-14.4571144850547,-16.0379621115825));
#58726=CARTESIAN_POINT('Ctrl Pts',(1.8944859507685,-14.4726231849777,-16.0256017970747));
#58727=CARTESIAN_POINT('Ctrl Pts',(1.92022261572266,-14.4887656905743,-16.0140404949249));
#58728=CARTESIAN_POINT('Ctrl Pts',(1.92864558703852,-14.4928358130947,-16.0113502799772));
#58729=CARTESIAN_POINT('Ctrl Pts',(1.94192278721418,-14.4968274282428,-16.0093032175839));
#58730=CARTESIAN_POINT('Ctrl Pts',(1.94616291414861,-14.4977854195714,-16.0089361080226));
#58731=CARTESIAN_POINT('Ctrl Pts',(1.95291207280144,-14.4987746553256,-16.0088368455885));
#58732=CARTESIAN_POINT('Ctrl Pts',(1.95533909573991,-14.4990248228335,-16.0088967498086));
#58733=CARTESIAN_POINT('Ctrl Pts',(1.95776807072638,-14.4991695475011,-16.0090523844052));
#58734=CARTESIAN_POINT('',(1.65494820650842,-13.8442282280737,-19.8399049986041));
#58735=CARTESIAN_POINT('Origin',(1.65494820650842,-15.755976249638,-18.1833659081392));
#58736=CARTESIAN_POINT('',(1.36757616935991,-14.0477083233403,-19.6168999455472));
#58737=CARTESIAN_POINT('Origin',(1.6653400148523,-14.0716505576406,-19.6445307568688));
#58738=CARTESIAN_POINT('Origin',(1.36757616935991,-15.7328695872647,-18.1566993982262));
#58739=CARTESIAN_POINT('Origin',(1.65494820650842,-15.755976249638,-18.1833659081392));
#58740=CARTESIAN_POINT('Origin',(6.4980472271939,-16.1453942842592,-18.6327782772971));
#58741=CARTESIAN_POINT('',(11.664677238709,-14.316798400859,-17.2902225464619));
#58742=CARTESIAN_POINT('Ctrl Pts',(11.664677238709,-14.316798400859,-17.2902225464619));
#58743=CARTESIAN_POINT('Ctrl Pts',(8.44646649976651,-14.1394557206779,-17.0715167051139));
#58744=CARTESIAN_POINT('Ctrl Pts',(5.17487115867276,-13.9594120777672,-16.848982766429));
#58745=CARTESIAN_POINT('Ctrl Pts',(1.95776807072638,-13.7826563450298,-16.6299146085789));
#58746=CARTESIAN_POINT('',(11.3203626311916,-14.3643941221169,-20.959492062422));
#58747=CARTESIAN_POINT('Origin',(11.3203626311916,-16.5331411750263,-19.0802620436377));
#58748=CARTESIAN_POINT('',(11.664677238709,-15.0767401623717,-16.6317292616657));
#58749=CARTESIAN_POINT('Origin',(11.3203626311916,-16.5331411750263,-19.0802620436377));
#58750=CARTESIAN_POINT('Ctrl Pts',(1.95776807072638,-14.4991695475011,-16.0090523844052));
#58751=CARTESIAN_POINT('Ctrl Pts',(5.17487115257265,-14.6908529434927,-16.2151856477085));
#58752=CARTESIAN_POINT('Ctrl Pts',(8.44646649340719,-14.8854989256118,-16.4250665874126));
#58753=CARTESIAN_POINT('Ctrl Pts',(11.664677238709,-15.0767401623716,-16.6317292616657));
#58754=CARTESIAN_POINT('Origin',(11.3307544395355,-16.5339767469533,-19.0812263450464));
#58755=CARTESIAN_POINT('',(11.6285182850279,-14.6157586859842,-20.7917486320082));
#58756=CARTESIAN_POINT('Origin',(11.6285182850279,-16.5579189812536,-19.1088571563679));
#58757=CARTESIAN_POINT('Origin',(11.3307544395355,-14.5918164516839,-20.7641178206866));
#58758=CARTESIAN_POINT('Ctrl Pts',(11.664677238709,-15.0767401623716,-16.6317292616657));
#58759=CARTESIAN_POINT('Ctrl Pts',(11.6681719057554,-15.0769478319436,-16.6319536774342));
#58760=CARTESIAN_POINT('Ctrl Pts',(11.6716519636862,-15.076923254483,-16.6323869095799));
#58761=CARTESIAN_POINT('Ctrl Pts',(11.6751111337893,-15.0766722907899,-16.6330228529951));
#58762=CARTESIAN_POINT('Ctrl Pts',(11.6833639439589,-15.0760735472598,-16.6345400724807));
#58763=CARTESIAN_POINT('Ctrl Pts',(11.6912209922801,-15.0742040415111,-16.6371623459814));
#58764=CARTESIAN_POINT('Ctrl Pts',(11.7092716451022,-15.0673685087776,-16.6454839841326));
#58765=CARTESIAN_POINT('Ctrl Pts',(11.7188321121789,-15.0614159673375,-16.6519996438999));
#58766=CARTESIAN_POINT('Ctrl Pts',(11.7448362096949,-15.0406027082651,-16.6738751139888));
#58767=CARTESIAN_POINT('Ctrl Pts',(11.7582763496123,-15.022038377504,-16.6921848294475));
#58768=CARTESIAN_POINT('Ctrl Pts',(11.7901173768951,-14.9694389699161,-16.7431769315634));
#58769=CARTESIAN_POINT('Ctrl Pts',(11.8074969006878,-14.9187368040632,-16.7905186715063));
#58770=CARTESIAN_POINT('Ctrl Pts',(11.8229354401012,-14.8329485272452,-16.8679921932309));
#58771=CARTESIAN_POINT('Ctrl Pts',(11.826199199177,-14.806478516273,-16.8916135343913));
#58772=CARTESIAN_POINT('Ctrl Pts',(11.8295237141305,-14.7632021791261,-16.9298134645279));
#58773=CARTESIAN_POINT('Ctrl Pts',(11.8303434615844,-14.7461967949088,-16.9447232097655));
#58774=CARTESIAN_POINT('Ctrl Pts',(11.8309946485842,-14.7141892768629,-16.9725964133232));
#58775=CARTESIAN_POINT('Ctrl Pts',(11.8309459330901,-14.6991103672785,-16.9856519542831));
#58776=CARTESIAN_POINT('Ctrl Pts',(11.8300359252892,-14.6661973816186,-17.0139777482937));
#58777=CARTESIAN_POINT('Ctrl Pts',(11.8290394062419,-14.648205145668,-17.0293561720867));
#58778=CARTESIAN_POINT('Ctrl Pts',(11.8249644421306,-14.6008656924252,-17.0695195134069));
#58779=CARTESIAN_POINT('Ctrl Pts',(11.8209395722477,-14.5708013862499,-17.0947280327935));
#58780=CARTESIAN_POINT('Ctrl Pts',(11.8028867656276,-14.4800669368871,-17.1697247641803));
#58781=CARTESIAN_POINT('Ctrl Pts',(11.7841990134598,-14.42738184272,-17.211775010527));
#58782=CARTESIAN_POINT('Ctrl Pts',(11.7507704380578,-14.3734252802354,-17.2529915779606));
#58783=CARTESIAN_POINT('Ctrl Pts',(11.737145998644,-14.3544245174278,-17.2672530332855));
#58784=CARTESIAN_POINT('Ctrl Pts',(11.7101248465184,-14.3325674214146,-17.2823211517671));
#58785=CARTESIAN_POINT('Ctrl Pts',(11.700195678653,-14.3262661007535,-17.2864153990732));
#58786=CARTESIAN_POINT('Ctrl Pts',(11.6812735959896,-14.3191264193213,-17.290180232345));
#58787=CARTESIAN_POINT('Ctrl Pts',(11.6731643433662,-14.3172676724499,-17.2907980108076));
#58788=CARTESIAN_POINT('Ctrl Pts',(11.6646867061662,-14.3167989230148,-17.2902231894927));
#58789=CARTESIAN_POINT('Ctrl Pts',(11.664681972407,-14.3167986617141,-17.2902228681585));
#58790=CARTESIAN_POINT('Ctrl Pts',(11.664677238709,-14.316798400859,-17.2902225464619));
#58791=CARTESIAN_POINT('Origin',(11.6285182850279,-16.5579189812536,-19.1088571563679));
#58792=CARTESIAN_POINT('Origin',(1.06052702375292,-17.3704893936218,-20.0466134020057));
#58793=CARTESIAN_POINT('Origin',(1.6653400148523,-20.2416680737422,-13.0085301837882));
#58794=CARTESIAN_POINT('',(1.95776807072638,-17.9095502835289,-12.0732632065885));
#58795=CARTESIAN_POINT('',(1.95776807072638,-18.4221225649395,-11.2756851683683));
#58796=CARTESIAN_POINT('Ctrl Pts',(1.95776807072638,-17.9095502835289,-12.0732632065885));
#58797=CARTESIAN_POINT('Ctrl Pts',(1.95134736183621,-17.9090886249723,-12.0729430865012));
#58798=CARTESIAN_POINT('Ctrl Pts',(1.94501567126188,-17.9091896400968,-12.0718023361232));
#58799=CARTESIAN_POINT('Ctrl Pts',(1.92948836979328,-17.9107469050198,-12.0670608355043));
#58800=CARTESIAN_POINT('Ctrl Pts',(1.92089186233993,-17.9128121444813,-12.062649573159));
#58801=CARTESIAN_POINT('Ctrl Pts',(1.90046800930196,-17.919961362657,-12.0488265486971));
#58802=CARTESIAN_POINT('Ctrl Pts',(1.88964186308622,-17.9262218707066,-12.0378146025024));
#58803=CARTESIAN_POINT('Ctrl Pts',(1.8581028383352,-17.9494022586918,-11.9982960736773));
#58804=CARTESIAN_POINT('Ctrl Pts',(1.8433562930373,-17.9707651964678,-11.9639355828322));
#58805=CARTESIAN_POINT('Ctrl Pts',(1.81854010589216,-18.0131834276005,-11.8961155639935));
#58806=CARTESIAN_POINT('Ctrl Pts',(1.80836917826496,-18.0441097727155,-11.847543312875));
#58807=CARTESIAN_POINT('Ctrl Pts',(1.79896764765298,-18.0890437001663,-11.7772259086882));
#58808=CARTESIAN_POINT('Ctrl Pts',(1.79670145400062,-18.1049089522812,-11.752458214319));
#58809=CARTESIAN_POINT('Ctrl Pts',(1.79434535609112,-18.1320533589037,-11.71013823657));
#58810=CARTESIAN_POINT('Ctrl Pts',(1.79381557303812,-18.1435051255807,-11.6923016721812));
#58811=CARTESIAN_POINT('Ctrl Pts',(1.79365032105971,-18.1660108445022,-11.657276600717));
#58812=CARTESIAN_POINT('Ctrl Pts',(1.79398945985931,-18.1771515286775,-11.6399523330916));
#58813=CARTESIAN_POINT('Ctrl Pts',(1.79575501944576,-18.2026866914744,-11.6002795066445));
#58814=CARTESIAN_POINT('Ctrl Pts',(1.79749007695645,-18.2172256623124,-11.5777166986477));
#58815=CARTESIAN_POINT('Ctrl Pts',(1.8045526777698,-18.2573136245575,-11.5156217429364));
#58816=CARTESIAN_POINT('Ctrl Pts',(1.81186451913778,-18.2839135086097,-11.4745394175059));
#58817=CARTESIAN_POINT('Ctrl Pts',(1.83578355228869,-18.3383663258931,-11.3913095468931));
#58818=CARTESIAN_POINT('Ctrl Pts',(1.85214505346182,-18.3623502820448,-11.3552506393502));
#58819=CARTESIAN_POINT('Ctrl Pts',(1.88061329933037,-18.3899158393672,-11.3152721287427));
#58820=CARTESIAN_POINT('Ctrl Pts',(1.8944859507629,-18.4013140249654,-11.2990431881354));
#58821=CARTESIAN_POINT('Ctrl Pts',(1.92022261571886,-18.4135454504487,-11.2834023305784));
#58822=CARTESIAN_POINT('Ctrl Pts',(1.92864558703543,-18.4166927832737,-11.2796744022134));
#58823=CARTESIAN_POINT('Ctrl Pts',(1.94192278721233,-18.4199459858402,-11.2765856922882));
#58824=CARTESIAN_POINT('Ctrl Pts',(1.94616291414708,-18.4207617450736,-11.275963555897));
#58825=CARTESIAN_POINT('Ctrl Pts',(1.95291207297762,-18.4216829443939,-11.2755896143607));
#58826=CARTESIAN_POINT('Ctrl Pts',(1.95533909587482,-18.4219398553151,-11.2755766117231));
#58827=CARTESIAN_POINT('Ctrl Pts',(1.95776807072638,-18.4221225649395,-11.2756851683683));
#58828=CARTESIAN_POINT('',(1.65494820650842,-18.8729868727,-15.1358796271483));
#58829=CARTESIAN_POINT('Origin',(1.65494820650842,-20.2405946732479,-13.0078403511776));
#58830=CARTESIAN_POINT('',(1.36757616935991,-19.0053968105924,-14.8645808781538));
#58831=CARTESIAN_POINT('Origin',(1.6653400148523,-19.0361537152975,-14.8843471405862));
#58832=CARTESIAN_POINT('Origin',(1.36757616935991,-20.2109111690372,-12.9887639213558));
#58833=CARTESIAN_POINT('Origin',(1.65494820650842,-20.2405946732479,-13.0078403511776));
#58834=CARTESIAN_POINT('Origin',(6.4980472271939,-20.7408526371047,-13.3293366230661));
#58835=CARTESIAN_POINT('',(11.664677238709,-18.6080860766515,-12.5563388263038));
#58836=CARTESIAN_POINT('Ctrl Pts',(11.664677238709,-18.6080860766515,-12.5563388263039));
#58837=CARTESIAN_POINT('Ctrl Pts',(8.44760841234031,-18.3763927057865,-12.3965120461773));
#58838=CARTESIAN_POINT('Ctrl Pts',(5.17558411912346,-18.1409160622912,-12.2336952666484));
#58839=CARTESIAN_POINT('Ctrl Pts',(1.95776807072638,-17.9095502835289,-12.0732632065885));
#58840=CARTESIAN_POINT('',(11.3203626311916,-19.6875065192443,-16.0635678809207));
#58841=CARTESIAN_POINT('Origin',(11.3203626311916,-21.2389637999728,-13.6494532297333));
#58842=CARTESIAN_POINT('',(11.664677238709,-19.1517258603906,-11.7104188108481));
#58843=CARTESIAN_POINT('Origin',(11.3203626311916,-21.2389637999728,-13.6494532297333));
#58844=CARTESIAN_POINT('Ctrl Pts',(1.95776807072638,-18.4221225649395,-11.2756851683683));
#58845=CARTESIAN_POINT('Ctrl Pts',(5.17558411308691,-18.6641695173893,-11.4194969967751));
#58846=CARTESIAN_POINT('Ctrl Pts',(8.44760840593807,-18.9100934023218,-11.5660575512547));
#58847=CARTESIAN_POINT('Ctrl Pts',(11.664677238709,-19.1517258603906,-11.710418810848));
#58848=CARTESIAN_POINT('Origin',(11.3307544395355,-21.2400372004671,-13.6501430623439));
#58849=CARTESIAN_POINT('',(11.6285182850279,-19.8814302665469,-15.831801656791));
#58850=CARTESIAN_POINT('Origin',(11.6285182850279,-21.2707941051722,-13.6699093247763));
#58851=CARTESIAN_POINT('Origin',(11.3307544395355,-19.8506733618418,-15.8120353943587));
#58852=CARTESIAN_POINT('Ctrl Pts',(11.664677238709,-19.1517258603906,-11.710418810848));
#58853=CARTESIAN_POINT('Ctrl Pts',(11.6681719057554,-19.151988343114,-11.7105756289215));
#58854=CARTESIAN_POINT('Ctrl Pts',(11.6716519636862,-19.1520868168133,-11.7109982363922));
#58855=CARTESIAN_POINT('Ctrl Pts',(11.6751111337893,-19.1520251848775,-11.7116791242736));
#58856=CARTESIAN_POINT('Ctrl Pts',(11.6833639439589,-19.1518781447924,-11.713303571255));
#58857=CARTESIAN_POINT('Ctrl Pts',(11.6912209922801,-19.1508231469805,-11.7163463248885));
#58858=CARTESIAN_POINT('Ctrl Pts',(11.7092716451022,-19.1466089777452,-11.7262566703379));
#58859=CARTESIAN_POINT('Ctrl Pts',(11.7188321121789,-19.142733229544,-11.7341854248227));
#58860=CARTESIAN_POINT('Ctrl Pts',(11.7448362096951,-19.1289260858263,-11.7610385573624));
#58861=CARTESIAN_POINT('Ctrl Pts',(11.7582763496125,-19.1162721838523,-11.7838367770654));
#58862=CARTESIAN_POINT('Ctrl Pts',(11.7901173768954,-19.080169557163,-11.8475823063438));
#58863=CARTESIAN_POINT('Ctrl Pts',(11.807496900688,-19.0448588947193,-11.9072908240012));
#58864=CARTESIAN_POINT('Ctrl Pts',(11.8229354401012,-18.9843724592575,-12.0057954743111));
#58865=CARTESIAN_POINT('Ctrl Pts',(11.826199199177,-18.9656295705594,-12.0359174490525));
#58866=CARTESIAN_POINT('Ctrl Pts',(11.8295237141305,-18.9348683931316,-12.0847623667265));
#58867=CARTESIAN_POINT('Ctrl Pts',(11.8303434615844,-18.9227524071091,-12.103859132896));
#58868=CARTESIAN_POINT('Ctrl Pts',(11.8309946485842,-18.8998942073469,-12.139620835759));
#58869=CARTESIAN_POINT('Ctrl Pts',(11.8309459330901,-18.8891042704865,-12.1563957553283));
#58870=CARTESIAN_POINT('Ctrl Pts',(11.8300359252892,-18.8655047903765,-12.1928468152564));
#58871=CARTESIAN_POINT('Ctrl Pts',(11.8290394062419,-18.8525739690576,-12.2126713034689));
#58872=CARTESIAN_POINT('Ctrl Pts',(11.8249644421306,-18.8184674171377,-12.2645448124643));
#58873=CARTESIAN_POINT('Ctrl Pts',(11.8209395722477,-18.7967229872269,-12.2972023035393));
#58874=CARTESIAN_POINT('Ctrl Pts',(11.8028867656278,-18.7307929414874,-12.3947239887608));
#58875=CARTESIAN_POINT('Ctrl Pts',(11.7841990134602,-18.6920888872388,-12.4499140109567));
#58876=CARTESIAN_POINT('Ctrl Pts',(11.7507704380579,-18.6519299935815,-12.5046623381132));
#58877=CARTESIAN_POINT('Ctrl Pts',(11.7371459986441,-18.6377168114472,-12.5236992377788));
#58878=CARTESIAN_POINT('Ctrl Pts',(11.7101248465183,-18.6209902609454,-12.5443148471325));
#58879=CARTESIAN_POINT('Ctrl Pts',(11.700195678653,-18.6160976708085,-12.5500185358362));
#58880=CARTESIAN_POINT('Ctrl Pts',(11.6812735959896,-18.6103078727442,-12.5556423476123));
#58881=CARTESIAN_POINT('Ctrl Pts',(11.6731643433662,-18.6086984664872,-12.556758771215));
#58882=CARTESIAN_POINT('Ctrl Pts',(11.6646867061662,-18.608086758819,-12.5563392961791));
#58883=CARTESIAN_POINT('Ctrl Pts',(11.6646819724071,-18.6080864175726,-12.5563390614781));
#58884=CARTESIAN_POINT('Ctrl Pts',(11.664677238709,-18.6080860766515,-12.5563388263038));
#58885=CARTESIAN_POINT('Origin',(11.6285182850279,-21.2707941051722,-13.6699093247763));
#58886=CARTESIAN_POINT('Origin',(1.06052702375292,-22.314646171184,-14.3407523135387));
#58887=CARTESIAN_POINT('Origin',(1.6653400148523,-23.0866647604201,-6.77885640724593));
#58888=CARTESIAN_POINT('',(1.95776807072638,-20.5855189702533,-6.53850782206133));
#58889=CARTESIAN_POINT('',(1.95776807072638,-20.8526247727479,-5.62882899907203));
#58890=CARTESIAN_POINT('Ctrl Pts',(1.95776807072638,-20.5855189702533,-6.53850782206133));
#58891=CARTESIAN_POINT('Ctrl Pts',(1.95134808313108,-20.5849858837543,-6.53833075322637));
#58892=CARTESIAN_POINT('Ctrl Pts',(1.94501708168414,-20.5847614100656,-6.53720798404442));
#58893=CARTESIAN_POINT('Ctrl Pts',(1.9295422670371,-20.5849190653626,-6.53223717834212));
#58894=CARTESIAN_POINT('Ctrl Pts',(1.92098940734579,-20.5856501048191,-6.52745980301533));
#58895=CARTESIAN_POINT('Ctrl Pts',(1.90083817144732,-20.5885608974204,-6.5124335905247));
#58896=CARTESIAN_POINT('Ctrl Pts',(1.89018614013605,-20.5913816029721,-6.50042022104495));
#58897=CARTESIAN_POINT('Ctrl Pts',(1.86077829278545,-20.6015952674766,-6.45943708810668));
#58898=CARTESIAN_POINT('Ctrl Pts',(1.84665745875343,-20.6111401079677,-6.42475570917512));
#58899=CARTESIAN_POINT('Ctrl Pts',(1.82247517384168,-20.6308899331561,-6.35397716492069));
#58900=CARTESIAN_POINT('Ctrl Pts',(1.81230887642857,-20.6450040326109,-6.30493959670102));
#58901=CARTESIAN_POINT('Ctrl Pts',(1.79934881945722,-20.6714274602793,-6.21380591726621));
#58902=CARTESIAN_POINT('Ctrl Pts',(1.79572382774366,-20.6848492864795,-6.16787314049738));
#58903=CARTESIAN_POINT('Ctrl Pts',(1.79301769946662,-20.7108870248801,-6.07902063441458));
#58904=CARTESIAN_POINT('Ctrl Pts',(1.79378222861456,-20.7240558919632,-6.0342124780035));
#58905=CARTESIAN_POINT('Ctrl Pts',(1.79982187672879,-20.750481671231,-5.94463801770676));
#58906=CARTESIAN_POINT('Ctrl Pts',(1.80545072973323,-20.7644003702219,-5.89763253001672));
#58907=CARTESIAN_POINT('Ctrl Pts',(1.82510992022552,-20.7940525831227,-5.79870751721765));
#58908=CARTESIAN_POINT('Ctrl Pts',(1.83960979647382,-20.8080958899708,-5.75272231988961));
#58909=CARTESIAN_POINT('Ctrl Pts',(1.86695154341724,-20.8259464835367,-5.69674419663136));
#58910=CARTESIAN_POINT('Ctrl Pts',(1.88252298601468,-20.834745760989,-5.66966644865782));
#58911=CARTESIAN_POINT('Ctrl Pts',(1.91281431352441,-20.8446460331116,-5.64327836389298));
#58912=CARTESIAN_POINT('Ctrl Pts',(1.92253441500334,-20.8472499388902,-5.63690645398558));
#58913=CARTESIAN_POINT('Ctrl Pts',(1.93813933311858,-20.8501988666454,-5.63122599523119));
#58914=CARTESIAN_POINT('Ctrl Pts',(1.94311288783717,-20.8509861372017,-5.62997943255939));
#58915=CARTESIAN_POINT('Ctrl Pts',(1.95140011049575,-20.8520210777408,-5.62892766975318));
#58916=CARTESIAN_POINT('Ctrl Pts',(1.95458052103001,-20.8523545794566,-5.6287598616123));
#58917=CARTESIAN_POINT('Ctrl Pts',(1.95776807072638,-20.8526247727479,-5.62882899907203));
#58918=CARTESIAN_POINT('',(1.65494820650842,-22.3727683628749,-9.20563530484313));
#58919=CARTESIAN_POINT('Origin',(1.65494820650842,-23.0854404918828,-6.77849692956889));
#58920=CARTESIAN_POINT('',(1.36757616935991,-22.4233810776973,-8.90802187107885));
#58921=CARTESIAN_POINT('Origin',(1.6653400148523,-22.4584609113062,-8.91832223959429));
#58922=CARTESIAN_POINT('Origin',(1.36757616935991,-23.0515849268112,-6.76855603873049));
#58923=CARTESIAN_POINT('Origin',(1.65494820650842,-23.0854404918828,-6.77849692956889));
#58924=CARTESIAN_POINT('Origin',(6.4980472271939,-23.6560104598922,-6.94603138825145));
#58925=CARTESIAN_POINT('',(11.664677238709,-21.3918572850628,-6.805215209861));
#58926=CARTESIAN_POINT('Ctrl Pts',(11.664677238709,-21.3918572850628,-6.80521520986101));
#58927=CARTESIAN_POINT('Ctrl Pts',(8.45037669575293,-21.1247507590271,-6.71721389334347));
#58928=CARTESIAN_POINT('Ctrl Pts',(5.17722936343353,-20.8528483573768,-6.62730336128236));
#58929=CARTESIAN_POINT('Ctrl Pts',(1.95776807072638,-20.5855189702533,-6.53850782206134));
#58930=CARTESIAN_POINT('',(11.3203626311916,-23.4156542242922,-9.86626896342394));
#58931=CARTESIAN_POINT('Origin',(11.3203626311916,-24.2241318908269,-7.11284689157993));
#58932=CARTESIAN_POINT('',(11.664677238709,-21.6751526289,-5.84039987251776));
#58933=CARTESIAN_POINT('Origin',(11.3203626311916,-24.2241318908269,-7.11284689157993));
#58934=CARTESIAN_POINT('Ctrl Pts',(1.95776807072638,-20.8526247727479,-5.62882899907202));
#58935=CARTESIAN_POINT('Ctrl Pts',(5.17722935754855,-21.1255230565072,-5.69865861625941));
#58936=CARTESIAN_POINT('Ctrl Pts',(8.45037668926196,-21.4028712159812,-5.77002260020613));
#58937=CARTESIAN_POINT('Ctrl Pts',(11.664677238709,-21.6751526289,-5.84039987251776));
#58938=CARTESIAN_POINT('Origin',(11.3307544395355,-24.2253561593642,-7.11320636925697));
#58939=CARTESIAN_POINT('',(11.6285182850279,-23.5364266063324,-9.58925626669053));
#58940=CARTESIAN_POINT('Origin',(11.6285182850279,-24.2604359929731,-7.1235067377724));
#58941=CARTESIAN_POINT('Origin',(11.3307544395355,-23.5013467727236,-9.5789558981751));
#58942=CARTESIAN_POINT('Ctrl Pts',(11.664677238709,-21.6751526289,-5.84039987251776));
#58943=CARTESIAN_POINT('Ctrl Pts',(11.6681756837601,-21.6754489800181,-5.84047647114824));
#58944=CARTESIAN_POINT('Ctrl Pts',(11.6716557442406,-21.6756623521126,-5.84085486706167));
#58945=CARTESIAN_POINT('Ctrl Pts',(11.6751111337893,-21.6757948999659,-5.84152480494109));
#58946=CARTESIAN_POINT('Ctrl Pts',(11.6834492137324,-21.6761147465654,-5.84314140866023));
#58947=CARTESIAN_POINT('Ctrl Pts',(11.691252831794,-21.6759503372767,-5.84637491140676));
#58948=CARTESIAN_POINT('Ctrl Pts',(11.7091239528621,-21.6747209936006,-5.85692922382957));
#58949=CARTESIAN_POINT('Ctrl Pts',(11.718489115776,-21.6732669685549,-5.86544860786683));
#58950=CARTESIAN_POINT('Ctrl Pts',(11.7423632180107,-21.6681303692968,-5.8923813682787));
#58951=CARTESIAN_POINT('Ctrl Pts',(11.7550185107735,-21.6632424395398,-5.91454378047483));
#58952=CARTESIAN_POINT('Ctrl Pts',(11.7829456066499,-21.6493229837901,-5.97457704224912));
#58953=CARTESIAN_POINT('Ctrl Pts',(11.7977324484731,-21.6371777263082,-6.02338974579431));
#58954=CARTESIAN_POINT('Ctrl Pts',(11.8194386441992,-21.6078719961959,-6.13462845786548));
#58955=CARTESIAN_POINT('Ctrl Pts',(11.825673894872,-21.5920955534046,-6.19191044279064));
#58956=CARTESIAN_POINT('Ctrl Pts',(11.8317749863308,-21.5603242616105,-6.30356890402385));
#58957=CARTESIAN_POINT('Ctrl Pts',(11.8316012176116,-21.5432716658125,-6.3615435087185));
#58958=CARTESIAN_POINT('Ctrl Pts',(11.824941361477,-21.5096050463401,-6.47243556191196));
#58959=CARTESIAN_POINT('Ctrl Pts',(11.8183083548574,-21.491887683975,-6.52901317940878));
#58960=CARTESIAN_POINT('Ctrl Pts',(11.7958216244887,-21.4564286561109,-6.63798947479533));
#58961=CARTESIAN_POINT('Ctrl Pts',(11.780565579694,-21.4404704012144,-6.68472301424738));
#58962=CARTESIAN_POINT('Ctrl Pts',(11.7536264417728,-21.4211446949063,-6.73846169515357));
#58963=CARTESIAN_POINT('Ctrl Pts',(11.7402881749122,-21.4127521672241,-6.76120915401777));
#58964=CARTESIAN_POINT('Ctrl Pts',(11.7136982696188,-21.4020408829818,-6.7873274883819));
#58965=CARTESIAN_POINT('Ctrl Pts',(11.7035133274599,-21.398679437698,-6.79496994538256));
#58966=CARTESIAN_POINT('Ctrl Pts',(11.6842762528667,-21.3943170183098,-6.80313984330739));
#58967=CARTESIAN_POINT('Ctrl Pts',(11.6760378533013,-21.3929463221456,-6.80507051068833));
#58968=CARTESIAN_POINT('Ctrl Pts',(11.6665534479108,-21.3920199943286,-6.80524520977615));
#58969=CARTESIAN_POINT('Ctrl Pts',(11.6656136423373,-21.3919350996656,-6.80524084677675));
#58970=CARTESIAN_POINT('Ctrl Pts',(11.664677238709,-21.3918572850628,-6.80521520986104));
#58971=CARTESIAN_POINT('Origin',(11.6285182850279,-24.2604359929731,-7.1235067377724));
#58972=CARTESIAN_POINT('Origin',(1.06052702375292,-25.4510030262676,-7.47308876036671));
#58973=CARTESIAN_POINT('Origin',(1.6653400148523,-24.0613171698908,2.94666150553761E-15));
#58974=CARTESIAN_POINT('',(1.95776807072638,-21.593771336803,-0.474041419794069));
#58975=CARTESIAN_POINT('',(1.79371994466189,-21.5846216014986,-2.61616378886991E-15));
#58976=CARTESIAN_POINT('Ctrl Pts',(1.95776807072638,-21.593771336803,-0.47404141979409));
#58977=CARTESIAN_POINT('Ctrl Pts',(1.95134776803084,-21.5932099304442,-0.47402171034616));
#58978=CARTESIAN_POINT('Ctrl Pts',(1.94501646548725,-21.5926782047101,-0.473007564224911));
#58979=CARTESIAN_POINT('Ctrl Pts',(1.92951932707461,-21.5914272389869,-0.468186519780772));
#58980=CARTESIAN_POINT('Ctrl Pts',(1.92094790453018,-21.5907814463351,-0.46338067495892));
#58981=CARTESIAN_POINT('Ctrl Pts',(1.9006842838642,-21.5893333422068,-0.44803695037139));
#58982=CARTESIAN_POINT('Ctrl Pts',(1.88996070920407,-21.5886516447308,-0.435581293464189));
#58983=CARTESIAN_POINT('Ctrl Pts',(1.85988430203368,-21.586868815578,-0.392217225061399));
#58984=CARTESIAN_POINT('Ctrl Pts',(1.84552319454939,-21.5862561010085,-0.354793494139702));
#58985=CARTESIAN_POINT('Ctrl Pts',(1.82174065150218,-21.5852941592389,-0.280937783834421));
#58986=CARTESIAN_POINT('Ctrl Pts',(1.81181923278629,-21.585029713215,-0.230359404107756));
#58987=CARTESIAN_POINT('Ctrl Pts',(1.799968444636,-21.5847372703622,-0.142150220758282));
#58988=CARTESIAN_POINT('Ctrl Pts',(1.79660846342292,-21.5846751446254,-0.101128548747823));
#58989=CARTESIAN_POINT('Ctrl Pts',(1.7941317217012,-21.5846288405808,-0.0406090573298228));
#58990=CARTESIAN_POINT('Ctrl Pts',(1.7937199446619,-21.5846216014986,-0.0202986714769121));
#58991=CARTESIAN_POINT('Ctrl Pts',(1.7937199446619,-21.5846216014986,-2.58897380223162E-15));
#58992=CARTESIAN_POINT('',(1.65494820650842,-24.0600412162663,-2.52960515816076));
#58993=CARTESIAN_POINT('Origin',(1.65494820650842,-24.0600412162663,3.10139888928781E-15));
#58994=CARTESIAN_POINT('',(1.36757616935991,-24.0247563668693,-2.22978791005503));
#58995=CARTESIAN_POINT('Origin',(1.6653400148523,-24.0613171698908,-2.22978791005503));
#58996=CARTESIAN_POINT('Origin',(1.36757616935991,-24.0247563668693,2.94218409849815E-15));
#58997=CARTESIAN_POINT('',(1.95776807072638,-21.593771336803,0.474041419794074));
#58998=CARTESIAN_POINT('Origin',(1.65494820650842,-24.0600412162663,3.10139888928781E-15));
#58999=CARTESIAN_POINT('Ctrl Pts',(1.7937199446619,-21.5846216014986,-2.58897380223162E-15));
#59000=CARTESIAN_POINT('Ctrl Pts',(1.7937199446619,-21.5846216014986,0.0170010253597482));
#59001=CARTESIAN_POINT('Ctrl Pts',(1.79400880365352,-21.5846267121308,0.0339938333246223));
#59002=CARTESIAN_POINT('Ctrl Pts',(1.79594647664015,-21.5846625069698,0.0907225510823662));
#59003=CARTESIAN_POINT('Ctrl Pts',(1.79895084940682,-21.5847168190493,0.131181998467417));
#59004=CARTESIAN_POINT('Ctrl Pts',(1.80977106001253,-21.5849749085674,0.218244549034728));
#59005=CARTESIAN_POINT('Ctrl Pts',(1.81886112579789,-21.5852081198308,0.267828304156));
#59006=CARTESIAN_POINT('Ctrl Pts',(1.8416420910732,-21.5860852333225,0.344658261477164));
#59007=CARTESIAN_POINT('Ctrl Pts',(1.8579971898861,-21.5867311486231,0.391115268135561));
#59008=CARTESIAN_POINT('Ctrl Pts',(1.89263444116857,-21.5888210219462,0.438752720203498));
#59009=CARTESIAN_POINT('Ctrl Pts',(1.90520057316487,-21.58962179489,0.453157912548167));
#59010=CARTESIAN_POINT('Ctrl Pts',(1.9276047246656,-21.5912873878866,0.466915949381054));
#59011=CARTESIAN_POINT('Ctrl Pts',(1.93461040386461,-21.5918315367061,0.47007865594089));
#59012=CARTESIAN_POINT('Ctrl Pts',(1.94721684080077,-21.5928636195134,0.473331332978818));
#59013=CARTESIAN_POINT('Ctrl Pts',(1.952468820417,-21.5933079578999,0.474025151823078));
#59014=CARTESIAN_POINT('Ctrl Pts',(1.95776807072638,-21.593771336803,0.474041419794074));
#59015=CARTESIAN_POINT('Origin',(6.4980472271939,-24.6546990029305,3.01932982178803E-15));
#59016=CARTESIAN_POINT('',(11.664677238709,-22.4425874385122,-0.502773529288436));
#59017=CARTESIAN_POINT('Ctrl Pts',(11.664677238709,-22.4425874385122,-0.502773529288436));
#59018=CARTESIAN_POINT('Ctrl Pts',(8.45174540654375,-22.1616274567787,-0.493593399690551));
#59019=CARTESIAN_POINT('Ctrl Pts',(5.17782841008702,-21.875340981737,-0.483926563002776));
#59020=CARTESIAN_POINT('Ctrl Pts',(1.95776807072638,-21.593771336803,-0.474041419794072));
#59021=CARTESIAN_POINT('',(11.3203626311916,-25.2468048823457,-2.86966361147139));
#59022=CARTESIAN_POINT('Origin',(11.3203626311916,-25.2468048823457,3.26755809660714E-15));
#59023=CARTESIAN_POINT('',(11.664677238709,-22.4425874385122,0.502773529288443));
#59024=CARTESIAN_POINT('Origin',(11.3203626311916,-25.2468048823457,3.26755809660714E-15));
#59025=CARTESIAN_POINT('Ctrl Pts',(1.95776807072638,-21.593771336803,0.474041419794083));
#59026=CARTESIAN_POINT('Ctrl Pts',(5.17782840427536,-21.8753409812288,0.483926562984946));
#59027=CARTESIAN_POINT('Ctrl Pts',(8.4517454000289,-22.161627456209,0.493593399671947));
#59028=CARTESIAN_POINT('Ctrl Pts',(11.664677238709,-22.4425874385122,0.502773529288447));
#59029=CARTESIAN_POINT('Origin',(11.3307544395355,-25.2480808359702,3.09199813803845E-15));
#59030=CARTESIAN_POINT('',(11.6285182850279,-25.2846416389917,-2.56984636336567));
#59031=CARTESIAN_POINT('Origin',(11.6285182850279,-25.2846416389917,3.09647554507791E-15));
#59032=CARTESIAN_POINT('Origin',(11.3307544395355,-25.2480808359702,-2.56984636336567));
#59033=CARTESIAN_POINT('',(11.8308859678787,-22.4627598424576,-2.87010257891296E-15));
#59034=CARTESIAN_POINT('Ctrl Pts',(11.8308859678787,-22.4627598424576,-2.98931046371777E-15));
#59035=CARTESIAN_POINT('Ctrl Pts',(11.8308859678787,-22.4627598424576,-0.0309229856857021));
#59036=CARTESIAN_POINT('Ctrl Pts',(11.8300161901638,-22.4626192678459,-0.0615943949967859));
#59037=CARTESIAN_POINT('Ctrl Pts',(11.825990760224,-22.4619778159673,-0.132571716988348));
#59038=CARTESIAN_POINT('Ctrl Pts',(11.8220311067205,-22.4613492475643,-0.173539728186851));
#59039=CARTESIAN_POINT('Ctrl Pts',(11.8081497193984,-22.4592328861399,-0.268683426062508));
#59040=CARTESIAN_POINT('Ctrl Pts',(11.795461589778,-22.4573293352261,-0.327557844264764));
#59041=CARTESIAN_POINT('Ctrl Pts',(11.7672407996649,-22.4535873444032,-0.403094447780781));
#59042=CARTESIAN_POINT('Ctrl Pts',(11.7555857098412,-22.4520974558946,-0.428285481038756));
#59043=CARTESIAN_POINT('Ctrl Pts',(11.7315700529649,-22.4492776427903,-0.464161175185097));
#59044=CARTESIAN_POINT('Ctrl Pts',(11.7196350773267,-22.4479351247539,-0.478241088357663));
#59045=CARTESIAN_POINT('Ctrl Pts',(11.6975720132428,-22.4456574568071,-0.494192277150503));
#59046=CARTESIAN_POINT('Ctrl Pts',(11.6885594272652,-22.4447671654469,-0.49875486063898));
#59047=CARTESIAN_POINT('Ctrl Pts',(11.6741930061584,-22.4434324790847,-0.50222507262704));
#59048=CARTESIAN_POINT('Ctrl Pts',(11.6694225684331,-22.4430024014875,-0.502787087852407));
#59049=CARTESIAN_POINT('Ctrl Pts',(11.664677238709,-22.4425874385122,-0.502773529288413));
#59050=CARTESIAN_POINT('Ctrl Pts',(11.664677238709,-22.4425874385122,0.502773529288419));
#59051=CARTESIAN_POINT('Ctrl Pts',(11.6681753033368,-22.4428933323889,0.502783524111933));
#59052=CARTESIAN_POINT('Ctrl Pts',(11.6716553635687,-22.4432046663249,0.502480637546269));
#59053=CARTESIAN_POINT('Ctrl Pts',(11.6751111337893,-22.4435206231749,0.50187511320202));
#59054=CARTESIAN_POINT('Ctrl Pts',(11.6835623119453,-22.4442933040705,0.500394287283531));
#59055=CARTESIAN_POINT('Ctrl Pts',(11.691384091347,-22.4450491314624,0.497199786883784));
#59056=CARTESIAN_POINT('Ctrl Pts',(11.7094694893507,-22.4468652011622,0.486572040199528));
#59057=CARTESIAN_POINT('Ctrl Pts',(11.7189285997145,-22.4478827563863,0.477782875801506));
#59058=CARTESIAN_POINT('Ctrl Pts',(11.7437048785722,-22.4506469894916,0.449218987208414));
#59059=CARTESIAN_POINT('Ctrl Pts',(11.756758696355,-22.4522625711256,0.425077089680007));
#59060=CARTESIAN_POINT('Ctrl Pts',(11.7862943788245,-22.4560498423181,0.357948221183704));
#59061=CARTESIAN_POINT('Ctrl Pts',(11.8016138506642,-22.4582634908384,0.301713314632811));
#59062=CARTESIAN_POINT('Ctrl Pts',(11.8195646608092,-22.4609621241242,0.195134214413126));
#59063=CARTESIAN_POINT('Ctrl Pts',(11.8242738201003,-22.4617066134238,0.151903163592283));
#59064=CARTESIAN_POINT('Ctrl Pts',(11.8295027526625,-22.46253623103,0.0759831017665234));
#59065=CARTESIAN_POINT('Ctrl Pts',(11.830683585196,-22.4627272832912,0.0420217792041652));
#59066=CARTESIAN_POINT('Ctrl Pts',(11.830878013723,-22.462758562633,0.00591621364952152));
#59067=CARTESIAN_POINT('Ctrl Pts',(11.8308859678787,-22.4627598424576,0.00295695664177951));
#59068=CARTESIAN_POINT('Ctrl Pts',(11.8308859678787,-22.4627598424576,-2.98931046371777E-15));
#59069=CARTESIAN_POINT('Origin',(11.6285182850279,-25.2846416389917,3.09647554507791E-15));
#59070=CARTESIAN_POINT('Origin',(1.06052702375292,-26.5254709791062,3.24843331304384E-15));
#59071=CARTESIAN_POINT('Origin',(1.6653400148523,-23.0866647604201,6.77885640724594));
#59072=CARTESIAN_POINT('',(1.95776807072638,-20.8526247727479,5.62882899907204));
#59073=CARTESIAN_POINT('',(1.95776807072638,-20.5855189702533,6.53850782206133));
#59074=CARTESIAN_POINT('Ctrl Pts',(1.95776807072638,-20.8526247727479,5.62882899907204));
#59075=CARTESIAN_POINT('Ctrl Pts',(1.95134808328295,-20.8520805812205,5.62868975053771));
#59076=CARTESIAN_POINT('Ctrl Pts',(1.94501708192101,-20.8512847271148,5.62951292437162));
#59077=CARTESIAN_POINT('Ctrl Pts',(1.92954226703916,-20.8487299346933,5.63377986718257));
#59078=CARTESIAN_POINT('Ctrl Pts',(1.92098940734792,-20.846762080117,5.63819408082297));
#59079=CARTESIAN_POINT('Ctrl Pts',(1.90083817144993,-20.8410870108723,5.65240862845604));
#59080=CARTESIAN_POINT('Ctrl Pts',(1.89018614013894,-20.8369650214871,5.66403990652636));
#59081=CARTESIAN_POINT('Ctrl Pts',(1.86077829278984,-20.8234001483423,5.70403903581996));
#59082=CARTESIAN_POINT('Ctrl Pts',(1.8466574587581,-20.8126796100708,5.7383751987311));
#59083=CARTESIAN_POINT('Ctrl Pts',(1.82247517384463,-20.7910284502593,5.8085954607679));
#59084=CARTESIAN_POINT('Ctrl Pts',(1.81230887643079,-20.77639027532,5.8574791465412));
#59085=CARTESIAN_POINT('Ctrl Pts',(1.79934881945839,-20.7493484902482,5.94843125986021));
#59086=CARTESIAN_POINT('Ctrl Pts',(1.79572382774438,-20.7358065149758,5.99432875767835));
#59087=CARTESIAN_POINT('Ctrl Pts',(1.79301769946659,-20.7096735628705,6.08315330649572));
#59088=CARTESIAN_POINT('Ctrl Pts',(1.7937822286142,-20.6965268005168,6.12796795344078));
#59089=CARTESIAN_POINT('Ctrl Pts',(1.7998218767276,-20.6703299712458,6.21760963952165));
#59090=CARTESIAN_POINT('Ctrl Pts',(1.80545072973152,-20.6566260406547,6.2646781889035));
#59091=CARTESIAN_POINT('Ctrl Pts',(1.82510992022243,-20.6280881697271,6.36393040202843));
#59092=CARTESIAN_POINT('Ctrl Pts',(1.83960979646987,-20.6150406765513,6.410207996633));
#59093=CARTESIAN_POINT('Ctrl Pts',(1.86695154341405,-20.5997934931318,6.46695055008921));
#59094=CARTESIAN_POINT('Ctrl Pts',(1.88252298601552,-20.5925565805734,6.49448704979649));
#59095=CARTESIAN_POINT('Ctrl Pts',(1.91281431353043,-20.5866187437543,6.52203861054359));
#59096=CARTESIAN_POINT('Ctrl Pts',(1.922534415008,-20.5853643741092,6.5288067800109));
#59097=CARTESIAN_POINT('Ctrl Pts',(1.9381393331208,-20.5847740821371,6.53517979671659));
#59098=CARTESIAN_POINT('Ctrl Pts',(1.94311288783888,-20.5847624336121,6.53665410256502));
#59099=CARTESIAN_POINT('Ctrl Pts',(1.95140011070329,-20.5850644551011,6.53809843287623));
#59100=CARTESIAN_POINT('Ctrl Pts',(1.95458052118134,-20.5852542906722,6.53841990667583));
#59101=CARTESIAN_POINT('Ctrl Pts',(1.95776807072638,-20.5855189702533,6.53850782206133));
#59102=CARTESIAN_POINT('',(1.65494820650842,-23.7981126208907,4.35135855429466));
#59103=CARTESIAN_POINT('Origin',(1.65494820650842,-23.0854404918828,6.7784969295689));
#59104=CARTESIAN_POINT('',(1.36757616935991,-23.6797887759252,4.62909020638214));
#59105=CARTESIAN_POINT('Origin',(1.6653400148523,-23.714868609534,4.63939057489758));
#59106=CARTESIAN_POINT('Origin',(1.36757616935991,-23.0515849268112,6.7685560387305));
#59107=CARTESIAN_POINT('Origin',(1.65494820650842,-23.0854404918828,6.7784969295689));
#59108=CARTESIAN_POINT('Origin',(6.4980472271939,-23.6560104598922,6.94603138825146));
#59109=CARTESIAN_POINT('',(11.664677238709,-21.6751526289,5.84039987251778));
#59110=CARTESIAN_POINT('Ctrl Pts',(11.664677238709,-21.6751526289,5.84039987251777));
#59111=CARTESIAN_POINT('Ctrl Pts',(8.45037669575292,-21.402871216531,5.77002260034827));
#59112=CARTESIAN_POINT('Ctrl Pts',(5.17722936343352,-21.1255230570061,5.69865861638707));
#59113=CARTESIAN_POINT('Ctrl Pts',(1.95776807072638,-20.8526247727479,5.62882899907203));
#59114=CARTESIAN_POINT('',(11.3203626311916,-25.0326095573615,4.35942481973593));
#59115=CARTESIAN_POINT('Origin',(11.3203626311916,-24.2241318908269,7.11284689157994));
#59116=CARTESIAN_POINT('',(11.664677238709,-21.3918572850628,6.805215209861));
#59117=CARTESIAN_POINT('Origin',(11.3203626311916,-24.2241318908269,7.11284689157994));
#59118=CARTESIAN_POINT('Ctrl Pts',(1.95776807072638,-20.5855189702533,6.53850782206134));
#59119=CARTESIAN_POINT('Ctrl Pts',(5.17722935754855,-20.8528483568881,6.62730336112004));
#59120=CARTESIAN_POINT('Ctrl Pts',(8.45037668926196,-21.1247507584877,6.71721389316576));
#59121=CARTESIAN_POINT('Ctrl Pts',(11.664677238709,-21.3918572850628,6.805215209861));
#59122=CARTESIAN_POINT('Origin',(11.3307544395355,-24.2253561593642,7.11320636925698));
#59123=CARTESIAN_POINT('',(11.6285182850279,-24.9844453796138,4.65775720885429));
#59124=CARTESIAN_POINT('Origin',(11.6285182850279,-24.2604359929731,7.12350673777241));
#59125=CARTESIAN_POINT('Origin',(11.3307544395355,-24.9493655460049,4.64745684033885));
#59126=CARTESIAN_POINT('Ctrl Pts',(11.664677238709,-21.3918572850628,6.805215209861));
#59127=CARTESIAN_POINT('Ctrl Pts',(11.6681756837601,-21.392148003834,6.80531099050321));
#59128=CARTESIAN_POINT('Ctrl Pts',(11.6716557442406,-21.3925320801382,6.80510802126781));
#59129=CARTESIAN_POINT('Ctrl Pts',(11.6751111337893,-21.3930057822509,6.80461609443974));
#59130=CARTESIAN_POINT('Ctrl Pts',(11.6834492137325,-21.394148856289,6.80342904297686));
#59131=CARTESIAN_POINT('Ctrl Pts',(11.6912528317941,-21.3957587099622,6.80061996099559));
#59132=CARTESIAN_POINT('Ctrl Pts',(11.709123952862,-21.4004306123475,6.79107647501339));
#59133=CARTESIAN_POINT('Ctrl Pts',(11.7184891157759,-21.403813335391,6.78312340780531));
#59134=CARTESIAN_POINT('Ctrl Pts',(11.7423632180108,-21.4140531027239,6.75768907273794));
#59135=CARTESIAN_POINT('Ctrl Pts',(11.7550185107736,-21.4219230191941,6.73640225084234));
#59136=CARTESIAN_POINT('Ctrl Pts',(11.7829456066499,-21.4426696595898,6.6783736313523));
#59137=CARTESIAN_POINT('Ctrl Pts',(11.7977324484731,-21.4588425587729,6.63074355011461));
#59138=CARTESIAN_POINT('Ctrl Pts',(11.8194386441992,-21.4943291980106,6.52131971671298));
#59139=CARTESIAN_POINT('Ctrl Pts',(11.825673894872,-21.5120261889324,6.46460165559978));
#59140=CARTESIAN_POINT('Ctrl Pts',(11.8317749863308,-21.5456655992248,6.35349172344992));
#59141=CARTESIAN_POINT('Ctrl Pts',(11.8316012176116,-21.5626634804396,6.29550105310408));
#59142=CARTESIAN_POINT('Ctrl Pts',(11.824941361477,-21.5942940881578,6.18401117291958));
#59143=CARTESIAN_POINT('Ctrl Pts',(11.8183083548574,-21.6099774638489,6.12683632304897));
#59144=CARTESIAN_POINT('Ctrl Pts',(11.795821624489,-21.6390644648082,6.01598903175088));
#59145=CARTESIAN_POINT('Ctrl Pts',(11.7805655796943,-21.6509055854708,5.96804659261232));
#59146=CARTESIAN_POINT('Ctrl Pts',(11.7536264417728,-21.6637010911389,5.91239047179329));
#59147=CARTESIAN_POINT('Ctrl Pts',(11.7402881749122,-21.6689390523323,5.88871674863418));
#59148=CARTESIAN_POINT('Ctrl Pts',(11.7136982696187,-21.6740487842635,5.86095365010984));
#59149=CARTESIAN_POINT('Ctrl Pts',(11.7035133274599,-21.6753527807432,5.85270707163255));
#59150=CARTESIAN_POINT('Ctrl Pts',(11.6842762528667,-21.6760998603139,5.84347561415638));
#59151=CARTESIAN_POINT('Ctrl Pts',(11.6760378533013,-21.6759905549143,5.84111037910665));
#59152=CARTESIAN_POINT('Ctrl Pts',(11.6665534479108,-21.6753057278234,5.84046260225363));
#59153=CARTESIAN_POINT('Ctrl Pts',(11.6656136423373,-21.6752319510726,5.84042037512235));
#59154=CARTESIAN_POINT('Ctrl Pts',(11.664677238709,-21.6751526289,5.84039987251778));
#59155=CARTESIAN_POINT('Origin',(11.6285182850279,-24.2604359929731,7.12350673777241));
#59156=CARTESIAN_POINT('Origin',(1.06052702375292,-25.4510030262676,7.47308876036672));
#59157=CARTESIAN_POINT('Origin',(1.6653400148523,-20.2416680737422,13.0085301837882));
#59158=CARTESIAN_POINT('',(1.95776807072638,-18.4221225649395,11.2756851683684));
#59159=CARTESIAN_POINT('',(1.95776807072638,-17.9095502835289,12.0732632065885));
#59160=CARTESIAN_POINT('Ctrl Pts',(1.95776807072638,-18.4221225649395,11.2756851683684));
#59161=CARTESIAN_POINT('Ctrl Pts',(1.95134736183191,-18.4216395935701,11.2753982116643));
#59162=CARTESIAN_POINT('Ctrl Pts',(1.94501567125517,-18.4206438937256,11.2759639830883));
#59163=CARTESIAN_POINT('Ctrl Pts',(1.92948836979317,-18.4169777842864,11.2793502116274));
#59164=CARTESIAN_POINT('Ctrl Pts',(1.9208918623398,-18.4138230903949,11.2830613241242));
#59165=CARTESIAN_POINT('Ctrl Pts',(1.90046800930186,-18.4042191176333,11.2953067736052));
#59166=CARTESIAN_POINT('Ctrl Pts',(1.88964186308612,-18.3968030080762,11.3055760598059));
#59167=CARTESIAN_POINT('Ctrl Pts',(1.85810283833502,-18.3704851710237,11.3430782725479));
#59168=CARTESIAN_POINT('Ctrl Pts',(1.8433562930371,-18.3481042542488,11.3767845480151));
#59169=CARTESIAN_POINT('Ctrl Pts',(1.81854010589205,-18.304034165225,11.4435429822473));
#59170=CARTESIAN_POINT('Ctrl Pts',(1.8083691782649,-18.2726985595794,11.4918522175932));
#59171=CARTESIAN_POINT('Ctrl Pts',(1.79896764765296,-18.2274018269571,11.5619364610537));
#59172=CARTESIAN_POINT('Ctrl Pts',(1.79670145400061,-18.2114630036213,11.5866568740703));
#59173=CARTESIAN_POINT('Ctrl Pts',(1.79434535609113,-18.1842435918483,11.6289286489356));
#59174=CARTESIAN_POINT('Ctrl Pts',(1.79381557303812,-18.1727761179962,11.6467551189356));
#59175=CARTESIAN_POINT('Ctrl Pts',(1.79365032105971,-18.1502654058706,11.6817769814635));
#59176=CARTESIAN_POINT('Ctrl Pts',(1.79398945985934,-18.1391347052042,11.6991076651001));
#59177=CARTESIAN_POINT('Ctrl Pts',(1.79575501944578,-18.1136547229072,11.7388159539009));
#59178=CARTESIAN_POINT('Ctrl Pts',(1.79749007695648,-18.0991705776079,11.7614139961321));
#59179=CARTESIAN_POINT('Ctrl Pts',(1.80455267776983,-18.0593401605001,11.8236744660528));
#59180=CARTESIAN_POINT('Ctrl Pts',(1.81186451913785,-18.0330203540242,11.8649367864125));
#59181=CARTESIAN_POINT('Ctrl Pts',(1.8357835522891,-17.9799323185448,11.9490437490344));
#59182=CARTESIAN_POINT('Ctrl Pts',(1.85214505346243,-17.957095277983,11.9858397344708));
#59183=CARTESIAN_POINT('Ctrl Pts',(1.88061329933065,-17.9321806919618,12.027521920884));
#59184=CARTESIAN_POINT('Ctrl Pts',(1.89448595076313,-17.9221533057532,12.0446318207664));
#59185=CARTESIAN_POINT('Ctrl Pts',(1.92022261571912,-17.9130069990607,12.0622553637802));
#59186=CARTESIAN_POINT('Ctrl Pts',(1.92864558703565,-17.91092340545,12.0666669158279));
#59187=CARTESIAN_POINT('Ctrl Pts',(1.94192278721254,-17.9094652452642,12.0709092294435));
#59188=CARTESIAN_POINT('Ctrl Pts',(1.94616291414725,-17.9092382087298,12.0719097149397));
#59189=CARTESIAN_POINT('Ctrl Pts',(1.95291207286072,-17.9092807395709,12.0729030082265));
#59190=CARTESIAN_POINT('Ctrl Pts',(1.95533909578542,-17.9093756366037,12.073142104124));
#59191=CARTESIAN_POINT('Ctrl Pts',(1.95776807072638,-17.9095502835289,12.0732632065885));
#59192=CARTESIAN_POINT('',(1.65494820650842,-21.6082024737958,10.8798010752069));
#59193=CARTESIAN_POINT('Origin',(1.65494820650842,-20.2405946732479,13.0078403511776));
#59194=CARTESIAN_POINT('',(1.36757616935991,-21.416425527482,11.1129469645577));
#59195=CARTESIAN_POINT('Origin',(1.6653400148523,-21.447182432187,11.1327132269901));
#59196=CARTESIAN_POINT('Origin',(1.36757616935991,-20.2109111690372,12.9887639213558));
#59197=CARTESIAN_POINT('Origin',(1.65494820650842,-20.2405946732479,13.0078403511776));
#59198=CARTESIAN_POINT('Origin',(6.4980472271939,-20.7408526371047,13.3293366230661));
#59199=CARTESIAN_POINT('',(11.664677238709,-19.1517258603906,11.7104188108481));
#59200=CARTESIAN_POINT('Ctrl Pts',(11.664677238709,-19.1517258603906,11.7104188108481));
#59201=CARTESIAN_POINT('Ctrl Pts',(8.44760841234032,-18.9100934028027,11.566057551542));
#59202=CARTESIAN_POINT('Ctrl Pts',(5.17558411912346,-18.6641695178434,11.4194969970449));
#59203=CARTESIAN_POINT('Ctrl Pts',(1.95776807072638,-18.4221225649395,11.2756851683684));
#59204=CARTESIAN_POINT('',(11.3203626311916,-22.7904210807013,11.2353385785459));
#59205=CARTESIAN_POINT('Origin',(11.3203626311916,-21.2389637999728,13.6494532297333));
#59206=CARTESIAN_POINT('',(11.664677238709,-18.6080860766515,12.5563388263039));
#59207=CARTESIAN_POINT('Origin',(11.3203626311916,-21.2389637999728,13.6494532297333));
#59208=CARTESIAN_POINT('Ctrl Pts',(1.95776807072638,-17.9095502835289,12.0732632065885));
#59209=CARTESIAN_POINT('Ctrl Pts',(5.17558411308691,-18.1409160618572,12.2336952663475));
#59210=CARTESIAN_POINT('Ctrl Pts',(8.44760840593807,-18.3763927053254,12.3965120458593));
#59211=CARTESIAN_POINT('Ctrl Pts',(11.664677238709,-18.6080860766515,12.5563388263038));
#59212=CARTESIAN_POINT('Origin',(11.3307544395355,-21.2400372004671,13.6501430623439));
#59213=CARTESIAN_POINT('',(11.6285182850279,-22.6601579437975,11.5080169927616));
#59214=CARTESIAN_POINT('Origin',(11.6285182850279,-21.2707941051722,13.6699093247763));
#59215=CARTESIAN_POINT('Origin',(11.3307544395355,-22.6294010390924,11.4882507303292));
#59216=CARTESIAN_POINT('Ctrl Pts',(11.664677238709,-18.6080860766515,12.5563388263039));
#59217=CARTESIAN_POINT('Ctrl Pts',(11.6681719057553,-18.6083377626526,12.5565124444052));
#59218=CARTESIAN_POINT('Ctrl Pts',(11.6716519636861,-18.6087630873824,12.5564264617449));
#59219=CARTESIAN_POINT('Ctrl Pts',(11.6751111337893,-18.6093568419532,12.5560875483161));
#59220=CARTESIAN_POINT('Ctrl Pts',(11.6833639439589,-18.6107734082434,12.5552789762861));
#59221=CARTESIAN_POINT('Ctrl Pts',(11.6912209922801,-18.6131029323726,12.5530553109812));
#59222=CARTESIAN_POINT('Ctrl Pts',(11.7092716451021,-18.6203670705107,12.5451050615273));
#59223=CARTESIAN_POINT('Ctrl Pts',(11.7188321121789,-18.6259692752841,12.5382858333101));
#59224=CARTESIAN_POINT('Ctrl Pts',(11.7448362096952,-18.6446600490307,12.5145712192167));
#59225=CARTESIAN_POINT('Ctrl Pts',(11.7582763496126,-18.6601414182568,12.4935901023805));
#59226=CARTESIAN_POINT('Ctrl Pts',(11.7901173768953,-18.7031288181134,12.4342691481542));
#59227=CARTESIAN_POINT('Ctrl Pts',(11.8074969006879,-18.7427730168715,12.3773456251793));
#59228=CARTESIAN_POINT('Ctrl Pts',(11.8229354401012,-18.807249025111,12.2814049176088));
#59229=CARTESIAN_POINT('Ctrl Pts',(11.826199199177,-18.8268628597469,12.2518426658347));
#59230=CARTESIAN_POINT('Ctrl Pts',(11.8295237141305,-18.8585151047524,12.2035704025212));
#59231=CARTESIAN_POINT('Ctrl Pts',(11.8303434615844,-18.8708529717768,12.1846162306134));
#59232=CARTESIAN_POINT('Ctrl Pts',(11.8309946485842,-18.893887321558,12.1489677324934));
#59233=CARTESIAN_POINT('Ctrl Pts',(11.8309459330901,-18.9046640233566,12.1321843072664));
#59234=CARTESIAN_POINT('Ctrl Pts',(11.8300359252892,-18.9280174953953,12.0955751475504));
#59235=CARTESIAN_POINT('Ctrl Pts',(11.8290394062419,-18.9406788268584,12.0755774687241));
#59236=CARTESIAN_POINT('Ctrl Pts',(11.8249644421306,-18.9736962566426,12.023004023433));
#59237=CARTESIAN_POINT('Ctrl Pts',(11.8209395722477,-18.9943695927783,11.9896581821858));
#59238=CARTESIAN_POINT('Ctrl Pts',(11.8028867656276,-19.055690107089,11.8891741309911));
#59239=CARTESIAN_POINT('Ctrl Pts',(11.7841990134599,-19.0898144719036,11.8310409211087));
#59240=CARTESIAN_POINT('Ctrl Pts',(11.7507704380578,-19.1229326946464,11.7717678295026));
#59241=CARTESIAN_POINT('Ctrl Pts',(11.737145998644,-19.1343448984334,11.7509308503555));
#59242=CARTESIAN_POINT('Ctrl Pts',(11.7101248465183,-19.1461490561111,11.7271518112195));
#59243=CARTESIAN_POINT('Ctrl Pts',(11.700195678653,-19.1493048584522,11.7203319567739));
#59244=CARTESIAN_POINT('Ctrl Pts',(11.6812735959897,-19.1520152885414,11.7127291553659));
#59245=CARTESIAN_POINT('Ctrl Pts',(11.6731643433663,-19.1523622516496,11.7108014088155));
#59246=CARTESIAN_POINT('Ctrl Pts',(11.6646867061662,-19.1517265711868,11.7104192361762));
#59247=CARTESIAN_POINT('Ctrl Pts',(11.6646819724071,-19.1517262159363,11.7104190232658));
#59248=CARTESIAN_POINT('Ctrl Pts',(11.664677238709,-19.1517258603906,11.7104188108481));
#59249=CARTESIAN_POINT('Origin',(11.6285182850279,-21.2707941051722,13.6699093247763));
#59250=CARTESIAN_POINT('Origin',(1.06052702375292,-22.314646171184,14.3407523135387));
#59251=CARTESIAN_POINT('Origin',(1.6653400148523,-15.756811821565,18.1843302095478));
#59252=CARTESIAN_POINT('',(1.95776807072638,-14.4991695475011,16.0090523844052));
#59253=CARTESIAN_POINT('',(1.95776807072638,-13.7826563450298,16.6299146085789));
#59254=CARTESIAN_POINT('Ctrl Pts',(1.95776807072638,-14.4991695475011,16.0090523844052));
#59255=CARTESIAN_POINT('Ctrl Pts',(1.95134736178518,-14.4987869849089,16.0086409827022));
#59256=CARTESIAN_POINT('Ctrl Pts',(1.94501567118224,-14.4976722216562,16.0089033153585));
#59257=CARTESIAN_POINT('Ctrl Pts',(1.92948836979211,-14.493200604605,16.0111195154527));
#59258=CARTESIAN_POINT('Ctrl Pts',(1.9208918623387,-14.4891281567696,16.0137915218418));
#59259=CARTESIAN_POINT('Ctrl Pts',(1.90046800930049,-14.4764632705936,16.0228351927759));
#59260=CARTESIAN_POINT('Ctrl Pts',(1.8896418630846,-14.4664543733233,16.0305991412226));
#59261=CARTESIAN_POINT('Ctrl Pts',(1.85810283833289,-14.4306369993061,16.0591676593216));
#59262=CARTESIAN_POINT('Ctrl Pts',(1.84335629303482,-14.3996665117469,16.085203160893));
#59263=CARTESIAN_POINT('Ctrl Pts',(1.81854010589082,-14.338573546615,16.1368414306076));
#59264=CARTESIAN_POINT('Ctrl Pts',(1.80836917826421,-14.2948969687822,16.1743655421829));
#59265=CARTESIAN_POINT('Ctrl Pts',(1.7989676476527,-14.2316900590003,16.2288493170451));
#59266=CARTESIAN_POINT('Ctrl Pts',(1.79670145400044,-14.2094323248369,16.2480778941875));
#59267=CARTESIAN_POINT('Ctrl Pts',(1.79434535609105,-14.1714061552799,16.2809687706783));
#59268=CARTESIAN_POINT('Ctrl Pts',(1.79381557303809,-14.1553808977212,16.2948423826588));
#59269=CARTESIAN_POINT('Ctrl Pts',(1.79365032105973,-14.123915228731,16.3221036131932));
#59270=CARTESIAN_POINT('Ctrl Pts',(1.79398945985937,-14.1083527818371,16.3355964016126));
#59271=CARTESIAN_POINT('Ctrl Pts',(1.79575501944591,-14.0727178001231,16.3665176851508));
#59272=CARTESIAN_POINT('Ctrl Pts',(1.79749007695668,-14.052453760262,16.3841196926005));
#59273=CARTESIAN_POINT('Ctrl Pts',(1.80455267777036,-13.996695953529,16.4326366507725));
#59274=CARTESIAN_POINT('Ctrl Pts',(1.81186451913875,-13.9598173451314,16.4648124108593));
#59275=CARTESIAN_POINT('Ctrl Pts',(1.8357835522914,-13.8851840784767,16.5305558225553));
#59276=CARTESIAN_POINT('Ctrl Pts',(1.85214505346569,-13.852905471461,16.5594273742107));
#59277=CARTESIAN_POINT('Ctrl Pts',(1.88061329933481,-13.8172568722815,16.5924018891755));
#59278=CARTESIAN_POINT('Ctrl Pts',(1.89448595076677,-13.8028152498312,16.6059936767355));
#59279=CARTESIAN_POINT('Ctrl Pts',(1.9202226157215,-13.7890743069931,16.6203265300558));
#59280=CARTESIAN_POINT('Ctrl Pts',(1.92864558703758,-13.7858322357261,16.6239723670925));
#59281=CARTESIAN_POINT('Ctrl Pts',(1.94192278721349,-13.783237943412,16.6276320260006));
#59282=CARTESIAN_POINT('Ctrl Pts',(1.94616291414808,-13.7827382341156,16.6285280212211));
#59283=CARTESIAN_POINT('Ctrl Pts',(1.95291207283927,-13.7824991991022,16.6294930614699));
#59284=CARTESIAN_POINT('Ctrl Pts',(1.9553390957689,-13.7825228910382,16.6297492078892));
#59285=CARTESIAN_POINT('Ctrl Pts',(1.95776807072638,-13.7826563450298,16.6299146085789));
#59286=CARTESIAN_POINT('',(1.65494820650842,-17.6677242712023,16.5268268176743));
#59287=CARTESIAN_POINT('Origin',(1.65494820650842,-15.755976249638,18.1833659081392));
#59288=CARTESIAN_POINT('',(1.36757616935991,-17.418030851189,16.6964988509053));
#59289=CARTESIAN_POINT('Origin',(1.6653400148523,-17.4419730854894,16.7241296622268));
#59290=CARTESIAN_POINT('Origin',(1.36757616935991,-15.7328695872647,18.1566993982262));
#59291=CARTESIAN_POINT('Origin',(1.65494820650842,-15.755976249638,18.1833659081392));
#59292=CARTESIAN_POINT('Origin',(6.4980472271939,-16.1453942842592,18.6327782772971));
#59293=CARTESIAN_POINT('',(11.664677238709,-15.0767401623716,16.6317292616657));
#59294=CARTESIAN_POINT('Ctrl Pts',(11.664677238709,-15.0767401623716,16.6317292616657));
#59295=CARTESIAN_POINT('Ctrl Pts',(8.44646649976651,-14.8854989259897,16.425066587821));
#59296=CARTESIAN_POINT('Ctrl Pts',(5.17487115867276,-14.6908529438561,16.2151856480993));
#59297=CARTESIAN_POINT('Ctrl Pts',(1.95776807072638,-14.4991695475011,16.0090523844052));
#59298=CARTESIAN_POINT('',(11.3203626311916,-18.7018882279357,17.2010320248535));
#59299=CARTESIAN_POINT('Origin',(11.3203626311916,-16.5331411750263,19.0802620436378));
#59300=CARTESIAN_POINT('',(11.664677238709,-14.316798400859,17.2902225464619));
#59301=CARTESIAN_POINT('Origin',(11.3203626311916,-16.5331411750263,19.0802620436378));
#59302=CARTESIAN_POINT('Ctrl Pts',(1.95776807072638,-13.7826563450298,16.6299146085789));
#59303=CARTESIAN_POINT('Ctrl Pts',(5.17487115257265,-13.959412077432,16.8489827660136));
#59304=CARTESIAN_POINT('Ctrl Pts',(8.44646649340719,-14.1394557203275,17.0715167046817));
#59305=CARTESIAN_POINT('Ctrl Pts',(11.664677238709,-14.316798400859,17.2902225464619));
#59306=CARTESIAN_POINT('Origin',(11.3307544395355,-16.5339767469533,19.0812263450464));
#59307=CARTESIAN_POINT('',(11.6285182850279,-18.5000792765231,17.4259656807277));
#59308=CARTESIAN_POINT('Origin',(11.6285182850279,-16.5579189812536,19.1088571563679));
#59309=CARTESIAN_POINT('Origin',(11.3307544395355,-18.4761370422228,17.3983348694061));
#59310=CARTESIAN_POINT('Ctrl Pts',(11.664677238709,-14.316798400859,17.2902225464619));
#59311=CARTESIAN_POINT('Ctrl Pts',(11.6681719057554,-14.316990977937,17.2904600399508));
#59312=CARTESIAN_POINT('Ctrl Pts',(11.6716519636863,-14.3174232981415,17.2904973680161));
#59313=CARTESIAN_POINT('Ctrl Pts',(11.6751111337893,-14.318088484427,17.2903394629558));
#59314=CARTESIAN_POINT('Ctrl Pts',(11.6833639439589,-14.3196754708945,17.2899627366173));
#59315=CARTESIAN_POINT('Ctrl Pts',(11.6912209922801,-14.3225371118403,17.2884854481707));
#59316=CARTESIAN_POINT('Ctrl Pts',(11.7092716451021,-14.3317468454494,17.282903783892));
#59317=CARTESIAN_POINT('Ctrl Pts',(11.7188321121789,-14.3390433201674,17.2779391058069));
#59318=CARTESIAN_POINT('Ctrl Pts',(11.744836209695,-14.3636581651116,17.2604508996895));
#59319=CARTESIAN_POINT('Ctrl Pts',(11.7582763496125,-14.3844234937974,17.2446812712422));
#59320=CARTESIAN_POINT('Ctrl Pts',(11.7901173768953,-14.4423822460226,17.1998741825471));
#59321=CARTESIAN_POINT('Ctrl Pts',(11.8074969006879,-14.4964577858478,17.1564255236994));
#59322=CARTESIAN_POINT('Ctrl Pts',(11.8229354401012,-14.5853516835692,17.0825360795582));
#59323=CARTESIAN_POINT('Ctrl Pts',(11.826199199177,-14.6124996688663,17.0596971624782));
#59324=CARTESIAN_POINT('Ctrl Pts',(11.8295237141305,-14.6564696437161,17.0222977329235));
#59325=CARTESIAN_POINT('Ctrl Pts',(11.8303434615844,-14.6736477477498,17.00758731698));
#59326=CARTESIAN_POINT('Ctrl Pts',(11.8309946485842,-14.7057923870393,16.9798723597733));
#59327=CARTESIAN_POINT('Ctrl Pts',(11.8309459330901,-14.7208609939957,16.9668049289467));
#59328=CARTESIAN_POINT('Ctrl Pts',(11.8300359252892,-14.753582478497,16.9382581308177));
#59329=CARTESIAN_POINT('Ctrl Pts',(11.8290394062419,-14.7713649342591,16.9226376077815));
#59330=CARTESIAN_POINT('Ctrl Pts',(11.8249644421306,-14.8178565773075,16.8814958413395));
#59331=CARTESIAN_POINT('Ctrl Pts',(11.8209395722478,-14.8470871071856,16.8553250928115));
#59332=CARTESIAN_POINT('Ctrl Pts',(11.8028867656276,-14.9342333384702,16.7761873370133));
#59333=CARTESIAN_POINT('Ctrl Pts',(11.7841990134599,-14.9833534445964,16.7300228751473));
#59334=CARTESIAN_POINT('Ctrl Pts',(11.7507704380578,-15.0318293062667,16.6824812417983));
#59335=CARTESIAN_POINT('Ctrl Pts',(11.7371459986441,-15.0486496910257,16.6657034960674));
#59336=CARTESIAN_POINT('Ctrl Pts',(11.7101248465184,-15.0666750268719,16.646213290621));
#59337=CARTESIAN_POINT('Ctrl Pts',(11.700195678653,-15.0716243720746,16.6405587804617));
#59338=CARTESIAN_POINT('Ctrl Pts',(11.6812735959896,-15.0763669673805,16.6340275623301));
#59339=CARTESIAN_POINT('Ctrl Pts',(11.6731643433662,-15.0772429850095,16.6322756538638));
#59340=CARTESIAN_POINT('Ctrl Pts',(11.6646867061662,-15.0767407245468,16.6317298700195));
#59341=CARTESIAN_POINT('Ctrl Pts',(11.6646819724071,-15.0767404436703,16.6317295656479));
#59342=CARTESIAN_POINT('Ctrl Pts',(11.664677238709,-15.0767401623716,16.6317292616657));
#59343=CARTESIAN_POINT('Origin',(11.6285182850279,-16.5579189812536,19.1088571563679));
#59344=CARTESIAN_POINT('Origin',(1.06052702375292,-17.3704893936218,20.0466134020057));
#59345=CARTESIAN_POINT('Origin',(1.6653400148523,-9.99543238497271,21.8869439481057));
#59346=CARTESIAN_POINT('',(1.95776807072638,-9.40158004320575,19.4454613857581));
#59347=CARTESIAN_POINT('',(1.95776807072638,-8.5391735580698,19.8393092308925));
#59348=CARTESIAN_POINT('Ctrl Pts',(1.95776807072638,-9.40158004320576,19.4454613857581));
#59349=CARTESIAN_POINT('Ctrl Pts',(1.95134736181189,-9.40132888234126,19.4449588683795));
#59350=CARTESIAN_POINT('Ctrl Pts',(1.94501567122392,-9.40018536719516,19.4448965096142));
#59351=CARTESIAN_POINT('Ctrl Pts',(1.92948836979269,-9.39527050632193,19.4457631379299));
#59352=CARTESIAN_POINT('Ctrl Pts',(1.92089186233927,-9.39061023004665,19.4471795681443));
#59353=CARTESIAN_POINT('Ctrl Pts',(1.90046800930126,-9.37591046421397,19.4522887960967));
#59354=CARTESIAN_POINT('Ctrl Pts',(1.88964186308544,-9.36411964056273,19.4569184178596));
#59355=CARTESIAN_POINT('Ctrl Pts',(1.85810283833409,-9.32170444021175,19.4742387898804));
#59356=CARTESIAN_POINT('Ctrl Pts',(1.8433562930361,-9.28465342658408,19.4904942760555));
#59357=CARTESIAN_POINT('Ctrl Pts',(1.81854010589152,-9.21148697404528,19.5228289557446));
#59358=CARTESIAN_POINT('Ctrl Pts',(1.80836917826461,-9.15900784060505,19.5465279631957));
#59359=CARTESIAN_POINT('Ctrl Pts',(1.79896764765285,-9.08301140158625,19.5809973180493));
#59360=CARTESIAN_POINT('Ctrl Pts',(1.79670145400053,-9.05623794584491,19.5931762743549));
#59361=CARTESIAN_POINT('Ctrl Pts',(1.79434535609109,-9.01048567261076,19.6140216292678));
#59362=CARTESIAN_POINT('Ctrl Pts',(1.7938155730381,-8.99120090240678,19.6228184256957));
#59363=CARTESIAN_POINT('Ctrl Pts',(1.79365032105972,-8.9533294379193,19.6401104814683));
#59364=CARTESIAN_POINT('Ctrl Pts',(1.79398945985935,-8.93459602169225,19.6486722691969));
#59365=CARTESIAN_POINT('Ctrl Pts',(1.79575501944583,-8.8916929748512,19.6683014889756));
#59366=CARTESIAN_POINT('Ctrl Pts',(1.79749007695656,-8.86729071242315,19.679481451683));
#59367=CARTESIAN_POINT('Ctrl Pts',(1.80455267777006,-8.80012268196332,19.7103243426951));
#59368=CARTESIAN_POINT('Ctrl Pts',(1.81186451913824,-8.75567295717225,19.7308068537822));
#59369=CARTESIAN_POINT('Ctrl Pts',(1.8357835522898,-8.6655408027488,19.7728605743248));
#59370=CARTESIAN_POINT('Ctrl Pts',(1.85214505346338,-8.62643565005096,19.7914686907898));
#59371=CARTESIAN_POINT('Ctrl Pts',(1.88061329933222,-8.58294107520611,19.8130641352128));
#59372=CARTESIAN_POINT('Ctrl Pts',(1.89448595076454,-8.56525519087471,19.8220366846582));
#59373=CARTESIAN_POINT('Ctrl Pts',(1.92022261572012,-8.54803282135671,19.8319176857523));
#59374=CARTESIAN_POINT('Ctrl Pts',(1.92864558703646,-8.54389492576558,19.8345024437447));
#59375=CARTESIAN_POINT('Ctrl Pts',(1.94192278721308,-8.54037467545699,19.8372829641462));
#59376=CARTESIAN_POINT('Ctrl Pts',(1.94616291414767,-8.5396427768739,19.8380018808868));
#59377=CARTESIAN_POINT('Ctrl Pts',(1.95291207287856,-8.53914154119839,19.8388604862844));
#59378=CARTESIAN_POINT('Ctrl Pts',(1.95533909579901,-8.53909210866278,19.8391129317611));
#59379=CARTESIAN_POINT('Ctrl Pts',(1.95776807072638,-8.5391735580698,19.8393092308925));
#59380=CARTESIAN_POINT('',(1.65494820650842,-12.2959121221581,20.8349473401973));
#59381=CARTESIAN_POINT('Origin',(1.65494820650842,-9.9949023346812,21.8857832998643));
#59382=CARTESIAN_POINT('',(1.36757616935991,-12.0085309043509,20.9273996982545));
#59383=CARTESIAN_POINT('Origin',(1.6653400148523,-12.0237188108135,20.9606565744588));
#59384=CARTESIAN_POINT('Origin',(1.36757616935991,-9.98024447851016,21.8536870719015));
#59385=CARTESIAN_POINT('Origin',(1.65494820650842,-9.9949023346812,21.8857832998643));
#59386=CARTESIAN_POINT('Origin',(6.4980472271939,-10.24193210686,22.4267030489007));
#59387=CARTESIAN_POINT('',(11.664677238709,-9.78032664122358,20.2056359204057));
#59388=CARTESIAN_POINT('Ctrl Pts',(11.664677238709,-9.78032664122359,20.2056359204057));
#59389=CARTESIAN_POINT('Ctrl Pts',(8.44908820479151,-9.65515767378836,19.9536710841398));
#59390=CARTESIAN_POINT('Ctrl Pts',(5.17648536371074,-9.52748760709608,19.697374593167));
#59391=CARTESIAN_POINT('Ctrl Pts',(1.95776807072638,-9.40158004320576,19.4454613857581));
#59392=CARTESIAN_POINT('',(11.3203626311916,-13.0982396153547,21.7732001549839));
#59393=CARTESIAN_POINT('Origin',(11.3203626311916,-10.4879017784557,22.9653015014543));
#59394=CARTESIAN_POINT('',(11.664677238709,-8.86564886390743,20.6233552648184));
#59395=CARTESIAN_POINT('Origin',(11.3203626311916,-10.4879017784557,22.9653015014543));
#59396=CARTESIAN_POINT('Ctrl Pts',(1.95776807072638,-8.5391735580698,19.8393092308925));
#59397=CARTESIAN_POINT('Ctrl Pts',(5.17648535775567,-8.64710493744507,20.0994318861236));
#59398=CARTESIAN_POINT('Ctrl Pts',(8.44908819833864,-8.7571947878114,20.3637569928305));
#59399=CARTESIAN_POINT('Ctrl Pts',(11.664677238709,-8.86564886390743,20.6233552648184));
#59400=CARTESIAN_POINT('Origin',(11.3307544395355,-10.4884318287472,22.9664621496957));
#59401=CARTESIAN_POINT('',(11.6285182850279,-12.8412342104726,21.9321662654496));
#59402=CARTESIAN_POINT('Origin',(11.6285182850279,-10.5036197352098,22.9997190259));
#59403=CARTESIAN_POINT('Origin',(11.3307544395355,-12.8260463040101,21.8989093892453));
#59404=CARTESIAN_POINT('Ctrl Pts',(11.664677238709,-8.86564886390743,20.6233552648184));
#59405=CARTESIAN_POINT('Ctrl Pts',(11.6681531449969,-8.86576609785752,20.6236358788069));
#59406=CARTESIAN_POINT('Ctrl Pts',(11.6716331726355,-8.86616731353295,20.6237948130829));
#59407=CARTESIAN_POINT('Ctrl Pts',(11.6751111337893,-8.86685375084358,20.623830903915));
#59408=CARTESIAN_POINT('Ctrl Pts',(11.6835034416364,-8.86851012162341,20.6239179909639));
#59409=CARTESIAN_POINT('Ctrl Pts',(11.6913221163004,-8.87170945339749,20.6232869878783));
#59410=CARTESIAN_POINT('Ctrl Pts',(11.7093237578239,-8.88207391467147,20.6205407109361));
#59411=CARTESIAN_POINT('Ctrl Pts',(11.7187565997267,-8.89041824124023,20.6178443174412));
#59412=CARTESIAN_POINT('Ctrl Pts',(11.7431727782354,-8.91707792401486,20.6086622526054));
#59413=CARTESIAN_POINT('Ctrl Pts',(11.7560898230283,-8.9391731957824,20.6003233906747));
#59414=CARTESIAN_POINT('Ctrl Pts',(11.7841758181737,-8.99805910753514,20.5773806426634));
#59415=CARTESIAN_POINT('Ctrl Pts',(11.7988195826634,-9.04537291470731,20.5580695606802));
#59416=CARTESIAN_POINT('Ctrl Pts',(11.8183861888449,-9.14332972967485,20.5165359590653));
#59417=CARTESIAN_POINT('Ctrl Pts',(11.8239771978735,-9.18842241074048,20.4969162334911));
#59418=CARTESIAN_POINT('Ctrl Pts',(11.8302306705076,-9.27219438300235,20.4597498600097));
#59419=CARTESIAN_POINT('Ctrl Pts',(11.8313291886565,-9.31273094134293,20.4414345067909));
#59420=CARTESIAN_POINT('Ctrl Pts',(11.8301000822046,-9.39324349826429,20.4044483831864));
#59421=CARTESIAN_POINT('Ctrl Pts',(11.8275983467483,-9.43446674805149,20.3851769035864));
#59422=CARTESIAN_POINT('Ctrl Pts',(11.8179490511515,-9.51988766495155,20.344508477833));
#59423=CARTESIAN_POINT('Ctrl Pts',(11.8098404493788,-9.56648167385494,20.3218506008119));
#59424=CARTESIAN_POINT('Ctrl Pts',(11.7817370234731,-9.66788637809189,20.2711283205783));
#59425=CARTESIAN_POINT('Ctrl Pts',(11.7608617911999,-9.71153922107345,20.2481472837838));
#59426=CARTESIAN_POINT('Ctrl Pts',(11.727864569176,-9.75179858555561,20.2255615388921));
#59427=CARTESIAN_POINT('Ctrl Pts',(11.7163738956147,-9.76278438208105,20.2191422746271));
#59428=CARTESIAN_POINT('Ctrl Pts',(11.6949981921877,-9.77494241482736,20.2111886963504));
#59429=CARTESIAN_POINT('Ctrl Pts',(11.6861739271888,-9.77828873356616,20.2087116448862));
#59430=CARTESIAN_POINT('Ctrl Pts',(11.6727399598044,-9.78026828421812,20.2064478679052));
#59431=CARTESIAN_POINT('Ctrl Pts',(11.6686987410324,-9.78048318090824,20.2059510344218));
#59432=CARTESIAN_POINT('Ctrl Pts',(11.664677238709,-9.78032664122358,20.2056359204057));
#59433=CARTESIAN_POINT('Origin',(11.6285182850279,-10.5036197352098,22.9997190259));
#59434=CARTESIAN_POINT('Origin',(1.06052702375292,-11.0190788716665,24.1284170944427));
#59435=CARTESIAN_POINT('Origin',(1.6653400148523,-3.42428246167523,23.8164076546558));
#59436=CARTESIAN_POINT('',(1.95776807072638,-3.54233043715926,21.3065147522487));
#59437=CARTESIAN_POINT('',(1.95776807072638,-2.60389771385557,21.4414410082343));
#59438=CARTESIAN_POINT('Ctrl Pts',(1.95776807072638,-3.54233043715926,21.3065147522487));
#59439=CARTESIAN_POINT('Ctrl Pts',(1.9513478551886,-3.54223103321939,21.3059618726496));
#59440=CARTESIAN_POINT('Ctrl Pts',(1.94501663599474,-3.54115156508234,21.3055798899085));
#59441=CARTESIAN_POINT('Ctrl Pts',(1.92952577557711,-3.53620362915065,21.3050279766057));
#59442=CARTESIAN_POINT('Ctrl Pts',(1.92095957337031,-3.53135931038363,21.3050724139772));
#59443=CARTESIAN_POINT('Ctrl Pts',(1.90072805817451,-3.51599592158736,21.3058205399649));
#59444=CARTESIAN_POINT('Ctrl Pts',(1.8900249560485,-3.5036082187607,21.3069139518805));
#59445=CARTESIAN_POINT('Ctrl Pts',(1.86013121923956,-3.460751246541,21.3112847102786));
#59446=CARTESIAN_POINT('Ctrl Pts',(1.84584490211046,-3.42403619031247,21.3159449618369));
#59447=CARTESIAN_POINT('Ctrl Pts',(1.82200825445925,-3.35110430677949,21.3254531739389));
#59448=CARTESIAN_POINT('Ctrl Pts',(1.81203215259484,-3.30105316932589,21.3323795986619));
#59449=CARTESIAN_POINT('Ctrl Pts',(1.79984169249385,-3.21193645609613,21.3448875851979));
#59450=CARTESIAN_POINT('Ctrl Pts',(1.79638078494031,-3.16936789071313,21.3509444797466));
#59451=CARTESIAN_POINT('Ctrl Pts',(1.793278948137,-3.08828446690857,21.3625442583892));
#59452=CARTESIAN_POINT('Ctrl Pts',(1.79337026915323,-3.04840338066611,21.36827974357));
#59453=CARTESIAN_POINT('Ctrl Pts',(1.79687828838527,-2.96705307114361,21.3800426367112));
#59454=CARTESIAN_POINT('Ctrl Pts',(1.80059938175366,-2.9241782817627,21.3862765917232));
#59455=CARTESIAN_POINT('Ctrl Pts',(1.81351118858407,-2.83463727606628,21.3994816448112));
#59456=CARTESIAN_POINT('Ctrl Pts',(1.82404219007376,-2.78419034711654,21.4070273995978));
#59457=CARTESIAN_POINT('Ctrl Pts',(1.84885798811656,-2.71258004937708,21.418374529977));
#59458=CARTESIAN_POINT('Ctrl Pts',(1.86388962647735,-2.67578411025365,21.4243315771977));
#59459=CARTESIAN_POINT('Ctrl Pts',(1.89490216133889,-2.63563438874777,21.4320245979053));
#59460=CARTESIAN_POINT('Ctrl Pts',(1.90722460488827,-2.62233152903652,21.4347412883592));
#59461=CARTESIAN_POINT('Ctrl Pts',(1.92907437017015,-2.60993293818409,21.4381786237551));
#59462=CARTESIAN_POINT('Ctrl Pts',(1.93579728934589,-2.60716195128727,21.439108054393));
#59463=CARTESIAN_POINT('Ctrl Pts',(1.94779808654528,-2.60440407097886,21.440500869962));
#59464=CARTESIAN_POINT('Ctrl Pts',(1.95276363818101,-2.60385064352413,21.4410056766482));
#59465=CARTESIAN_POINT('Ctrl Pts',(1.95776807072638,-2.60389771385557,21.4414410082343));
#59466=CARTESIAN_POINT('',(1.65494820650842,-5.92795829958165,23.4551443394205));
#59467=CARTESIAN_POINT('Origin',(1.65494820650842,-3.42410087454152,23.8151446883994));
#59468=CARTESIAN_POINT('',(1.36757616935991,-5.62617120112542,23.4628870820895));
#59469=CARTESIAN_POINT('Origin',(1.6653400148523,-5.63137434589457,23.4990757488526));
#59470=CARTESIAN_POINT('Origin',(1.36757616935991,-3.41907931690608,23.7802189878927));
#59471=CARTESIAN_POINT('Origin',(1.65494820650842,-3.42410087454152,23.8151446883994));
#59472=CARTESIAN_POINT('Origin',(6.4980472271939,-3.50872950127858,24.4037497162211));
#59473=CARTESIAN_POINT('',(11.664677238709,-3.69156922144577,22.1426021244183));
#59474=CARTESIAN_POINT('Ctrl Pts',(11.664677238709,-3.69156922144575,22.1426021244183));
#59475=CARTESIAN_POINT('Ctrl Pts',(8.45131537604982,-3.64249119006552,21.8657713317644));
#59476=CARTESIAN_POINT('Ctrl Pts',(5.17772237568178,-3.5921848606183,21.5838024904321));
#59477=CARTESIAN_POINT('Ctrl Pts',(1.95776807072638,-3.54233043715926,21.3065147522487));
#59478=CARTESIAN_POINT('',(11.3203626311916,-6.43344952736807,24.5814330987647));
#59479=CARTESIAN_POINT('Origin',(11.3203626311916,-3.59299495374821,24.98982881153));
#59480=CARTESIAN_POINT('',(11.664677238709,-2.69625718204607,22.2857063914358));
#59481=CARTESIAN_POINT('Origin',(11.3203626311916,-3.59299495374821,24.98982881153));
#59482=CARTESIAN_POINT('Ctrl Pts',(1.95776807072638,-2.60389771385557,21.4414410082343));
#59483=CARTESIAN_POINT('Ctrl Pts',(5.17772236984729,-2.63418372824733,21.7215422583742));
#59484=CARTESIAN_POINT('Ctrl Pts',(8.45131536953639,-2.66535496122479,22.0062623111724));
#59485=CARTESIAN_POINT('Ctrl Pts',(11.664677238709,-2.69625718204608,22.2857063914358));
#59486=CARTESIAN_POINT('Origin',(11.3307544395355,-3.59317654088192,24.9910917777863));
#59487=CARTESIAN_POINT('',(11.6285182850279,-6.14206871845015,24.6615531749599));
#59488=CARTESIAN_POINT('Origin',(11.6285182850279,-3.59837968565107,25.0272804445494));
#59489=CARTESIAN_POINT('Origin',(11.3307544395355,-6.136865573681,24.6253645081968));
#59490=CARTESIAN_POINT('Ctrl Pts',(11.664677238709,-2.69625718204609,22.2857063914358));
#59491=CARTESIAN_POINT('Ctrl Pts',(11.6681739314188,-2.69629080899963,22.2860104748593));
#59492=CARTESIAN_POINT('Ctrl Pts',(11.6716539907384,-2.69663467728557,22.2862755639135));
#59493=CARTESIAN_POINT('Ctrl Pts',(11.6751111337893,-2.69727925957649,22.2865022196842));
#59494=CARTESIAN_POINT('Ctrl Pts',(11.6834715430146,-2.69883805296518,22.2870503413465));
#59495=CARTESIAN_POINT('Ctrl Pts',(11.6912510114763,-2.70206385531499,22.2873454247033));
#59496=CARTESIAN_POINT('Ctrl Pts',(11.709035822972,-2.71261693877732,22.2876313864347));
#59497=CARTESIAN_POINT('Ctrl Pts',(11.7183186554656,-2.72116951930901,22.2874079360076));
#59498=CARTESIAN_POINT('Ctrl Pts',(11.7418333015259,-2.74801369053582,22.2861920544586));
#59499=CARTESIAN_POINT('Ctrl Pts',(11.7542369034695,-2.7699680354384,22.2845703704499));
#59500=CARTESIAN_POINT('Ctrl Pts',(11.7824157539259,-2.83096774741543,22.2794147158946));
#59501=CARTESIAN_POINT('Ctrl Pts',(11.797437382068,-2.88153241037179,22.2742976507484));
#59502=CARTESIAN_POINT('Ctrl Pts',(11.8209603099608,-3.00475150470514,22.2601056375114));
#59503=CARTESIAN_POINT('Ctrl Pts',(11.8274214370012,-3.07312747241122,22.2513392489145));
#59504=CARTESIAN_POINT('Ctrl Pts',(11.8323708659761,-3.20740533159261,22.2328342493678));
#59505=CARTESIAN_POINT('Ctrl Pts',(11.8303885473322,-3.27899188856714,22.2222076907846));
#59506=CARTESIAN_POINT('Ctrl Pts',(11.8177935569394,-3.40658761118928,22.2018688414514));
#59507=CARTESIAN_POINT('Ctrl Pts',(11.8075558566742,-3.4692947461111,22.1912401030955));
#59508=CARTESIAN_POINT('Ctrl Pts',(11.7765253671338,-3.57657231689547,22.1714404504546));
#59509=CARTESIAN_POINT('Ctrl Pts',(11.7586671916647,-3.61570515885675,22.1634661165603));
#59510=CARTESIAN_POINT('Ctrl Pts',(11.7297382659251,-3.65639661653946,22.1542106095143));
#59511=CARTESIAN_POINT('Ctrl Pts',(11.7183817710579,-3.66905637710909,22.1511082048343));
#59512=CARTESIAN_POINT('Ctrl Pts',(11.6971067724022,-3.68375234586312,22.1467808943914));
#59513=CARTESIAN_POINT('Ctrl Pts',(11.688166617688,-3.68804578318867,22.1452727334554));
#59514=CARTESIAN_POINT('Ctrl Pts',(11.6739702938601,-3.69116836143547,22.1434932346172));
#59515=CARTESIAN_POINT('Ctrl Pts',(11.6693161741268,-3.69164007241986,22.1430017682255));
#59516=CARTESIAN_POINT('Ctrl Pts',(11.664677238709,-3.69156922144579,22.1426021244183));
#59517=CARTESIAN_POINT('Origin',(11.6285182850279,-3.59837968565107,25.0272804445494));
#59518=CARTESIAN_POINT('Origin',(1.06052702375292,-3.77496811251421,26.2554799311097));
#59519=CARTESIAN_POINT('Origin',(1.6653400148523,3.42428246167523,23.8164076546558));
#59520=CARTESIAN_POINT('',(1.95776807072638,2.60389771385558,21.4414410082343));
#59521=CARTESIAN_POINT('',(1.95776807072638,3.54233043715926,21.3065147522487));
#59522=CARTESIAN_POINT('Ctrl Pts',(1.95776807072638,2.60389771385558,21.4414410082343));
#59523=CARTESIAN_POINT('Ctrl Pts',(1.95134785518859,2.60383732705436,21.4408825188176));
#59524=CARTESIAN_POINT('Ctrl Pts',(1.94501663599474,2.60476545217276,21.4402118877432));
#59525=CARTESIAN_POINT('Ctrl Pts',(1.92952577557707,2.6093574699872,21.4382883361661));
#59526=CARTESIAN_POINT('Ctrl Pts',(1.92095957337023,2.61401807926046,21.4369661711994));
#59527=CARTESIAN_POINT('Ctrl Pts',(1.90072805817454,2.62896991430866,21.4333556260207));
#59528=CARTESIAN_POINT('Ctrl Pts',(1.89002495604858,2.64116387786459,21.4309147278802));
#59529=CARTESIAN_POINT('Ctrl Pts',(1.86013121923974,2.68351622651848,21.4230342354906));
#59530=CARTESIAN_POINT('Ctrl Pts',(1.84584490211065,2.72005700958236,21.4171618874503));
#59531=CARTESIAN_POINT('Ctrl Pts',(1.82200825445924,2.79271341229181,21.4057376641306));
#59532=CARTESIAN_POINT('Ctrl Pts',(1.81203215259483,2.842688526347,21.398282485057));
#59533=CARTESIAN_POINT('Ctrl Pts',(1.79984169249385,2.93171929355019,21.3851767307768));
#59534=CARTESIAN_POINT('Ctrl Pts',(1.79638078494032,2.97426995731976,21.3789953277719));
#59535=CARTESIAN_POINT('Ctrl Pts',(1.79327894813701,3.05533696803247,21.367281393569));
#59536=CARTESIAN_POINT('Ctrl Pts',(1.79337026915323,3.09521846296703,21.3615487509036));
#59537=CARTESIAN_POINT('Ctrl Pts',(1.79687828838528,3.17658750331596,21.3499161335203));
#59538=CARTESIAN_POINT('Ctrl Pts',(1.80059938175367,3.21948187055682,21.3438183455158));
#59539=CARTESIAN_POINT('Ctrl Pts',(1.81351118858406,3.30911612974249,21.331261884693));
#59540=CARTESIAN_POINT('Ctrl Pts',(1.82404219007375,3.35964548839958,21.3242894411135));
#59541=CARTESIAN_POINT('Ctrl Pts',(1.84885798811638,3.43155192197307,21.3150019807047));
#59542=CARTESIAN_POINT('Ctrl Pts',(1.8638896264772,3.46853566116457,21.3103511116458));
#59543=CARTESIAN_POINT('Ctrl Pts',(1.89490216133104,3.50922641122572,21.3064210272653));
#59544=CARTESIAN_POINT('Ctrl Pts',(1.90722460488041,3.52275579180111,21.3052798239866));
#59545=CARTESIAN_POINT('Ctrl Pts',(1.92907437017047,3.53562056190136,21.3050848364448));
#59546=CARTESIAN_POINT('Ctrl Pts',(1.93579728934604,3.53854115522866,21.305195941388));
#59547=CARTESIAN_POINT('Ctrl Pts',(1.94779808654526,3.54157972349806,21.3057553534692));
#59548=CARTESIAN_POINT('Ctrl Pts',(1.952763638181,3.54225295373072,21.3060837934058));
#59549=CARTESIAN_POINT('Ctrl Pts',(1.95776807072638,3.54233043715926,21.3065147522487));
#59550=CARTESIAN_POINT('',(1.65494820650842,0.920243449501388,24.1751450373783));
#59551=CARTESIAN_POINT('Origin',(1.65494820650842,3.42410087454152,23.8151446883994));
#59552=CARTESIAN_POINT('',(1.36757616935991,1.21198743268674,24.0975508936959));
#59553=CARTESIAN_POINT('Origin',(1.6653400148523,1.21719057745589,24.133739560459));
#59554=CARTESIAN_POINT('Origin',(1.36757616935991,3.41907931690608,23.7802189878927));
#59555=CARTESIAN_POINT('Origin',(1.65494820650842,3.42410087454152,23.8151446883994));
#59556=CARTESIAN_POINT('Origin',(6.4980472271939,3.50872950127858,24.4037497162211));
#59557=CARTESIAN_POINT('',(11.664677238709,2.69625718204608,22.2857063914358));
#59558=CARTESIAN_POINT('Ctrl Pts',(11.664677238709,2.69625718204609,22.2857063914358));
#59559=CARTESIAN_POINT('Ctrl Pts',(8.45131537604982,2.66535496128743,22.0062623117388));
#59560=CARTESIAN_POINT('Ctrl Pts',(5.17772237568179,2.63418372830221,21.7215422588817));
#59561=CARTESIAN_POINT('Ctrl Pts',(1.95776807072638,2.60389771385557,21.4414410082343));
#59562=CARTESIAN_POINT('',(11.3203626311916,0.752540380128346,25.3982245242953));
#59563=CARTESIAN_POINT('Origin',(11.3203626311916,3.59299495374821,24.98982881153));
#59564=CARTESIAN_POINT('',(11.664677238709,3.69156922144577,22.1426021244183));
#59565=CARTESIAN_POINT('Origin',(11.3203626311916,3.59299495374821,24.98982881153));
#59566=CARTESIAN_POINT('Ctrl Pts',(1.95776807072638,3.54233043715926,21.3065147522487));
#59567=CARTESIAN_POINT('Ctrl Pts',(5.17772236984729,3.59218486052797,21.5838024899296));
#59568=CARTESIAN_POINT('Ctrl Pts',(8.45131536953639,3.64249118996605,21.8657713312033));
#59569=CARTESIAN_POINT('Ctrl Pts',(11.664677238709,3.69156922144575,22.1426021244183));
#59570=CARTESIAN_POINT('Origin',(11.3307544395355,3.59317654088192,24.9910917777863));
#59571=CARTESIAN_POINT('',(11.6285182850279,1.054690652852,25.393007714139));
#59572=CARTESIAN_POINT('Origin',(11.6285182850279,3.59837968565108,25.0272804445494));
#59573=CARTESIAN_POINT('Origin',(11.3307544395355,1.04948750808285,25.3568190473759));
#59574=CARTESIAN_POINT('Ctrl Pts',(11.664677238709,3.69156922144577,22.1426021244183));
#59575=CARTESIAN_POINT('Ctrl Pts',(11.6681739314189,3.69162262682054,22.1429033641341));
#59576=CARTESIAN_POINT('Ctrl Pts',(11.6716539907386,3.6913673718333,22.1432545941104));
#59577=CARTESIAN_POINT('Ctrl Pts',(11.6751111337893,3.69081275596405,22.1436536685467));
#59578=CARTESIAN_POINT('Ctrl Pts',(11.6834715430145,3.68947152837768,22.1446187502773));
#59579=CARTESIAN_POINT('Ctrl Pts',(11.6912510114761,3.68645952827754,22.1458106942287));
#59580=CARTESIAN_POINT('Ctrl Pts',(11.7090358229721,3.67641448357504,22.1490582196872));
#59581=CARTESIAN_POINT('Ctrl Pts',(11.7183186554658,3.66814538938823,22.1512533609532));
#59582=CARTESIAN_POINT('Ctrl Pts',(11.7418333015259,3.6420460422962,22.1576496081462));
#59583=CARTESIAN_POINT('Ctrl Pts',(11.7542369034695,3.62052412143971,22.1622788674576));
#59584=CARTESIAN_POINT('Ctrl Pts',(11.7824157539258,3.56054281066528,22.1745176579593));
#59585=CARTESIAN_POINT('Ctrl Pts',(11.797437382068,3.51058472799836,22.1838535816865));
#59586=CARTESIAN_POINT('Ctrl Pts',(11.8209603099608,3.38835852059419,22.2049512752024));
#59587=CARTESIAN_POINT('Ctrl Pts',(11.8274214370012,3.32028248294247,22.215803723148));
#59588=CARTESIAN_POINT('Ctrl Pts',(11.8323708659761,3.18623035970919,22.2358787507006));
#59589=CARTESIAN_POINT('Ctrl Pts',(11.8303885473322,3.11454971376682,22.2458509061382));
#59590=CARTESIAN_POINT('Ctrl Pts',(11.8177935569394,2.9863923984218,22.2622837922879));
#59591=CARTESIAN_POINT('Ctrl Pts',(11.8075558566742,2.92323088143582,22.2697522339709));
#59592=CARTESIAN_POINT('Ctrl Pts',(11.7765253671337,2.8147205992782,22.2809781906907));
#59593=CARTESIAN_POINT('Ctrl Pts',(11.7586671916645,2.77492628290187,22.2843518689721));
#59594=CARTESIAN_POINT('Ctrl Pts',(11.7297382659251,2.73327553750452,22.2869353834087));
#59595=CARTESIAN_POINT('Ctrl Pts',(11.7183817710578,2.7202545377875,22.2875253146313));
#59596=CARTESIAN_POINT('Ctrl Pts',(11.6971067724021,2.70493471479212,22.287513623519));
#59597=CARTESIAN_POINT('Ctrl Pts',(11.688166617688,2.70039029380911,22.2872761547731));
#59598=CARTESIAN_POINT('Ctrl Pts',(11.6739702938601,2.69689285916418,22.2864484700947));
#59599=CARTESIAN_POINT('Ctrl Pts',(11.6693161741268,2.69630179370592,22.2861098078869));
#59600=CARTESIAN_POINT('Ctrl Pts',(11.664677238709,2.69625718204608,22.2857063914358));
#59601=CARTESIAN_POINT('Origin',(11.6285182850279,3.59837968565108,25.0272804445494));
#59602=CARTESIAN_POINT('Origin',(1.06052702375292,3.77496811251421,26.2554799311097));
#59603=CARTESIAN_POINT('Origin',(1.6653400148523,9.99543238497271,21.8869439481057));
#59604=CARTESIAN_POINT('',(1.95776807072638,8.53917355806981,19.8393092308925));
#59605=CARTESIAN_POINT('',(1.95776807072638,9.40158004320575,19.4454613857581));
#59606=CARTESIAN_POINT('Ctrl Pts',(1.95776807072638,8.53917355806979,19.8393092308925));
#59607=CARTESIAN_POINT('Ctrl Pts',(1.95134736181104,8.53895825616285,19.8387903372766));
#59608=CARTESIAN_POINT('Ctrl Pts',(1.94501567122259,8.53965997172072,19.8378852898847));
#59609=CARTESIAN_POINT('Ctrl Pts',(1.92948836979272,8.54353347509978,19.8347384067269));
#59610=CARTESIAN_POINT('Ctrl Pts',(1.92089186233936,8.54765577357339,19.8321439694453));
#59611=CARTESIAN_POINT('Ctrl Pts',(1.90046800930124,8.56114336986575,19.8243804604409));
#59612=CARTESIAN_POINT('Ctrl Pts',(1.88964186308543,8.57236355197253,19.8185013079907));
#59613=CARTESIAN_POINT('Ctrl Pts',(1.85810283833411,8.61322946498717,19.7977884699131));
#59614=CARTESIAN_POINT('Ctrl Pts',(1.84335629303613,8.64977779572247,19.7804322617419));
#59615=CARTESIAN_POINT('Ctrl Pts',(1.81854010589151,8.72212855294431,19.7463114584517));
#59616=CARTESIAN_POINT('Ctrl Pts',(1.8083691782646,8.77440559157947,19.7221699251049));
#59617=CARTESIAN_POINT('Ctrl Pts',(1.79896764765282,8.85022287567161,19.6873082756821));
#59618=CARTESIAN_POINT('Ctrl Pts',(1.79670145400052,8.87696000159275,19.6750497681665));
#59619=CARTESIAN_POINT('Ctrl Pts',(1.79434535609109,8.92267523692494,19.6541233115618));
#59620=CARTESIAN_POINT('Ctrl Pts',(1.7938155730381,8.94195225085063,19.6453095312538));
#59621=CARTESIAN_POINT('Ctrl Pts',(1.79365032105971,8.97982124967058,19.6280120764218));
#59622=CARTESIAN_POINT('Ctrl Pts',(1.79398945985935,8.99855959580194,19.6194610836778));
#59623=CARTESIAN_POINT('Ctrl Pts',(1.79575501944583,9.04148989103746,19.5998915295602));
#59624=CARTESIAN_POINT('Ctrl Pts',(1.79749007695656,9.06591922657839,19.588770848701));
#59625=CARTESIAN_POINT('Ctrl Pts',(1.80455267777006,9.13321443405714,19.558206436516));
#59626=CARTESIAN_POINT('Ctrl Pts',(1.81186451913824,9.17780246249336,19.5380267681685));
#59627=CARTESIAN_POINT('Ctrl Pts',(1.83578355229015,9.2686085526925,19.4974487611264));
#59628=CARTESIAN_POINT('Ctrl Pts',(1.85214505346393,9.30828005778674,19.4800807834258));
#59629=CARTESIAN_POINT('Ctrl Pts',(1.88061329933267,9.35308369492278,19.4613517855849));
#59630=CARTESIAN_POINT('Ctrl Pts',(1.89448595076488,9.37144648654037,19.4538614563447));
#59631=CARTESIAN_POINT('Ctrl Pts',(1.92022261572016,9.39019230245401,19.4473163375408));
#59632=CARTESIAN_POINT('Ctrl Pts',(1.92864558703649,9.39485547755034,19.445881781225));
#59633=CARTESIAN_POINT('Ctrl Pts',(1.94192278721305,9.39926212836099,19.4450422071836));
#59634=CARTESIAN_POINT('Ctrl Pts',(1.94616291414765,9.40028474102504,19.4449598654854));
#59635=CARTESIAN_POINT('Ctrl Pts',(1.95291207287644,9.40126187125082,19.4451433237977));
#59636=CARTESIAN_POINT('Ctrl Pts',(1.95533909579739,9.40148502823919,19.4452712818101));
#59637=CARTESIAN_POINT('Ctrl Pts',(1.95776807072638,9.40158004320578,19.4454613857581));
#59638=CARTESIAN_POINT('',(1.65494820650842,7.69389254720435,22.9366192595313));
#59639=CARTESIAN_POINT('Origin',(1.65494820650842,9.99490233468121,21.8857832998643));
#59640=CARTESIAN_POINT('',(1.36757616935991,7.95195805266942,22.7799744455484));
#59641=CARTESIAN_POINT('Origin',(1.6653400148523,7.96714595913197,22.8132313217527));
#59642=CARTESIAN_POINT('Origin',(1.36757616935991,9.98024447851016,21.8536870719015));
#59643=CARTESIAN_POINT('Origin',(1.65494820650842,9.99490233468121,21.8857832998643));
#59644=CARTESIAN_POINT('Origin',(6.4980472271939,10.24193210686,22.4267030489007));
#59645=CARTESIAN_POINT('',(11.664677238709,8.86564886390743,20.6233552648184));
#59646=CARTESIAN_POINT('Ctrl Pts',(11.664677238709,8.86564886390742,20.6233552648184));
#59647=CARTESIAN_POINT('Ctrl Pts',(8.44908820479151,8.75719478802903,20.3637569933514));
#59648=CARTESIAN_POINT('Ctrl Pts',(5.17648536371074,8.64710493764475,20.0994318866049));
#59649=CARTESIAN_POINT('Ctrl Pts',(1.95776807072638,8.53917355806979,19.8393092308925));
#59650=CARTESIAN_POINT('',(11.3203626311916,7.87756394155674,24.1574028479247));
#59651=CARTESIAN_POINT('Origin',(11.3203626311916,10.4879017784557,22.9653015014543));
#59652=CARTESIAN_POINT('',(11.664677238709,9.78032664122359,20.2056359204057));
#59653=CARTESIAN_POINT('Origin',(11.3203626311916,10.4879017784557,22.9653015014543));
#59654=CARTESIAN_POINT('Ctrl Pts',(1.95776807072638,9.40158004320577,19.4454613857581));
#59655=CARTESIAN_POINT('Ctrl Pts',(5.17648535775567,9.52748760686315,19.6973745927009));
#59656=CARTESIAN_POINT('Ctrl Pts',(8.44908819833864,9.65515767353719,19.9536710836342));
#59657=CARTESIAN_POINT('Ctrl Pts',(11.664677238709,9.7803266412236,20.2056359204057));
#59658=CARTESIAN_POINT('Origin',(11.3307544395355,10.4884318287472,22.9664621496957));
#59659=CARTESIAN_POINT('',(11.6285182850279,8.16600525994691,24.0672717863504));
#59660=CARTESIAN_POINT('Origin',(11.6285182850279,10.5036197352098,22.9997190259));
#59661=CARTESIAN_POINT('Origin',(11.3307544395355,8.15081735348436,24.0340149101461));
#59662=CARTESIAN_POINT('Ctrl Pts',(11.664677238709,9.78032664122359,20.2056359204057));
#59663=CARTESIAN_POINT('Ctrl Pts',(11.6681531449969,9.78046194321534,20.205908282996));
#59664=CARTESIAN_POINT('Ctrl Pts',(11.6716331726355,9.7803193173351,20.2063155813886));
#59665=CARTESIAN_POINT('Ctrl Pts',(11.6751111337893,9.77989707212502,20.2068579905627));
#59666=CARTESIAN_POINT('Ctrl Pts',(11.6835034416363,9.77887819594063,20.2081668219633));
#59667=CARTESIAN_POINT('Ctrl Pts',(11.6913221163002,9.77630619887362,20.210171496446));
#59668=CARTESIAN_POINT('Ctrl Pts',(11.709323757824,9.76744342252662,20.2162060047083));
#59669=CARTESIAN_POINT('Ctrl Pts',(11.7187565997267,9.7599412524694,20.2207464637378));
#59670=CARTESIAN_POINT('Ctrl Pts',(11.7431727782355,9.73554353144946,20.2348815339297));
#59671=CARTESIAN_POINT('Ctrl Pts',(11.7560898230284,9.7147721142082,20.2461192329191));
#59672=CARTESIAN_POINT('Ctrl Pts',(11.7841758181731,9.65887107077625,20.2755979308595));
#59673=CARTESIAN_POINT('Ctrl Pts',(11.798819582663,9.61329277429722,20.2987092511699));
#59674=CARTESIAN_POINT('Ctrl Pts',(11.8183861888449,9.51775570080864,20.3455413475508));
#59675=CARTESIAN_POINT('Ctrl Pts',(11.8239771978735,9.47339867533874,20.3667719341834));
#59676=CARTESIAN_POINT('Ctrl Pts',(11.8302306705076,9.39045122916063,20.4057437679469));
#59677=CARTESIAN_POINT('Ctrl Pts',(11.8313291886565,9.35006360841491,20.4243852490072));
#59678=CARTESIAN_POINT('Ctrl Pts',(11.8301000822046,9.26938684912612,20.4610118195814));
#59679=CARTESIAN_POINT('Ctrl Pts',(11.8275983467482,9.22782694901014,20.4795461377865));
#59680=CARTESIAN_POINT('Ctrl Pts',(11.8179490511515,9.141152999222,20.5174708042373));
#59681=CARTESIAN_POINT('Ctrl Pts',(11.8098404493788,9.0935167314396,20.5378464526579));
#59682=CARTESIAN_POINT('Ctrl Pts',(11.7817370234727,8.98877743069939,20.5812669850618));
#59683=CARTESIAN_POINT('Ctrl Pts',(11.7608617911994,8.94282298913066,20.599208223942));
#59684=CARTESIAN_POINT('Ctrl Pts',(11.7278645691761,8.89938954507017,20.6148437040365));
#59685=CARTESIAN_POINT('Ctrl Pts',(11.7163738956147,8.88734402205844,20.6189424909766));
#59686=CARTESIAN_POINT('Ctrl Pts',(11.6949981921877,8.87337129041363,20.6229224329418));
#59687=CARTESIAN_POINT('Ctrl Pts',(11.6861739271888,8.86930788707863,20.6238292881645));
#59688=CARTESIAN_POINT('Ctrl Pts',(11.6727399598044,8.86630070859597,20.6238428740718));
#59689=CARTESIAN_POINT('Ctrl Pts',(11.6686987410323,8.86578449949815,20.6236799254143));
#59690=CARTESIAN_POINT('Ctrl Pts',(11.664677238709,8.86564886390743,20.6233552648184));
#59691=CARTESIAN_POINT('Origin',(11.6285182850279,10.5036197352098,22.9997190259));
#59692=CARTESIAN_POINT('Origin',(1.06052702375292,11.0190788716665,24.1284170944427));
#59693=CARTESIAN_POINT('Origin',(1.6653400148523,15.756811821565,18.1843302095478));
#59694=CARTESIAN_POINT('',(1.95776807072638,13.7826563450298,16.6299146085789));
#59695=CARTESIAN_POINT('',(1.95776807072638,14.4991695475011,16.0090523844052));
#59696=CARTESIAN_POINT('Ctrl Pts',(1.95776807072638,13.7826563450298,16.6299146085789));
#59697=CARTESIAN_POINT('Ctrl Pts',(1.95134736178812,13.7823035751365,16.6294773913556));
#59698=CARTESIAN_POINT('Ctrl Pts',(1.94501567118683,13.7827218849757,16.628411308616));
#59699=CARTESIAN_POINT('Ctrl Pts',(1.92948836979218,13.7855519048067,16.6243006043356));
#59700=CARTESIAN_POINT('Ctrl Pts',(1.92089186233878,13.7887762837785,16.6206498743044));
#59701=CARTESIAN_POINT('Ctrl Pts',(1.90046800930057,13.7995303044103,16.6094009469748));
#59702=CARTESIAN_POINT('Ctrl Pts',(1.88964186308468,13.8086396416528,16.6005988509147));
#59703=CARTESIAN_POINT('Ctrl Pts',(1.858102838333,13.8420147172205,16.5692117701535));
#59704=CARTESIAN_POINT('Ctrl Pts',(1.84335629303492,13.8721927748541,16.5422617556975));
#59705=CARTESIAN_POINT('Ctrl Pts',(1.8185401058909,13.9319998768916,16.4891395208651));
#59706=CARTESIAN_POINT('Ctrl Pts',(1.80836917826425,13.975357872227,16.4512477454883));
#59707=CARTESIAN_POINT('Ctrl Pts',(1.79896764765271,14.0382823619637,16.3964380405191));
#59708=CARTESIAN_POINT('Ctrl Pts',(1.79670145400044,14.060482825754,16.3771433698427));
#59709=CARTESIAN_POINT('Ctrl Pts',(1.79434535609105,14.0984506087175,16.3441851116311));
#59710=CARTESIAN_POINT('Ctrl Pts',(1.79381557303809,14.1144636392699,16.3302973889329));
#59711=CARTESIAN_POINT('Ctrl Pts',(1.79365032105973,14.1459254213784,16.303031672698));
#59712=CARTESIAN_POINT('Ctrl Pts',(1.79398945985937,14.1614956397794,16.2895478530761));
#59713=CARTESIAN_POINT('Ctrl Pts',(1.79575501944589,14.1971735758954,16.2586761415607));
#59714=CARTESIAN_POINT('Ctrl Pts',(1.79749007695665,14.2174802938449,16.2411233872504));
#59715=CARTESIAN_POINT('Ctrl Pts',(1.80455267777032,14.2734385825861,16.1928377976495));
#59716=CARTESIAN_POINT('Ctrl Pts',(1.81186451913869,14.3105352130186,16.1609136484041));
#59717=CARTESIAN_POINT('Ctrl Pts',(1.83578355229124,14.3862308728513,16.0963963037948));
#59718=CARTESIAN_POINT('Ctrl Pts',(1.85214505346546,14.4194022784773,16.0685550966611));
#59719=CARTESIAN_POINT('Ctrl Pts',(1.88061329933466,14.4571144850523,16.0379621115844));
#59720=CARTESIAN_POINT('Ctrl Pts',(1.89448595076662,14.4726231849761,16.0256017970759));
#59721=CARTESIAN_POINT('Ctrl Pts',(1.92022261572143,14.4887656905737,16.0140404949253));
#59722=CARTESIAN_POINT('Ctrl Pts',(1.9286455870375,14.4928358130943,16.0113502799774));
#59723=CARTESIAN_POINT('Ctrl Pts',(1.94192278721348,14.4968274282426,16.009303217584));
#59724=CARTESIAN_POINT('Ctrl Pts',(1.94616291414806,14.4977854195713,16.0089361080226));
#59725=CARTESIAN_POINT('Ctrl Pts',(1.95291207281715,14.4987746553279,16.0088368455883));
#59726=CARTESIAN_POINT('Ctrl Pts',(1.95533909575199,14.4990248228342,16.0088967498094));
#59727=CARTESIAN_POINT('Ctrl Pts',(1.95776807072638,14.4991695475011,16.0090523844052));
#59728=CARTESIAN_POINT('',(1.65494820650842,13.8442282280737,19.8399049986041));
#59729=CARTESIAN_POINT('Origin',(1.65494820650842,15.755976249638,18.1833659081392));
#59730=CARTESIAN_POINT('',(1.36757616935991,14.0477083233403,19.6168999455472));
#59731=CARTESIAN_POINT('Origin',(1.6653400148523,14.0716505576406,19.6445307568688));
#59732=CARTESIAN_POINT('Origin',(1.36757616935991,15.7328695872647,18.1566993982262));
#59733=CARTESIAN_POINT('Origin',(1.65494820650842,15.755976249638,18.1833659081392));
#59734=CARTESIAN_POINT('Origin',(6.4980472271939,16.1453942842592,18.6327782772971));
#59735=CARTESIAN_POINT('',(11.664677238709,14.316798400859,17.2902225464619));
#59736=CARTESIAN_POINT('Ctrl Pts',(11.664677238709,14.316798400859,17.2902225464619));
#59737=CARTESIAN_POINT('Ctrl Pts',(8.44646649976651,14.1394557206779,17.0715167051139));
#59738=CARTESIAN_POINT('Ctrl Pts',(5.17487115867276,13.9594120777672,16.848982766429));
#59739=CARTESIAN_POINT('Ctrl Pts',(1.95776807072638,13.7826563450298,16.6299146085789));
#59740=CARTESIAN_POINT('',(11.3203626311916,14.3643941221169,20.959492062422));
#59741=CARTESIAN_POINT('Origin',(11.3203626311916,16.5331411750263,19.0802620436378));
#59742=CARTESIAN_POINT('',(11.664677238709,15.0767401623716,16.6317292616657));
#59743=CARTESIAN_POINT('Origin',(11.3203626311916,16.5331411750263,19.0802620436378));
#59744=CARTESIAN_POINT('Ctrl Pts',(1.95776807072638,14.4991695475011,16.0090523844052));
#59745=CARTESIAN_POINT('Ctrl Pts',(5.17487115257265,14.6908529434927,16.2151856477085));
#59746=CARTESIAN_POINT('Ctrl Pts',(8.44646649340719,14.8854989256118,16.4250665874126));
#59747=CARTESIAN_POINT('Ctrl Pts',(11.664677238709,15.0767401623716,16.6317292616657));
#59748=CARTESIAN_POINT('Origin',(11.3307544395355,16.5339767469533,19.0812263450464));
#59749=CARTESIAN_POINT('',(11.6285182850279,14.6157586859842,20.7917486320082));
#59750=CARTESIAN_POINT('Origin',(11.6285182850279,16.5579189812536,19.1088571563679));
#59751=CARTESIAN_POINT('Origin',(11.3307544395355,14.5918164516839,20.7641178206866));
#59752=CARTESIAN_POINT('Ctrl Pts',(11.664677238709,15.0767401623717,16.6317292616657));
#59753=CARTESIAN_POINT('Ctrl Pts',(11.6681719057553,15.0769478319436,16.6319536774341));
#59754=CARTESIAN_POINT('Ctrl Pts',(11.6716519636861,15.076923254483,16.6323869095799));
#59755=CARTESIAN_POINT('Ctrl Pts',(11.6751111337893,15.0766722907899,16.6330228529951));
#59756=CARTESIAN_POINT('Ctrl Pts',(11.6833639439589,15.0760735472598,16.6345400724807));
#59757=CARTESIAN_POINT('Ctrl Pts',(11.6912209922802,15.0742040415111,16.6371623459815));
#59758=CARTESIAN_POINT('Ctrl Pts',(11.7092716451021,15.0673685087776,16.6454839841325));
#59759=CARTESIAN_POINT('Ctrl Pts',(11.7188321121789,15.0614159673375,16.6519996438999));
#59760=CARTESIAN_POINT('Ctrl Pts',(11.7448362096952,15.0406027082649,16.6738751139891));
#59761=CARTESIAN_POINT('Ctrl Pts',(11.7582763496127,15.0220383775034,16.6921848294481));
#59762=CARTESIAN_POINT('Ctrl Pts',(11.7901173768955,14.9694389699155,16.743176931564));
#59763=CARTESIAN_POINT('Ctrl Pts',(11.807496900688,14.9187368040621,16.7905186715073));
#59764=CARTESIAN_POINT('Ctrl Pts',(11.8229354401012,14.8329485272452,16.8679921932309));
#59765=CARTESIAN_POINT('Ctrl Pts',(11.826199199177,14.8064785162731,16.8916135343912));
#59766=CARTESIAN_POINT('Ctrl Pts',(11.8295237141305,14.7632021791261,16.9298134645279));
#59767=CARTESIAN_POINT('Ctrl Pts',(11.8303434615844,14.7461967949088,16.9447232097654));
#59768=CARTESIAN_POINT('Ctrl Pts',(11.8309946485842,14.7141892768628,16.9725964133233));
#59769=CARTESIAN_POINT('Ctrl Pts',(11.8309459330901,14.6991103672785,16.9856519542831));
#59770=CARTESIAN_POINT('Ctrl Pts',(11.8300359252892,14.6661973816187,17.0139777482936));
#59771=CARTESIAN_POINT('Ctrl Pts',(11.8290394062419,14.648205145668,17.0293561720866));
#59772=CARTESIAN_POINT('Ctrl Pts',(11.8249644421306,14.6008656924252,17.0695195134069));
#59773=CARTESIAN_POINT('Ctrl Pts',(11.8209395722477,14.5708013862499,17.0947280327935));
#59774=CARTESIAN_POINT('Ctrl Pts',(11.8028867656277,14.4800669368877,17.1697247641798));
#59775=CARTESIAN_POINT('Ctrl Pts',(11.7841990134601,14.4273818427204,17.2117750105268));
#59776=CARTESIAN_POINT('Ctrl Pts',(11.7507704380578,14.3734252802354,17.2529915779606));
#59777=CARTESIAN_POINT('Ctrl Pts',(11.7371459986441,14.3544245174278,17.2672530332855));
#59778=CARTESIAN_POINT('Ctrl Pts',(11.7101248465183,14.3325674214145,17.2823211517672));
#59779=CARTESIAN_POINT('Ctrl Pts',(11.700195678653,14.3262661007535,17.2864153990732));
#59780=CARTESIAN_POINT('Ctrl Pts',(11.6812735959896,14.3191264193213,17.290180232345));
#59781=CARTESIAN_POINT('Ctrl Pts',(11.6731643433662,14.3172676724499,17.2907980108076));
#59782=CARTESIAN_POINT('Ctrl Pts',(11.6646867061662,14.3167989230148,17.2902231894927));
#59783=CARTESIAN_POINT('Ctrl Pts',(11.664681972407,14.3167986617141,17.2902228681585));
#59784=CARTESIAN_POINT('Ctrl Pts',(11.664677238709,14.316798400859,17.2902225464619));
#59785=CARTESIAN_POINT('Origin',(11.6285182850279,16.5579189812536,19.1088571563679));
#59786=CARTESIAN_POINT('Origin',(1.06052702375292,17.3704893936218,20.0466134020057));
#59787=CARTESIAN_POINT('Origin',(1.6653400148523,20.2416680737422,13.0085301837882));
#59788=CARTESIAN_POINT('',(1.95776807072638,17.9095502835289,12.0732632065885));
#59789=CARTESIAN_POINT('',(1.95776807072638,18.4221225649395,11.2756851683683));
#59790=CARTESIAN_POINT('Ctrl Pts',(1.95776807072638,17.9095502835289,12.0732632065885));
#59791=CARTESIAN_POINT('Ctrl Pts',(1.9513473618362,17.9090886249722,12.0729430865012));
#59792=CARTESIAN_POINT('Ctrl Pts',(1.94501567126187,17.9091896400968,12.0718023361232));
#59793=CARTESIAN_POINT('Ctrl Pts',(1.92948836979327,17.9107469050198,12.0670608355043));
#59794=CARTESIAN_POINT('Ctrl Pts',(1.92089186233992,17.9128121444813,12.062649573159));
#59795=CARTESIAN_POINT('Ctrl Pts',(1.90046800930197,17.919961362657,12.0488265486971));
#59796=CARTESIAN_POINT('Ctrl Pts',(1.88964186308624,17.9262218707066,12.0378146025024));
#59797=CARTESIAN_POINT('Ctrl Pts',(1.85810283833519,17.9494022586918,11.9982960736772));
#59798=CARTESIAN_POINT('Ctrl Pts',(1.84335629303728,17.9707651964678,11.9639355828322));
#59799=CARTESIAN_POINT('Ctrl Pts',(1.81854010589216,18.0131834276005,11.8961155639935));
#59800=CARTESIAN_POINT('Ctrl Pts',(1.80836917826496,18.0441097727155,11.847543312875));
#59801=CARTESIAN_POINT('Ctrl Pts',(1.79896764765298,18.0890437001662,11.7772259086882));
#59802=CARTESIAN_POINT('Ctrl Pts',(1.79670145400061,18.1049089522812,11.752458214319));
#59803=CARTESIAN_POINT('Ctrl Pts',(1.79434535609112,18.1320533589037,11.7101382365699));
#59804=CARTESIAN_POINT('Ctrl Pts',(1.79381557303812,18.1435051255807,11.6923016721812));
#59805=CARTESIAN_POINT('Ctrl Pts',(1.79365032105971,18.1660108445023,11.6572766007167));
#59806=CARTESIAN_POINT('Ctrl Pts',(1.79398945985933,18.1771515286776,11.6399523330915));
#59807=CARTESIAN_POINT('Ctrl Pts',(1.79575501944576,18.2026866914743,11.6002795066447));
#59808=CARTESIAN_POINT('Ctrl Pts',(1.79749007695644,18.2172256623124,11.5777166986477));
#59809=CARTESIAN_POINT('Ctrl Pts',(1.80455267776979,18.2573136245575,11.5156217429365));
#59810=CARTESIAN_POINT('Ctrl Pts',(1.81186451913778,18.2839135086097,11.4745394175059));
#59811=CARTESIAN_POINT('Ctrl Pts',(1.83578355228877,18.3383663258933,11.3913095468929));
#59812=CARTESIAN_POINT('Ctrl Pts',(1.85214505346194,18.362350282045,11.3552506393501));
#59813=CARTESIAN_POINT('Ctrl Pts',(1.88061329933071,18.3899158393675,11.3152721287423));
#59814=CARTESIAN_POINT('Ctrl Pts',(1.89448595076315,18.4013140249655,11.2990431881352));
#59815=CARTESIAN_POINT('Ctrl Pts',(1.92022261571902,18.4135454504488,11.2834023305783));
#59816=CARTESIAN_POINT('Ctrl Pts',(1.9286455870355,18.4166927832737,11.2796744022134));
#59817=CARTESIAN_POINT('Ctrl Pts',(1.94192278721223,18.4199459858402,11.2765856922883));
#59818=CARTESIAN_POINT('Ctrl Pts',(1.94616291414703,18.4207617450735,11.275963555897));
#59819=CARTESIAN_POINT('Ctrl Pts',(1.9529120729776,18.4216829443939,11.2755896143607));
#59820=CARTESIAN_POINT('Ctrl Pts',(1.9553390958748,18.4219398553151,11.2755766117231));
#59821=CARTESIAN_POINT('Ctrl Pts',(1.95776807072638,18.4221225649395,11.2756851683683));
#59822=CARTESIAN_POINT('',(1.65494820650842,18.8729868727,15.1358796271483));
#59823=CARTESIAN_POINT('Origin',(1.65494820650842,20.2405946732479,13.0078403511776));
#59824=CARTESIAN_POINT('',(1.36757616935991,19.0053968105924,14.8645808781538));
#59825=CARTESIAN_POINT('Origin',(1.6653400148523,19.0361537152975,14.8843471405862));
#59826=CARTESIAN_POINT('Origin',(1.36757616935991,20.2109111690372,12.9887639213558));
#59827=CARTESIAN_POINT('Origin',(1.65494820650842,20.2405946732479,13.0078403511776));
#59828=CARTESIAN_POINT('Origin',(6.4980472271939,20.7408526371047,13.3293366230661));
#59829=CARTESIAN_POINT('',(11.664677238709,18.6080860766515,12.5563388263038));
#59830=CARTESIAN_POINT('Ctrl Pts',(11.664677238709,18.6080860766515,12.5563388263039));
#59831=CARTESIAN_POINT('Ctrl Pts',(8.44760841234031,18.3763927057865,12.3965120461773));
#59832=CARTESIAN_POINT('Ctrl Pts',(5.17558411912346,18.1409160622912,12.2336952666484));
#59833=CARTESIAN_POINT('Ctrl Pts',(1.95776807072638,17.9095502835289,12.0732632065885));
#59834=CARTESIAN_POINT('',(11.3203626311916,19.6875065192443,16.0635678809207));
#59835=CARTESIAN_POINT('Origin',(11.3203626311916,21.2389637999728,13.6494532297333));
#59836=CARTESIAN_POINT('',(11.664677238709,19.1517258603906,11.7104188108481));
#59837=CARTESIAN_POINT('Origin',(11.3203626311916,21.2389637999728,13.6494532297333));
#59838=CARTESIAN_POINT('Ctrl Pts',(1.95776807072638,18.4221225649395,11.2756851683683));
#59839=CARTESIAN_POINT('Ctrl Pts',(5.17558411308691,18.6641695173893,11.4194969967751));
#59840=CARTESIAN_POINT('Ctrl Pts',(8.44760840593806,18.9100934023218,11.5660575512547));
#59841=CARTESIAN_POINT('Ctrl Pts',(11.664677238709,19.1517258603906,11.710418810848));
#59842=CARTESIAN_POINT('Origin',(11.3307544395355,21.2400372004671,13.6501430623439));
#59843=CARTESIAN_POINT('',(11.6285182850279,19.8814302665469,15.831801656791));
#59844=CARTESIAN_POINT('Origin',(11.6285182850279,21.2707941051722,13.6699093247763));
#59845=CARTESIAN_POINT('Origin',(11.3307544395355,19.8506733618418,15.8120353943587));
#59846=CARTESIAN_POINT('Ctrl Pts',(11.664677238709,19.1517258603906,11.710418810848));
#59847=CARTESIAN_POINT('Ctrl Pts',(11.6681719057553,19.151988343114,11.7105756289215));
#59848=CARTESIAN_POINT('Ctrl Pts',(11.6716519636862,19.1520868168133,11.7109982363921));
#59849=CARTESIAN_POINT('Ctrl Pts',(11.6751111337893,19.1520251848775,11.7116791242736));
#59850=CARTESIAN_POINT('Ctrl Pts',(11.6833639439589,19.1518781447924,11.713303571255));
#59851=CARTESIAN_POINT('Ctrl Pts',(11.6912209922801,19.1508231469805,11.7163463248885));
#59852=CARTESIAN_POINT('Ctrl Pts',(11.7092716451022,19.1466089777452,11.7262566703379));
#59853=CARTESIAN_POINT('Ctrl Pts',(11.7188321121789,19.142733229544,11.7341854248228));
#59854=CARTESIAN_POINT('Ctrl Pts',(11.7448362096952,19.1289260858262,11.7610385573625));
#59855=CARTESIAN_POINT('Ctrl Pts',(11.7582763496126,19.1162721838521,11.7838367770656));
#59856=CARTESIAN_POINT('Ctrl Pts',(11.7901173768954,19.0801695571631,11.8475823063438));
#59857=CARTESIAN_POINT('Ctrl Pts',(11.8074969006879,19.0448588947193,11.9072908240011));
#59858=CARTESIAN_POINT('Ctrl Pts',(11.8229354401012,18.9843724592575,12.0057954743111));
#59859=CARTESIAN_POINT('Ctrl Pts',(11.826199199177,18.9656295705593,12.0359174490527));
#59860=CARTESIAN_POINT('Ctrl Pts',(11.8295237141305,18.9348683931316,12.0847623667266));
#59861=CARTESIAN_POINT('Ctrl Pts',(11.8303434615844,18.9227524071091,12.103859132896));
#59862=CARTESIAN_POINT('Ctrl Pts',(11.8309946485842,18.8998942073469,12.139620835759));
#59863=CARTESIAN_POINT('Ctrl Pts',(11.8309459330901,18.8891042704865,12.1563957553283));
#59864=CARTESIAN_POINT('Ctrl Pts',(11.8300359252892,18.8655047903765,12.1928468152565));
#59865=CARTESIAN_POINT('Ctrl Pts',(11.8290394062419,18.8525739690576,12.2126713034689));
#59866=CARTESIAN_POINT('Ctrl Pts',(11.8249644421306,18.8184674171377,12.2645448124642));
#59867=CARTESIAN_POINT('Ctrl Pts',(11.8209395722477,18.7967229872269,12.2972023035393));
#59868=CARTESIAN_POINT('Ctrl Pts',(11.8028867656277,18.7307929414874,12.3947239887609));
#59869=CARTESIAN_POINT('Ctrl Pts',(11.7841990134601,18.6920888872387,12.4499140109568));
#59870=CARTESIAN_POINT('Ctrl Pts',(11.7507704380581,18.6519299935817,12.5046623381128));
#59871=CARTESIAN_POINT('Ctrl Pts',(11.7371459986443,18.6377168114473,12.5236992377786));
#59872=CARTESIAN_POINT('Ctrl Pts',(11.7101248465184,18.6209902609454,12.5443148471325));
#59873=CARTESIAN_POINT('Ctrl Pts',(11.700195678653,18.6160976708085,12.5500185358362));
#59874=CARTESIAN_POINT('Ctrl Pts',(11.6812735959896,18.6103078727442,12.5556423476123));
#59875=CARTESIAN_POINT('Ctrl Pts',(11.6731643433662,18.6086984664872,12.556758771215));
#59876=CARTESIAN_POINT('Ctrl Pts',(11.6646867061662,18.608086758819,12.5563392961791));
#59877=CARTESIAN_POINT('Ctrl Pts',(11.6646819724071,18.6080864175726,12.5563390614781));
#59878=CARTESIAN_POINT('Ctrl Pts',(11.664677238709,18.6080860766515,12.5563388263038));
#59879=CARTESIAN_POINT('Origin',(11.6285182850279,21.2707941051722,13.6699093247763));
#59880=CARTESIAN_POINT('Origin',(1.06052702375292,22.314646171184,14.3407523135387));
#59881=CARTESIAN_POINT('Origin',(1.6653400148523,23.0866647604201,6.77885640724594));
#59882=CARTESIAN_POINT('',(1.95776807072638,20.5855189702533,6.53850782206133));
#59883=CARTESIAN_POINT('',(1.95776807072638,20.8526247727479,5.62882899907204));
#59884=CARTESIAN_POINT('Ctrl Pts',(1.95776807072638,20.5855189702533,6.53850782206133));
#59885=CARTESIAN_POINT('Ctrl Pts',(1.9513480833199,20.58498588377,6.53833075323157));
#59886=CARTESIAN_POINT('Ctrl Pts',(1.94501708197863,20.5847614100627,6.53720798413881));
#59887=CARTESIAN_POINT('Ctrl Pts',(1.92954226703964,20.5849190653624,6.53223717834333));
#59888=CARTESIAN_POINT('Ctrl Pts',(1.9209894073484,20.5856501048189,6.52745980301691));
#59889=CARTESIAN_POINT('Ctrl Pts',(1.90083817145052,20.5885608974198,6.51243359052771));
#59890=CARTESIAN_POINT('Ctrl Pts',(1.89018614013953,20.5913816029711,6.50042022104901));
#59891=CARTESIAN_POINT('Ctrl Pts',(1.86077829279052,20.6015952674743,6.45943708811552));
#59892=CARTESIAN_POINT('Ctrl Pts',(1.84665745875882,20.611140107964,6.42475570918836));
#59893=CARTESIAN_POINT('Ctrl Pts',(1.82247517384536,20.6308899331518,6.35397716493558));
#59894=CARTESIAN_POINT('Ctrl Pts',(1.81230887643135,20.6450040326066,6.30493959671585));
#59895=CARTESIAN_POINT('Ctrl Pts',(1.79934881945864,20.6714274602751,6.21380591728078));
#59896=CARTESIAN_POINT('Ctrl Pts',(1.79572382774455,20.6848492864753,6.16787314051173));
#59897=CARTESIAN_POINT('Ctrl Pts',(1.79301769946659,20.7108870248761,6.07902063442843));
#59898=CARTESIAN_POINT('Ctrl Pts',(1.79378222861411,20.7240558919591,6.03421247801754));
#59899=CARTESIAN_POINT('Ctrl Pts',(1.7998218767273,20.7504816712267,5.94463801772135));
#59900=CARTESIAN_POINT('Ctrl Pts',(1.8054507297311,20.7644003702175,5.89763253003153));
#59901=CARTESIAN_POINT('Ctrl Pts',(1.82510992022202,20.7940525831188,5.79870751723029));
#59902=CARTESIAN_POINT('Ctrl Pts',(1.83960979646949,20.8080958899669,5.75272231990244));
#59903=CARTESIAN_POINT('Ctrl Pts',(1.86695154341265,20.8259464835343,5.69674419663866));
#59904=CARTESIAN_POINT('Ctrl Pts',(1.88252298601309,20.8347457609889,5.66966644865797));
#59905=CARTESIAN_POINT('Ctrl Pts',(1.91281431352699,20.8446460331123,5.64327836389123));
#59906=CARTESIAN_POINT('Ctrl Pts',(1.92253441500524,20.8472499388906,5.63690645398473));
#59907=CARTESIAN_POINT('Ctrl Pts',(1.93813933311943,20.8501988666455,5.63122599523098));
#59908=CARTESIAN_POINT('Ctrl Pts',(1.94311288783775,20.8509861372018,5.62997943255931));
#59909=CARTESIAN_POINT('Ctrl Pts',(1.95140011063542,20.8520210777582,5.6289276697355));
#59910=CARTESIAN_POINT('Ctrl Pts',(1.95458052113192,20.8523545794652,5.6287598616145));
#59911=CARTESIAN_POINT('Ctrl Pts',(1.95776807072638,20.8526247727479,5.62882899907202));
#59912=CARTESIAN_POINT('',(1.65494820650842,22.3727683628749,9.20563530484314));
#59913=CARTESIAN_POINT('Origin',(1.65494820650842,23.0854404918828,6.7784969295689));
#59914=CARTESIAN_POINT('',(1.36757616935991,22.4233810776973,8.90802187107886));
#59915=CARTESIAN_POINT('Origin',(1.6653400148523,22.4584609113062,8.9183222395943));
#59916=CARTESIAN_POINT('Origin',(1.36757616935991,23.0515849268112,6.7685560387305));
#59917=CARTESIAN_POINT('Origin',(1.65494820650842,23.0854404918828,6.7784969295689));
#59918=CARTESIAN_POINT('Origin',(6.4980472271939,23.6560104598922,6.94603138825146));
#59919=CARTESIAN_POINT('',(11.664677238709,21.3918572850628,6.805215209861));
#59920=CARTESIAN_POINT('Ctrl Pts',(11.664677238709,21.3918572850628,6.805215209861));
#59921=CARTESIAN_POINT('Ctrl Pts',(8.45037669575292,21.1247507590271,6.71721389334346));
#59922=CARTESIAN_POINT('Ctrl Pts',(5.17722936343352,20.8528483573768,6.62730336128235));
#59923=CARTESIAN_POINT('Ctrl Pts',(1.95776807072638,20.5855189702533,6.53850782206133));
#59924=CARTESIAN_POINT('',(11.3203626311916,23.4156542242922,9.86626896342395));
#59925=CARTESIAN_POINT('Origin',(11.3203626311916,24.2241318908269,7.11284689157994));
#59926=CARTESIAN_POINT('',(11.664677238709,21.6751526289,5.84039987251778));
#59927=CARTESIAN_POINT('Origin',(11.3203626311916,24.2241318908269,7.11284689157994));
#59928=CARTESIAN_POINT('Ctrl Pts',(1.95776807072638,20.8526247727479,5.62882899907203));
#59929=CARTESIAN_POINT('Ctrl Pts',(5.17722935754855,21.1255230565072,5.69865861625942));
#59930=CARTESIAN_POINT('Ctrl Pts',(8.45037668926196,21.4028712159812,5.77002260020614));
#59931=CARTESIAN_POINT('Ctrl Pts',(11.664677238709,21.6751526289,5.84039987251777));
#59932=CARTESIAN_POINT('Origin',(11.3307544395355,24.2253561593642,7.11320636925698));
#59933=CARTESIAN_POINT('',(11.6285182850279,23.5364266063324,9.58925626669054));
#59934=CARTESIAN_POINT('Origin',(11.6285182850279,24.2604359929731,7.12350673777241));
#59935=CARTESIAN_POINT('Origin',(11.3307544395355,23.5013467727236,9.57895589817511));
#59936=CARTESIAN_POINT('Ctrl Pts',(11.664677238709,21.6751526289,5.84039987251778));
#59937=CARTESIAN_POINT('Ctrl Pts',(11.6681756837601,21.6754489800181,5.84047647114826));
#59938=CARTESIAN_POINT('Ctrl Pts',(11.6716557442405,21.6756623521125,5.84085486706167));
#59939=CARTESIAN_POINT('Ctrl Pts',(11.6751111337893,21.6757948999659,5.84152480494111));
#59940=CARTESIAN_POINT('Ctrl Pts',(11.6834492137325,21.6761147465654,5.84314140866026));
#59941=CARTESIAN_POINT('Ctrl Pts',(11.6912528317941,21.6759503372767,5.84637491140685));
#59942=CARTESIAN_POINT('Ctrl Pts',(11.7091239528621,21.6747209936006,5.85692922382961));
#59943=CARTESIAN_POINT('Ctrl Pts',(11.718489115776,21.6732669685549,5.86544860786681));
#59944=CARTESIAN_POINT('Ctrl Pts',(11.7423632180108,21.6681303692968,5.89238136827878));
#59945=CARTESIAN_POINT('Ctrl Pts',(11.7550185107735,21.6632424395397,5.91454378047491));
#59946=CARTESIAN_POINT('Ctrl Pts',(11.782945606649,21.6493229837906,5.97457704224723));
#59947=CARTESIAN_POINT('Ctrl Pts',(11.7977324484725,21.637177726309,6.02338974579153));
#59948=CARTESIAN_POINT('Ctrl Pts',(11.8194386441993,21.6078719961958,6.13462845786581));
#59949=CARTESIAN_POINT('Ctrl Pts',(11.825673894872,21.5920955534044,6.19191044279121));
#59950=CARTESIAN_POINT('Ctrl Pts',(11.8317749863308,21.5603242616104,6.30356890402402));
#59951=CARTESIAN_POINT('Ctrl Pts',(11.8316012176116,21.5432716658125,6.36154350871869));
#59952=CARTESIAN_POINT('Ctrl Pts',(11.824941361477,21.50960504634,6.47243556191222));
#59953=CARTESIAN_POINT('Ctrl Pts',(11.8183083548574,21.4918876839749,6.529013179409));
#59954=CARTESIAN_POINT('Ctrl Pts',(11.795821624489,21.4564286561113,6.637989474794));
#59955=CARTESIAN_POINT('Ctrl Pts',(11.7805655796944,21.4404704012147,6.68472301424652));
#59956=CARTESIAN_POINT('Ctrl Pts',(11.7536264417725,21.4211446949061,6.73846169515414));
#59957=CARTESIAN_POINT('Ctrl Pts',(11.7402881749119,21.412752167224,6.76120915401804));
#59958=CARTESIAN_POINT('Ctrl Pts',(11.7136982696185,21.4020408829817,6.78732748838213));
#59959=CARTESIAN_POINT('Ctrl Pts',(11.7035133274598,21.398679437698,6.79496994538257));
#59960=CARTESIAN_POINT('Ctrl Pts',(11.6842762528669,21.3943170183099,6.80313984330724));
#59961=CARTESIAN_POINT('Ctrl Pts',(11.6760378533014,21.3929463221456,6.80507051068837));
#59962=CARTESIAN_POINT('Ctrl Pts',(11.6665534479108,21.3920199943286,6.80524520977619));
#59963=CARTESIAN_POINT('Ctrl Pts',(11.6656136423373,21.3919350996656,6.80524084677671));
#59964=CARTESIAN_POINT('Ctrl Pts',(11.664677238709,21.3918572850628,6.805215209861));
#59965=CARTESIAN_POINT('Origin',(11.6285182850279,24.2604359929731,7.12350673777241));
#59966=CARTESIAN_POINT('Origin',(1.06052702375292,25.4510030262676,7.47308876036672));
#59967=CARTESIAN_POINT('Origin',(1.6653400148523,24.0613171698908,0.));
#59968=CARTESIAN_POINT('',(1.95776807072638,21.593771336803,0.47404141979407));
#59969=CARTESIAN_POINT('',(1.95776807072638,21.593771336803,-0.47404141979407));
#59970=CARTESIAN_POINT('Ctrl Pts',(1.95776807072638,21.593771336803,0.47404141979407));
#59971=CARTESIAN_POINT('Ctrl Pts',(1.9513477680545,21.5932099304462,0.474021710346213));
#59972=CARTESIAN_POINT('Ctrl Pts',(1.94501646552415,21.5926782047131,0.473007564236366));
#59973=CARTESIAN_POINT('Ctrl Pts',(1.92951932707503,21.591427238987,0.468186519780974));
#59974=CARTESIAN_POINT('Ctrl Pts',(1.92094790453061,21.5907814463352,0.463380674959194));
#59975=CARTESIAN_POINT('Ctrl Pts',(1.90068428386471,21.5893333422069,0.448036950371891));
#59976=CARTESIAN_POINT('Ctrl Pts',(1.88996070920461,21.5886516447309,0.435581293464837));
#59977=CARTESIAN_POINT('Ctrl Pts',(1.85988430203394,21.5868688155781,0.392217225062086));
#59978=CARTESIAN_POINT('Ctrl Pts',(1.84552319454968,21.5862561010085,0.354793494140223));
#59979=CARTESIAN_POINT('Ctrl Pts',(1.82174065150271,21.5852941592389,0.280937783836869));
#59980=CARTESIAN_POINT('Ctrl Pts',(1.81181923278667,21.585029713215,0.230359404109805));
#59981=CARTESIAN_POINT('Ctrl Pts',(1.79996844463622,21.5847372703622,0.1421502207605));
#59982=CARTESIAN_POINT('Ctrl Pts',(1.79660846342306,21.5846751446254,0.101128548750127));
#59983=CARTESIAN_POINT('Ctrl Pts',(1.79344073698656,21.5846159222426,0.0237247600543095));
#59984=CARTESIAN_POINT('Ctrl Pts',(1.79332003639192,21.5846139884599,-0.0138289841184048));
#59985=CARTESIAN_POINT('Ctrl Pts',(1.79594647664003,21.5846625069698,-0.0907225510804983));
#59986=CARTESIAN_POINT('Ctrl Pts',(1.79895084940664,21.5847168190493,-0.131181998465391));
#59987=CARTESIAN_POINT('Ctrl Pts',(1.80977106001214,21.5849749085674,-0.218244549032268));
#59988=CARTESIAN_POINT('Ctrl Pts',(1.81886112579735,21.5852081198308,-0.267828304153497));
#59989=CARTESIAN_POINT('Ctrl Pts',(1.84164209107167,21.5860852333224,-0.344658261472531));
#59990=CARTESIAN_POINT('Ctrl Pts',(1.85799718988476,21.586731148623,-0.39111526813368));
#59991=CARTESIAN_POINT('Ctrl Pts',(1.89263444116559,21.588821021946,-0.438752720199368));
#59992=CARTESIAN_POINT('Ctrl Pts',(1.90520057316188,21.5896217948898,-0.453157912546355));
#59993=CARTESIAN_POINT('Ctrl Pts',(1.92760472466551,21.5912873878866,-0.466915949380981));
#59994=CARTESIAN_POINT('Ctrl Pts',(1.9346104038645,21.591831536706,-0.470078655940862));
#59995=CARTESIAN_POINT('Ctrl Pts',(1.94721684091347,21.5928636195227,-0.473331333007928));
#59996=CARTESIAN_POINT('Ctrl Pts',(1.95246882049205,21.5933079579064,-0.474025151823304));
#59997=CARTESIAN_POINT('Ctrl Pts',(1.95776807072638,21.593771336803,-0.47404141979407));
#59998=CARTESIAN_POINT('',(1.65494820650842,24.0600412162663,2.52960515816076));
#59999=CARTESIAN_POINT('Origin',(1.65494820650842,24.0600412162663,-1.54893643002411E-16));
#60000=CARTESIAN_POINT('',(1.36757616935991,24.0247563668693,2.22978791005503));
#60001=CARTESIAN_POINT('Origin',(1.6653400148523,24.0613171698908,2.22978791005503));
#60002=CARTESIAN_POINT('Origin',(1.36757616935991,24.0247563668693,0.));
#60003=CARTESIAN_POINT('Origin',(1.65494820650842,24.0600412162663,-1.54893643002411E-16));
#60004=CARTESIAN_POINT('Origin',(6.4980472271939,24.6546990029305,0.));
#60005=CARTESIAN_POINT('',(11.664677238709,22.4425874385122,0.502773529288439));
#60006=CARTESIAN_POINT('Ctrl Pts',(11.664677238709,22.4425874385122,0.502773529288439));
#60007=CARTESIAN_POINT('Ctrl Pts',(8.45174540654375,22.1616274567787,0.493593399690554));
#60008=CARTESIAN_POINT('Ctrl Pts',(5.17782841008702,21.875340981737,0.48392656300278));
#60009=CARTESIAN_POINT('Ctrl Pts',(1.95776807072638,21.593771336803,0.474041419794075));
#60010=CARTESIAN_POINT('',(11.3203626311916,25.2468048823457,2.8696636114714));
#60011=CARTESIAN_POINT('Origin',(11.3203626311916,25.2468048823457,-1.75716217820904E-16));
#60012=CARTESIAN_POINT('',(11.664677238709,22.4425874385122,-0.50277352928844));
#60013=CARTESIAN_POINT('Origin',(11.3203626311916,25.2468048823457,-1.75716217820904E-16));
#60014=CARTESIAN_POINT('Ctrl Pts',(1.95776807072638,21.593771336803,-0.474041419794078));
#60015=CARTESIAN_POINT('Ctrl Pts',(5.17782840427536,21.8753409812288,-0.483926562984941));
#60016=CARTESIAN_POINT('Ctrl Pts',(8.4517454000289,22.161627456209,-0.493593399671942));
#60017=CARTESIAN_POINT('Ctrl Pts',(11.664677238709,22.4425874385122,-0.502773529288442));
#60018=CARTESIAN_POINT('Origin',(11.3307544395355,25.2480808359702,0.));
#60019=CARTESIAN_POINT('',(11.6285182850279,25.2846416389917,2.56984636336567));
#60020=CARTESIAN_POINT('Origin',(11.6285182850279,25.2846416389917,0.));
#60021=CARTESIAN_POINT('Origin',(11.3307544395355,25.2480808359702,2.56984636336567));
#60022=CARTESIAN_POINT('Ctrl Pts',(11.664677238709,22.4425874385122,-0.502773529288416));
#60023=CARTESIAN_POINT('Ctrl Pts',(11.6681753033367,22.4428933323889,-0.50278352411193));
#60024=CARTESIAN_POINT('Ctrl Pts',(11.6716553635686,22.4432046663249,-0.502480637546283));
#60025=CARTESIAN_POINT('Ctrl Pts',(11.6751111337893,22.4435206231749,-0.501875113202017));
#60026=CARTESIAN_POINT('Ctrl Pts',(11.6835623119454,22.4442933040705,-0.500394287283524));
#60027=CARTESIAN_POINT('Ctrl Pts',(11.691384091347,22.4450491314624,-0.497199786883766));
#60028=CARTESIAN_POINT('Ctrl Pts',(11.7094694893508,22.4468652011622,-0.486572040199507));
#60029=CARTESIAN_POINT('Ctrl Pts',(11.7189285997146,22.4478827563863,-0.47778287580148));
#60030=CARTESIAN_POINT('Ctrl Pts',(11.7437048785723,22.4506469894916,-0.449218987208357));
#60031=CARTESIAN_POINT('Ctrl Pts',(11.7567586963551,22.4522625711256,-0.425077089679939));
#60032=CARTESIAN_POINT('Ctrl Pts',(11.7862943788244,22.4560498423181,-0.357948221183821));
#60033=CARTESIAN_POINT('Ctrl Pts',(11.8016138506642,22.4582634908384,-0.301713314632985));
#60034=CARTESIAN_POINT('Ctrl Pts',(11.8195646608092,22.4609621241242,-0.195134214413052));
#60035=CARTESIAN_POINT('Ctrl Pts',(11.8242738201003,22.4617066134238,-0.151903163592294));
#60036=CARTESIAN_POINT('Ctrl Pts',(11.8295027526625,22.4625362310301,-0.0759831017663084));
#60037=CARTESIAN_POINT('Ctrl Pts',(11.830683585196,22.4627272832912,-0.0420217792038241));
#60038=CARTESIAN_POINT('Ctrl Pts',(11.8310447700704,22.46278539012,0.0250506013991047));
#60039=CARTESIAN_POINT('Ctrl Pts',(11.8301786225274,22.4626451514276,0.0587303495792302));
#60040=CARTESIAN_POINT('Ctrl Pts',(11.825990760224,22.4619778159673,0.132571716988474));
#60041=CARTESIAN_POINT('Ctrl Pts',(11.8220311067205,22.4613492475643,0.173539728186971));
#60042=CARTESIAN_POINT('Ctrl Pts',(11.8081497193984,22.4592328861399,0.268683426062675));
#60043=CARTESIAN_POINT('Ctrl Pts',(11.7954615897779,22.4573293352261,0.327557844264918));
#60044=CARTESIAN_POINT('Ctrl Pts',(11.7672407996649,22.4535873444032,0.403094447780868));
#60045=CARTESIAN_POINT('Ctrl Pts',(11.7555857098412,22.4520974558946,0.428285481038826));
#60046=CARTESIAN_POINT('Ctrl Pts',(11.7315700529649,22.4492776427903,0.46416117518514));
#60047=CARTESIAN_POINT('Ctrl Pts',(11.7196350773267,22.4479351247539,0.478241088357696));
#60048=CARTESIAN_POINT('Ctrl Pts',(11.6975720132429,22.4456574568071,0.494192277150456));
#60049=CARTESIAN_POINT('Ctrl Pts',(11.6885594272653,22.4447671654469,0.498754860639004));
#60050=CARTESIAN_POINT('Ctrl Pts',(11.6741930061583,22.4434324790847,0.502225072627091));
#60051=CARTESIAN_POINT('Ctrl Pts',(11.6694225684331,22.4430024014875,0.502787087852409));
#60052=CARTESIAN_POINT('Ctrl Pts',(11.664677238709,22.4425874385122,0.502773529288416));
#60053=CARTESIAN_POINT('Origin',(11.6285182850279,25.2846416389917,0.));
#60054=CARTESIAN_POINT('Origin',(1.06052702375292,26.5254709791062,0.));
#60055=CARTESIAN_POINT('Origin',(-0.688999999999999,0.,0.));
#60056=CARTESIAN_POINT('',(-0.888999999999999,-22.3743990607509,-2.74007361925941E-15));
#60057=CARTESIAN_POINT('',(-0.688999999999999,-22.5743990607509,-2.76456655524236E-15));
#60058=CARTESIAN_POINT('Origin',(-0.888999999999999,0.,0.));
#60059=CARTESIAN_POINT('Origin',(6.67356988158431,0.,0.));
#60060=CARTESIAN_POINT('',(6.67356988158431,-22.011553150687,-2.69563781102507E-15));
#60061=CARTESIAN_POINT('',(6.67356988158431,-22.011553150687,-2.69563781102507E-15));
#60062=CARTESIAN_POINT('Origin',(15.625,0.,0.));
#60063=CARTESIAN_POINT('',(15.875,-25.3846416389917,-3.10872201306938E-15));
#60064=CARTESIAN_POINT('Origin',(15.875,0.,0.));
#60065=CARTESIAN_POINT('',(15.625,-25.6346416389917,-3.13933818304807E-15));
#60066=CARTESIAN_POINT('Origin',(15.875,18.294,0.));
#60067=CARTESIAN_POINT('',(15.875,-18.294,-2.24036885436017E-15));
#60068=CARTESIAN_POINT('Origin',(15.875,0.,0.));
#60069=CARTESIAN_POINT('Origin',(15.475,0.,0.));
#60070=CARTESIAN_POINT('',(15.075,-17.494,-2.14239711042838E-15));
#60071=CARTESIAN_POINT('',(15.475,-17.894,-2.19138298239427E-15));
#60072=CARTESIAN_POINT('Origin',(15.075,0.,0.));
#60073=CARTESIAN_POINT('Origin',(7.393,0.,0.));
#60074=CARTESIAN_POINT('',(-0.288999999999999,-17.494,-2.14239711042838E-15));
#60075=CARTESIAN_POINT('',(7.393,-17.494,-2.14239711042838E-15));
#60076=CARTESIAN_POINT('Origin',(-0.288999999999999,0.,0.));
#60077=CARTESIAN_POINT('Origin',(-0.588999999999999,0.,0.));
#60078=CARTESIAN_POINT('',(-0.889,-18.094,-2.21587591837722E-15));
#60079=CARTESIAN_POINT('',(-0.588999999999999,-17.794,-2.1791365144028E-15));
#60080=CARTESIAN_POINT('Origin',(-0.888999999999999,0.,0.));
#60081=CARTESIAN_POINT('Origin',(-0.888999999999999,22.3743990607509,0.));
#71604=UNCERTAINTY_MEASURE_WITH_UNIT(LENGTH_MEASURE(0.01),#71629,
'DISTANCE_ACCURACY_VALUE',
'Maximum model space distance between geometric entities at asserted c
onnectivities');
#71613=UNCERTAINTY_MEASURE_WITH_UNIT(LENGTH_MEASURE(0.01),#71629,
'DISTANCE_ACCURACY_VALUE',
'Maximum model space distance between geometric entities at asserted c
onnectivities');
#71619=(
GEOMETRIC_REPRESENTATION_CONTEXT(3)
GLOBAL_UNCERTAINTY_ASSIGNED_CONTEXT((#71604))
GLOBAL_UNIT_ASSIGNED_CONTEXT((#71629,#71631,#71632))
REPRESENTATION_CONTEXT('','3D')
);
#71628=(
GEOMETRIC_REPRESENTATION_CONTEXT(3)
GLOBAL_UNCERTAINTY_ASSIGNED_CONTEXT((#71613))
GLOBAL_UNIT_ASSIGNED_CONTEXT((#71629,#71631,#71632))
REPRESENTATION_CONTEXT('','3D')
);
#71629=(
LENGTH_UNIT()
NAMED_UNIT(*)
SI_UNIT(.MILLI.,.METRE.)
);
#71631=(
NAMED_UNIT(*)
PLANE_ANGLE_UNIT()
SI_UNIT($,.RADIAN.)
);
#71632=(
NAMED_UNIT(*)
SI_UNIT($,.STERADIAN.)
SOLID_ANGLE_UNIT()
);
#71638=SHAPE_DEFINITION_REPRESENTATION(#71652,#71687);
#71652=PRODUCT_DEFINITION_SHAPE('',$,#71702);
#71687=SHAPE_REPRESENTATION('',(#36394),#71619);
#71696=PRODUCT_DEFINITION_CONTEXT('part definition',#71740,'design');
#71702=PRODUCT_DEFINITION('2026-10-25-00-23-50-612',
'04_Inner_Bearing_Cone_L68149',#71716,#71696);
#71716=PRODUCT_DEFINITION_FORMATION('',$,#71747);
#71740=APPLICATION_CONTEXT(
'Core Data for Automotive Mechanical Design Process');
#71741=PRODUCT_CONTEXT('part definition',#71740,'mechanical');
#71747=PRODUCT('2026-10-25-00-23-50-612','04_Inner_Bearing_Cone_L68149',
$,(#71741));
#71812=COLOUR_RGB('Grey',0.48,0.52,0.57);
#71813=FILL_AREA_STYLE_COLOUR('',#71812);
#71814=FILL_AREA_STYLE('',(#71813));
#71815=SURFACE_STYLE_FILL_AREA(#71814);
#71816=SURFACE_SIDE_STYLE('',(#71815));
#71817=SURFACE_STYLE_USAGE(.BOTH.,#71816);
#71818=PRESENTATION_STYLE_ASSIGNMENT((#71817));
ENDSEC;
END-ISO-10303-21;
